ISO-10303-21;
HEADER;
/* Generated by software containing ST-Developer
 * from STEP Tools, Inc. (www.steptools.com) 
 */

FILE_DESCRIPTION(
/* description */ (''),
/* implementation_level */ '2;1');

FILE_NAME(
/* name */ '12_Through_Bolt_ISO_4762_M10x90.step',
/* time_stamp */ '2026-10-26T06:59:52-07:00',
/* author */ (''),
/* organization */ (''),
/* preprocessor_version */ 'ST-DEVELOPER v20.2',
/* originating_system */ 'Autodesk Translation Framework v15.15.0.0',
/* authorisation */ '');

FILE_SCHEMA (('AUTOMOTIVE_DESIGN { 1 0 10303 214 3 1 1 }'));
ENDSEC;

DATA;
#10=MECHANICAL_DESIGN_GEOMETRIC_PRESENTATION_REPRESENTATION('',(#176),#46395);
#148=SHAPE_REPRESENTATION_RELATIONSHIP('SRR','None',#46468,#162);
#162=ADVANCED_BREP_SHAPE_REPRESENTATION('',(#190),#46393);
#176=STYLED_ITEM('',(#46603),#190);
#190=MANIFOLD_SOLID_BREP('Body1',#24949);
#301=B_SPLINE_CURVE_WITH_KNOTS('',3,(#40735,#40736,#40737,#40738,#40739,
#40740,#40741,#40742,#40743,#40744,#40745,#40746,#40747,#40748,#40749,#40750),
 .UNSPECIFIED.,.F.,.F.,(4,3,3,3,3,4),(-4.09323272002465,-3.97204877033225,
-3.47554267404072,-2.97903657774919,-2.48253048145766,-2.06652207565088),
 .UNSPECIFIED.);
#302=B_SPLINE_CURVE_WITH_KNOTS('',3,(#40753,#40754,#40755,#40756,#40757,
#40758,#40759,#40760,#40761,#40762),.UNSPECIFIED.,.F.,.F.,(4,3,3,4),(0.,
0.496506096291522,0.993012192583062,1.11488200921577),.UNSPECIFIED.);
#303=B_SPLINE_CURVE_WITH_KNOTS('',3,(#40767,#40768,#40769,#40770,#40771,
#40772,#40773,#40774,#40775,#40776,#40777,#40778,#40779,#40780,#40781,#40782,
#40783,#40784,#40785,#40786,#40787,#40788,#40789,#40790,#40791,#40792,#40793,
#40794,#40795,#40796,#40797,#40798,#40799,#40800,#40801,#40802,#40803,#40804,
#40805,#40806),.UNSPECIFIED.,.F.,.F.,(4,3,3,3,3,3,3,3,3,3,3,3,3,4),(-10.3764180272042,
-9.93012192583063,-9.4336158295391,-8.93710973324757,-8.44060363695603,
-7.9440975406645,-7.44759144437297,-6.95108534808144,-6.45457925178991,
-5.95807315549838,-5.46156705920685,-4.96506096291531,-4.46855486662378,
-4.09323272002465),.UNSPECIFIED.);
#304=B_SPLINE_CURVE_WITH_KNOTS('',3,(#40807,#40808,#40809,#40810,#40811,
#40812,#40813,#40814,#40815,#40816,#40817,#40818,#40819,#40820,#40821,#40822,
#40823,#40824,#40825,#40826,#40827,#40828,#40829,#40830,#40831,#40832,#40833,
#40834,#40835,#40836,#40837,#40838,#40839,#40840,#40841,#40842,#40843,#40844,
#40845,#40846),.UNSPECIFIED.,.F.,.F.,(4,3,3,3,3,3,3,3,3,3,3,3,3,4),(1.11488200921577,
1.4895182888746,1.98602438516613,2.48253048145766,2.97903657774919,3.47554267404072,
3.97204877033226,4.46855486662379,4.96506096291532,5.46156705920685,5.95807315549838,
6.45457925178991,6.95108534808145,7.39806731639537),.UNSPECIFIED.);
#305=B_SPLINE_CURVE_WITH_KNOTS('',3,(#40851,#40852,#40853,#40854,#40855,
#40856,#40857,#40858,#40859,#40860,#40861,#40862,#40863,#40864,#40865,#40866,
#40867,#40868,#40869,#40870,#40871,#40872,#40873,#40874,#40875,#40876,#40877,
#40878,#40879,#40880,#40881,#40882,#40883,#40884,#40885,#40886,#40887,#40888,
#40889,#40890,#40891,#40892,#40893),.UNSPECIFIED.,.F.,.F.,(4,3,3,3,3,3,
3,3,3,3,3,3,3,3,4),(-16.6596033343838,-16.3847011776205,-15.888195081329,
-15.3916889850375,-14.8951828887459,-14.3986767924544,-13.9021706961629,
-13.4056645998713,-12.9091585035798,-12.4126524072883,-11.9161463109968,
-11.4196402147052,-10.9231341184137,-10.4266280221222,-10.3764180272042),
 .UNSPECIFIED.);
#306=B_SPLINE_CURVE_WITH_KNOTS('',3,(#40894,#40895,#40896,#40897,#40898,
#40899,#40900,#40901,#40902,#40903,#40904,#40905,#40906,#40907,#40908,#40909,
#40910,#40911,#40912,#40913,#40914,#40915,#40916,#40917,#40918,#40919,#40920,
#40921,#40922,#40923,#40924,#40925,#40926,#40927,#40928,#40929,#40930,#40931,
#40932,#40933,#40934,#40935,#40936),.UNSPECIFIED.,.F.,.F.,(4,3,3,3,3,3,
3,3,3,3,3,3,3,3,4),(7.39806731639537,7.44759144437298,7.94409754066451,
8.44060363695604,8.93710973324757,9.4336158295391,9.93012192583063,10.4266280221222,
10.9231341184137,11.4196402147052,11.9161463109967,12.4126524072883,12.9091585035798,
13.4056645998713,13.681252623575),.UNSPECIFIED.);
#307=B_SPLINE_CURVE_WITH_KNOTS('',3,(#40941,#40942,#40943,#40944,#40945,
#40946,#40947,#40948,#40949,#40950,#40951,#40952,#40953,#40954,#40955,#40956,
#40957,#40958,#40959,#40960,#40961,#40962,#40963,#40964,#40965,#40966,#40967,
#40968,#40969,#40970,#40971,#40972,#40973,#40974,#40975,#40976,#40977,#40978,
#40979,#40980,#40981,#40982,#40983),.UNSPECIFIED.,.F.,.F.,(4,3,3,3,3,3,
3,3,3,3,3,3,3,3,4),(-22.9427886415634,-22.8392804294104,-22.3427743331189,
-21.8462682368274,-21.3497621405359,-20.8532560442443,-20.3567499479528,
-19.8602438516613,-19.3637377553697,-18.8672316590782,-18.3707255627867,
-17.8742194664951,-17.3777133702036,-16.8812072739121,-16.6596033343838),
 .UNSPECIFIED.);
#308=B_SPLINE_CURVE_WITH_KNOTS('',3,(#40984,#40985,#40986,#40987,#40988,
#40989,#40990,#40991,#40992,#40993,#40994,#40995,#40996,#40997,#40998,#40999,
#41000,#41001,#41002,#41003,#41004,#41005,#41006,#41007,#41008,#41009,#41010,
#41011,#41012,#41013,#41014,#41015,#41016,#41017,#41018,#41019,#41020,#41021,
#41022,#41023,#41024,#41025,#41026),.UNSPECIFIED.,.F.,.F.,(4,3,3,3,3,3,
3,3,3,3,3,3,3,3,4),(13.681252623575,13.9021706961629,14.3986767924544,14.8951828887459,
15.3916889850375,15.888195081329,16.3847011776205,16.8812072739121,17.3777133702036,
17.8742194664951,18.3707255627867,18.8672316590782,19.3637377553697,19.8602438516613,
19.9644379307546),.UNSPECIFIED.);
#309=B_SPLINE_CURVE_WITH_KNOTS('',3,(#41031,#41032,#41033,#41034,#41035,
#41036,#41037,#41038,#41039,#41040,#41041,#41042,#41043,#41044,#41045,#41046,
#41047,#41048,#41049,#41050,#41051,#41052,#41053,#41054,#41055,#41056,#41057,
#41058,#41059,#41060,#41061,#41062,#41063,#41064,#41065,#41066,#41067,#41068,
#41069,#41070),.UNSPECIFIED.,.F.,.F.,(4,3,3,3,3,3,3,3,3,3,3,3,3,4),(-29.225973948743,
-28.7973535849088,-28.3008474886173,-27.8043413923258,-27.3078352960342,
-26.8113291997427,-26.3148231034512,-25.8183170071596,-25.3218109108681,
-24.8253048145766,-24.328798718285,-23.8322926219935,-23.335786525702,-22.9427886415634),
 .UNSPECIFIED.);
#310=B_SPLINE_CURVE_WITH_KNOTS('',3,(#41071,#41072,#41073,#41074,#41075,
#41076,#41077,#41078,#41079,#41080,#41081,#41082,#41083,#41084,#41085,#41086,
#41087,#41088,#41089,#41090,#41091,#41092,#41093,#41094,#41095,#41096,#41097,
#41098,#41099,#41100,#41101,#41102,#41103,#41104,#41105,#41106,#41107,#41108,
#41109,#41110),.UNSPECIFIED.,.F.,.F.,(4,3,3,3,3,3,3,3,3,3,3,3,3,4),(19.9644379307546,
20.3567499479528,20.8532560442443,21.3497621405358,21.8462682368274,22.3427743331189,
22.8392804294104,23.335786525702,23.8322926219935,24.328798718285,24.8253048145766,
25.3218109108681,25.8183170071596,26.2476232379342),.UNSPECIFIED.);
#311=B_SPLINE_CURVE_WITH_KNOTS('',3,(#41115,#41116,#41117,#41118,#41119,
#41120,#41121,#41122,#41123,#41124,#41125,#41126,#41127,#41128,#41129,#41130,
#41131,#41132,#41133,#41134,#41135,#41136,#41137,#41138,#41139,#41140,#41141,
#41142,#41143,#41144,#41145,#41146,#41147,#41148,#41149,#41150,#41151,#41152,
#41153,#41154,#41155,#41156,#41157),.UNSPECIFIED.,.F.,.F.,(4,3,3,3,3,3,
3,3,3,3,3,3,3,3,4),(-35.5091592559226,-35.2519328366987,-34.7554267404072,
-34.2589206441157,-33.7624145478241,-33.2659084515326,-32.7694023552411,
-32.2728962589495,-31.776390162658,-31.2798840663665,-30.7833779700749,
-30.2868718737834,-29.7903657774919,-29.2938596812004,-29.225973948743),
 .UNSPECIFIED.);
#312=B_SPLINE_CURVE_WITH_KNOTS('',3,(#41158,#41159,#41160,#41161,#41162,
#41163,#41164,#41165,#41166,#41167,#41168,#41169,#41170,#41171,#41172,#41173,
#41174,#41175,#41176,#41177,#41178,#41179,#41180,#41181,#41182,#41183,#41184,
#41185,#41186,#41187,#41188,#41189,#41190,#41191,#41192,#41193,#41194,#41195,
#41196,#41197,#41198,#41199,#41200),.UNSPECIFIED.,.F.,.F.,(4,3,3,3,3,3,
3,3,3,3,3,3,3,3,4),(26.2476232379342,26.3148231034511,26.8113291997427,
27.3078352960342,27.8043413923257,28.3008474886173,28.7973535849088,29.2938596812003,
29.7903657774919,30.2868718737834,30.783377970075,31.2798840663665,31.776390162658,
32.2728962589496,32.5308085451137),.UNSPECIFIED.);
#313=B_SPLINE_CURVE_WITH_KNOTS('',3,(#41205,#41206,#41207,#41208,#41209,
#41210,#41211,#41212,#41213,#41214,#41215,#41216,#41217,#41218,#41219,#41220,
#41221,#41222,#41223,#41224,#41225,#41226,#41227,#41228,#41229,#41230,#41231,
#41232,#41233,#41234,#41235,#41236,#41237,#41238,#41239,#41240,#41241,#41242,
#41243,#41244,#41245,#41246,#41247),.UNSPECIFIED.,.F.,.F.,(4,3,3,3,3,3,
3,3,3,3,3,3,3,3,4),(-41.7923445631022,-41.7065120884886,-41.2100059921971,
-40.7134998959056,-40.216993799614,-39.7204877033225,-39.223981607031,-38.7274755107394,
-38.2309694144479,-37.7344633181564,-37.2379572218649,-36.7414511255733,
-36.2449450292818,-35.7484389329903,-35.5091592559226),.UNSPECIFIED.);
#314=B_SPLINE_CURVE_WITH_KNOTS('',3,(#41248,#41249,#41250,#41251,#41252,
#41253,#41254,#41255,#41256,#41257,#41258,#41259,#41260,#41261,#41262,#41263,
#41264,#41265,#41266,#41267,#41268,#41269,#41270,#41271,#41272,#41273,#41274,
#41275,#41276,#41277,#41278,#41279,#41280,#41281,#41282,#41283,#41284,#41285,
#41286,#41287,#41288,#41289,#41290),.UNSPECIFIED.,.F.,.F.,(4,3,3,3,3,3,
3,3,3,3,3,3,3,3,4),(32.5308085451137,32.7694023552411,33.2659084515326,
33.7624145478241,34.2589206441157,34.7554267404072,35.2519328366987,35.7484389329903,
36.2449450292818,36.7414511255733,37.2379572218648,37.7344633181564,38.2309694144479,
38.7274755107394,38.8139938522933),.UNSPECIFIED.);
#315=B_SPLINE_CURVE_WITH_KNOTS('',3,(#41295,#41296,#41297,#41298,#41299,
#41300,#41301,#41302,#41303,#41304,#41305,#41306,#41307,#41308,#41309,#41310,
#41311,#41312,#41313,#41314,#41315,#41316,#41317,#41318,#41319,#41320,#41321,
#41322,#41323,#41324,#41325,#41326,#41327,#41328,#41329,#41330,#41331,#41332,
#41333,#41334),.UNSPECIFIED.,.F.,.F.,(4,3,3,3,3,3,3,3,3,3,3,3,3,4),(-48.0755298702818,
-47.664585243987,-47.1680791476955,-46.6715730514039,-46.1750669551124,
-45.6785608588209,-45.1820547625294,-44.6855486662378,-44.1890425699463,
-43.6925364736548,-43.1960303773632,-42.6995242810717,-42.2030181847802,
-41.7923445631022),.UNSPECIFIED.);
#316=B_SPLINE_CURVE_WITH_KNOTS('',3,(#41335,#41336,#41337,#41338,#41339,
#41340,#41341,#41342,#41343,#41344,#41345,#41346,#41347,#41348,#41349,#41350,
#41351,#41352,#41353,#41354,#41355,#41356,#41357,#41358,#41359,#41360,#41361,
#41362,#41363,#41364,#41365,#41366,#41367,#41368,#41369,#41370,#41371,#41372,
#41373,#41374),.UNSPECIFIED.,.F.,.F.,(4,3,3,3,3,3,3,3,3,3,3,3,3,4),(38.8139938522933,
39.223981607031,39.7204877033225,40.216993799614,40.7134998959056,41.2100059921971,
41.7065120884886,42.2030181847802,42.6995242810717,43.1960303773632,43.6925364736548,
44.1890425699463,44.6855486662378,45.0971791594729),.UNSPECIFIED.);
#317=B_SPLINE_CURVE_WITH_KNOTS('',3,(#41379,#41380,#41381,#41382,#41383,
#41384,#41385,#41386,#41387,#41388,#41389,#41390,#41391,#41392,#41393,#41394,
#41395,#41396,#41397,#41398,#41399,#41400,#41401,#41402,#41403,#41404,#41405,
#41406,#41407,#41408,#41409,#41410,#41411,#41412,#41413,#41414,#41415,#41416,
#41417,#41418,#41419,#41420,#41421),.UNSPECIFIED.,.F.,.F.,(4,3,3,3,3,3,
3,3,3,3,3,3,3,3,4),(-54.3587151774614,-54.1191644957769,-53.6226583994854,
-53.1261523031939,-52.6296462069023,-52.1331401106108,-51.6366340143193,
-51.1401279180277,-50.6436218217362,-50.1471157254447,-49.6506096291531,
-49.1541035328616,-48.6575974365701,-48.1610913402785,-48.0755298702818),
 .UNSPECIFIED.);
#318=B_SPLINE_CURVE_WITH_KNOTS('',3,(#41422,#41423,#41424,#41425,#41426,
#41427,#41428,#41429,#41430,#41431,#41432,#41433,#41434,#41435,#41436,#41437,
#41438,#41439,#41440,#41441,#41442,#41443,#41444,#41445,#41446,#41447,#41448,
#41449,#41450,#41451,#41452,#41453,#41454,#41455,#41456,#41457,#41458,#41459,
#41460,#41461,#41462,#41463,#41464),.UNSPECIFIED.,.F.,.F.,(4,3,3,3,3,3,
3,3,3,3,3,3,3,3,4),(45.0971791594729,45.1820547625293,45.6785608588209,
46.1750669551124,46.6715730514039,47.1680791476955,47.664585243987,48.1610913402785,
48.6575974365701,49.1541035328616,49.6506096291531,50.1471157254447,50.6436218217362,
51.1401279180277,51.3803644666525),.UNSPECIFIED.);
#319=B_SPLINE_CURVE_WITH_KNOTS('',3,(#41469,#41470,#41471,#41472,#41473,
#41474,#41475,#41476,#41477,#41478,#41479,#41480,#41481,#41482,#41483,#41484,
#41485,#41486,#41487,#41488,#41489,#41490,#41491,#41492,#41493,#41494,#41495,
#41496,#41497,#41498,#41499,#41500,#41501,#41502),.UNSPECIFIED.,.F.,.F.,
(4,3,3,3,3,3,3,3,3,3,3,4),(-60.641900484641,-60.5737437475668,-59.5807315549838,
-58.5877193624007,-57.5947071698176,-57.0982010735261,-56.6016949772346,
-56.1051888809431,-55.6086827846515,-55.11217668836,-54.6156705920684,-54.3587151774614),
 .UNSPECIFIED.);
#320=B_SPLINE_CURVE_WITH_KNOTS('',3,(#41503,#41504,#41505,#41506,#41507,
#41508,#41509,#41510,#41511,#41512,#41513,#41514,#41515,#41516,#41517,#41518,
#41519,#41520,#41521,#41522,#41523,#41524,#41525,#41526,#41527,#41528,#41529,
#41530,#41531,#41532,#41533,#41534,#41535,#41536,#41537,#41538,#41539,#41540,
#41541,#41542),.UNSPECIFIED.,.F.,.F.,(4,3,3,3,3,3,3,3,3,3,3,3,3,4),(51.3803644666525,
51.6366340143193,52.1331401106108,52.6296462069023,53.1261523031939,53.6226583994854,
54.1191644957769,54.6156705920685,55.11217668836,55.6086827846515,56.1051888809431,
56.6016949772346,57.5947071698176,57.6635497738321),.UNSPECIFIED.);
#321=B_SPLINE_CURVE_WITH_KNOTS('',3,(#41547,#41548,#41549,#41550,#41551,
#41552,#41553,#41554,#41555,#41556,#41557,#41558,#41559,#41560,#41561,#41562,
#41563,#41564,#41565,#41566,#41567,#41568),.UNSPECIFIED.,.F.,.F.,(4,3,3,
3,3,3,3,4),(-66.9250857918206,-66.5318169030652,-65.5388047104821,-64.5457925178991,
-63.552780325316,-62.5597681327329,-61.5667559401499,-60.641900484641),
 .UNSPECIFIED.);
#322=B_SPLINE_CURVE_WITH_KNOTS('',3,(#41569,#41570,#41571,#41572,#41573,
#41574,#41575,#41576,#41577,#41578,#41579,#41580,#41581,#41582,#41583,#41584,
#41585,#41586,#41587,#41588,#41589,#41590),.UNSPECIFIED.,.F.,.F.,(4,3,3,
3,3,3,3,4),(57.6635497738321,58.5877193624007,59.5807315549838,60.5737437475668,
61.5667559401499,62.5597681327329,63.552780325316,63.9467350810117),
 .UNSPECIFIED.);
#323=B_SPLINE_CURVE_WITH_KNOTS('',3,(#41595,#41596,#41597,#41598,#41599,
#41600,#41601,#41602,#41603,#41604,#41605,#41606,#41607,#41608,#41609,#41610,
#41611,#41612,#41613,#41614,#41615,#41616,#41617,#41618,#41619,#41620,#41621,
#41622),.UNSPECIFIED.,.F.,.F.,(4,3,3,3,3,3,3,3,3,4),(-73.2082710990002,
-72.9863961548551,-72.4898900585636,-71.993383962272,-71.4968778659805,
-70.5038656733974,-69.5108534808144,-68.5178412882313,-67.5248290956483,
-66.9250857918206),.UNSPECIFIED.);
#324=B_SPLINE_CURVE_WITH_KNOTS('',3,(#41623,#41624,#41625,#41626,#41627,
#41628,#41629,#41630,#41631,#41632,#41633,#41634,#41635,#41636,#41637,#41638,
#41639,#41640,#41641,#41642,#41643,#41644),.UNSPECIFIED.,.F.,.F.,(4,3,3,
3,3,3,3,4),(63.9467350810117,64.5457925178991,65.5388047104821,66.5318169030652,
67.5248290956483,68.5178412882313,69.5108534808144,70.2299203881913),
 .UNSPECIFIED.);
#325=B_SPLINE_CURVE_WITH_KNOTS('',3,(#41649,#41650,#41651,#41652,#41653,
#41654,#41655,#41656,#41657,#41658,#41659,#41660,#41661,#41662,#41663,#41664,
#41665,#41666,#41667,#41668,#41669,#41670,#41671,#41672,#41673,#41674,#41675,
#41676,#41677,#41678,#41679,#41680,#41681,#41682,#41683,#41684,#41685,#41686,
#41687,#41688,#41689,#41690,#41691),.UNSPECIFIED.,.F.,.F.,(4,3,3,3,3,3,
3,3,3,3,3,3,3,3,4),(-79.4914564061798,-79.440975406645,-78.9444693103535,
-78.4479632140619,-77.9514571177704,-77.4549510214789,-76.9584449251874,
-76.4619388288958,-75.9654327326043,-75.4689266363128,-74.9724205400212,
-74.4759144437297,-73.9794083474382,-73.4829022511466,-73.2082710990002),
 .UNSPECIFIED.);
#326=B_SPLINE_CURVE_WITH_KNOTS('',3,(#41692,#41693,#41694,#41695,#41696,
#41697,#41698,#41699,#41700,#41701,#41702,#41703,#41704,#41705,#41706,#41707,
#41708,#41709,#41710,#41711,#41712,#41713,#41714,#41715,#41716,#41717,#41718,
#41719,#41720,#41721,#41722,#41723,#41724,#41725,#41726,#41727,#41728),
 .UNSPECIFIED.,.F.,.F.,(4,3,3,3,3,3,3,3,3,3,3,3,4),(70.2299203881913,70.5038656733975,
71.4968778659805,72.4898900585636,72.9863961548551,73.4829022511466,73.9794083474382,
74.4759144437297,74.9724205400212,75.4689266363127,75.9654327326043,76.4619388288958,
76.5131056953709),.UNSPECIFIED.);
#327=B_SPLINE_CURVE_WITH_KNOTS('',3,(#41733,#41734,#41735,#41736,#41737,
#41738,#41739,#41740,#41741,#41742,#41743,#41744,#41745,#41746,#41747,#41748,
#41749,#41750,#41751,#41752,#41753,#41754,#41755,#41756,#41757,#41758,#41759,
#41760,#41761,#41762,#41763,#41764,#41765,#41766,#41767,#41768,#41769,#41770,
#41771,#41772),.UNSPECIFIED.,.F.,.F.,(4,3,3,3,3,3,3,3,3,3,3,3,3,4),(-85.7746417133594,
-85.3990485621434,-84.9025424658519,-84.4060363695603,-83.9095302732688,
-83.4130241769773,-82.9165180806857,-82.4200119843942,-81.9235058881027,
-81.4269997918111,-80.9304936955196,-80.4339875992281,-79.9374815029365,
-79.4914564061798),.UNSPECIFIED.);
#328=B_SPLINE_CURVE_WITH_KNOTS('',3,(#41773,#41774,#41775,#41776,#41777,
#41778,#41779,#41780,#41781,#41782,#41783,#41784,#41785,#41786,#41787,#41788,
#41789,#41790,#41791,#41792,#41793,#41794,#41795,#41796,#41797,#41798,#41799,
#41800,#41801,#41802,#41803,#41804,#41805,#41806,#41807,#41808,#41809,#41810,
#41811,#41812),.UNSPECIFIED.,.F.,.F.,(4,3,3,3,3,3,3,3,3,3,3,3,3,4),(76.5131056953709,
76.9584449251873,77.4549510214789,77.9514571177704,78.4479632140619,78.9444693103535,
79.440975406645,79.9374815029365,80.4339875992281,80.9304936955196,81.4269997918111,
81.9235058881027,82.4200119843942,82.7962910025505),.UNSPECIFIED.);
#329=B_SPLINE_CURVE_WITH_KNOTS('',3,(#41817,#41818,#41819,#41820,#41821,
#41822,#41823,#41824,#41825,#41826,#41827,#41828,#41829,#41830,#41831,#41832,
#41833,#41834,#41835,#41836,#41837,#41838,#41839,#41840,#41841,#41842,#41843,
#41844,#41845,#41846,#41847,#41848,#41849,#41850,#41851,#41852,#41853,#41854,
#41855,#41856,#41857,#41858,#41859),.UNSPECIFIED.,.F.,.F.,(4,3,3,3,3,3,
3,3,3,3,3,3,3,3,4),(-92.0578270205389,-91.8536278139333,-91.3571217176418,
-90.8606156213502,-90.3641095250587,-89.8676034287672,-89.3710973324757,
-88.8745912361841,-88.3780851398926,-87.8815790436011,-87.3850729473095,
-86.888566851018,-86.3920607547265,-85.8955546584349,-85.7746417133594),
 .UNSPECIFIED.);
#330=B_SPLINE_CURVE_WITH_KNOTS('',3,(#41860,#41861,#41862,#41863,#41864,
#41865,#41866,#41867,#41868,#41869,#41870,#41871,#41872,#41873,#41874,#41875,
#41876,#41877,#41878,#41879,#41880,#41881,#41882,#41883,#41884,#41885,#41886,
#41887,#41888,#41889,#41890,#41891,#41892,#41893,#41894,#41895,#41896,#41897,
#41898,#41899,#41900,#41901,#41902),.UNSPECIFIED.,.F.,.F.,(4,3,3,3,3,3,
3,3,3,3,3,3,3,3,4),(82.7962910025505,82.9165180806857,83.4130241769772,
83.9095302732688,84.4060363695603,84.9025424658518,85.3990485621434,85.8955546584349,
86.3920607547264,86.888566851018,87.3850729473095,87.881579043601,88.3780851398926,
88.8745912361841,89.0794763097301),.UNSPECIFIED.);
#331=B_SPLINE_CURVE_WITH_KNOTS('',3,(#41907,#41908,#41909,#41910,#41911,
#41912,#41913,#41914,#41915,#41916,#41917,#41918,#41919,#41920,#41921,#41922,
#41923,#41924,#41925,#41926,#41927,#41928,#41929,#41930,#41931,#41932,#41933,
#41934,#41935,#41936,#41937,#41938,#41939,#41940,#41941,#41942,#41943,#41944,
#41945,#41946,#41947,#41948,#41949),.UNSPECIFIED.,.F.,.F.,(4,3,3,3,3,3,
3,3,3,3,3,3,3,3,4),(-98.3410123277185,-98.3082070657232,-97.8117009694317,
-97.3151948731401,-96.8186887768486,-96.3221826805571,-95.8256765842656,
-95.329170487974,-94.8326643916825,-94.336158295391,-93.8396521990994,-93.3431461028079,
-92.8466400065164,-92.3501339102248,-92.0578270205389),.UNSPECIFIED.);
#332=B_SPLINE_CURVE_WITH_KNOTS('',3,(#41950,#41951,#41952,#41953,#41954,
#41955,#41956,#41957,#41958,#41959,#41960,#41961,#41962,#41963,#41964,#41965,
#41966,#41967,#41968,#41969,#41970,#41971,#41972,#41973,#41974,#41975,#41976,
#41977,#41978,#41979,#41980,#41981,#41982,#41983,#41984,#41985,#41986,#41987,
#41988,#41989,#41990,#41991,#41992),.UNSPECIFIED.,.F.,.F.,(4,3,3,3,3,3,
3,3,3,3,3,3,3,3,4),(89.0794763097301,89.3710973324756,89.8676034287672,
90.3641095250587,90.8606156213502,91.3571217176417,91.8536278139333,92.3501339102248,
92.8466400065163,93.3431461028079,93.8396521990994,94.3361582953909,94.8326643916825,
95.329170487974,95.3626616169096),.UNSPECIFIED.);
#333=B_SPLINE_CURVE_WITH_KNOTS('',3,(#41997,#41998,#41999,#42000,#42001,
#42002,#42003,#42004,#42005,#42006,#42007,#42008,#42009,#42010,#42011,#42012,
#42013,#42014,#42015,#42016,#42017,#42018,#42019,#42020,#42021,#42022,#42023,
#42024,#42025,#42026,#42027,#42028,#42029,#42030,#42031,#42032,#42033,#42034,
#42035,#42036),.UNSPECIFIED.,.F.,.F.,(4,3,3,3,3,3,3,3,3,3,3,3,3,4),(-104.624197634898,
-104.266280221222,-103.76977412493,-103.273268028639,-102.776761932347,
-102.280255836055,-101.783749739764,-101.287243643472,-100.790737547181,
-100.294231450889,-99.7977253545978,-99.3012192583063,-98.8047131620147,
-98.3410123277185),.UNSPECIFIED.);
#334=B_SPLINE_CURVE_WITH_KNOTS('',3,(#42037,#42038,#42039,#42040,#42041,
#42042,#42043,#42044,#42045,#42046,#42047,#42048,#42049,#42050,#42051,#42052,
#42053,#42054,#42055,#42056,#42057,#42058,#42059,#42060,#42061,#42062,#42063,
#42064,#42065,#42066,#42067,#42068,#42069,#42070,#42071,#42072,#42073,#42074,
#42075,#42076),.UNSPECIFIED.,.F.,.F.,(4,3,3,3,3,3,3,3,3,3,3,3,3,4),(95.3626616169096,
95.8256765842655,96.3221826805571,96.8186887768486,97.3151948731401,97.8117009694316,
98.3082070657232,98.8047131620147,99.3012192583062,99.7977253545978,100.294231450889,
100.790737547181,101.287243643472,101.645846924089),.UNSPECIFIED.);
#335=B_SPLINE_CURVE_WITH_KNOTS('',3,(#42081,#42082,#42083,#42084,#42085,
#42086,#42087,#42088,#42089,#42090,#42091,#42092,#42093,#42094,#42095,#42096,
#42097,#42098,#42099,#42100,#42101,#42102,#42103,#42104,#42105,#42106,#42107,
#42108,#42109,#42110,#42111,#42112,#42113,#42114,#42115,#42116,#42117,#42118,
#42119,#42120,#42121,#42122,#42123),.UNSPECIFIED.,.F.,.F.,(4,3,3,3,3,3,
3,3,3,3,3,3,3,3,4),(-110.907382942078,-110.720859473011,-110.22435337672,
-109.727847280428,-109.231341184137,-108.734835087845,-108.238328991554,
-107.741822895262,-107.245316798971,-106.748810702679,-106.252304606388,
-105.755798510096,-105.259292413805,-104.762786317513,-104.624197634898),
 .UNSPECIFIED.);
#336=B_SPLINE_CURVE_WITH_KNOTS('',3,(#42124,#42125,#42126,#42127,#42128,
#42129,#42130,#42131,#42132,#42133,#42134,#42135,#42136,#42137,#42138,#42139,
#42140,#42141,#42142,#42143,#42144,#42145,#42146,#42147,#42148,#42149,#42150,
#42151,#42152,#42153,#42154,#42155,#42156,#42157,#42158,#42159,#42160,#42161,
#42162,#42163,#42164,#42165,#42166),.UNSPECIFIED.,.F.,.F.,(4,3,3,3,3,3,
3,3,3,3,3,3,3,3,4),(101.645846924089,101.783749739764,102.280255836055,
102.776761932347,103.273268028638,103.76977412493,104.266280221222,104.762786317513,
105.259292413805,105.755798510096,106.252304606388,106.748810702679,107.245316798971,
107.741822895262,107.929032231269),.UNSPECIFIED.);
#337=B_SPLINE_CURVE_WITH_KNOTS('',3,(#42171,#42172,#42173,#42174,#42175,
#42176,#42177,#42178,#42179,#42180,#42181,#42182,#42183,#42184,#42185,#42186,
#42187,#42188,#42189,#42190,#42191,#42192,#42193,#42194,#42195,#42196,#42197,
#42198,#42199,#42200,#42201,#42202,#42203,#42204,#42205,#42206,#42207,#42208,
#42209,#42210,#42211,#42212,#42213),.UNSPECIFIED.,.F.,.F.,(4,3,3,3,3,3,
3,3,3,3,3,3,3,3,4),(-117.190568249257,-117.175438724801,-116.67893262851,
-116.182426532218,-115.685920435927,-115.189414339635,-114.692908243344,
-114.196402147052,-113.699896050761,-113.203389954469,-112.706883858178,
-112.210377761886,-111.713871665595,-111.217365569303,-110.907382942078),
 .UNSPECIFIED.);
#338=B_SPLINE_CURVE_WITH_KNOTS('',3,(#42214,#42215,#42216,#42217,#42218,
#42219,#42220,#42221,#42222,#42223,#42224,#42225,#42226,#42227,#42228,#42229,
#42230,#42231,#42232,#42233,#42234,#42235,#42236,#42237,#42238,#42239,#42240,
#42241,#42242,#42243,#42244,#42245,#42246,#42247,#42248,#42249,#42250,#42251,
#42252,#42253,#42254,#42255,#42256),.UNSPECIFIED.,.F.,.F.,(4,3,3,3,3,3,
3,3,3,3,3,3,3,3,4),(107.929032231269,108.238328991554,108.734835087845,
109.231341184137,109.727847280428,110.22435337672,110.720859473011,111.217365569303,
111.713871665595,112.210377761886,112.706883858178,113.203389954469,113.699896050761,
114.196402147052,114.212217538448),.UNSPECIFIED.);
#339=B_SPLINE_CURVE_WITH_KNOTS('',3,(#42261,#42262,#42263,#42264,#42265,
#42266,#42267,#42268,#42269,#42270,#42271,#42272,#42273,#42274,#42275,#42276,
#42277,#42278,#42279,#42280,#42281,#42282,#42283,#42284,#42285,#42286,#42287,
#42288,#42289,#42290,#42291,#42292,#42293,#42294,#42295,#42296,#42297,#42298,
#42299,#42300),.UNSPECIFIED.,.F.,.F.,(4,3,3,3,3,3,3,3,3,3,3,3,3,4),(-123.473753556437,
-123.1335118803,-122.637005784008,-122.140499687717,-121.643993591425,-121.147487495134,
-120.650981398842,-120.154475302551,-119.657969206259,-119.161463109968,
-118.664957013676,-118.168450917384,-117.671944821093,-117.190568249257),
 .UNSPECIFIED.);
#340=B_SPLINE_CURVE_WITH_KNOTS('',3,(#42301,#42302,#42303,#42304,#42305,
#42306,#42307,#42308,#42309,#42310,#42311,#42312,#42313,#42314,#42315,#42316,
#42317,#42318,#42319,#42320,#42321,#42322,#42323,#42324,#42325,#42326,#42327,
#42328,#42329,#42330,#42331,#42332,#42333,#42334,#42335,#42336,#42337,#42338,
#42339,#42340),.UNSPECIFIED.,.F.,.F.,(4,3,3,3,3,3,3,3,3,3,3,3,3,4),(114.212217538448,
114.692908243344,115.189414339635,115.685920435927,116.182426532218,116.67893262851,
117.175438724801,117.671944821093,118.168450917384,118.664957013676,119.161463109967,
119.657969206259,120.154475302551,120.495402845628),.UNSPECIFIED.);
#341=B_SPLINE_CURVE_WITH_KNOTS('',3,(#42347,#42348,#42349,#42350,#42351,
#42352,#42353,#42354,#42355,#42356,#42357,#42358,#42359,#42360,#42361,#42362,
#42363,#42364,#42365,#42366,#42367,#42368,#42369,#42370,#42371,#42372,#42373,
#42374,#42375,#42376,#42377,#42378,#42379,#42380,#42381,#42382,#42383),
 .UNSPECIFIED.,.F.,.F.,(4,3,3,3,3,3,3,3,3,3,3,3,4),(-129.091585035798,-128.595078939507,
-128.098572843215,-127.602066746924,-127.105560650632,-126.60905455434,
-126.112548458049,-125.616042361757,-125.119536265466,-124.623030169174,
-124.126524072883,-123.630017976591,-123.473753556437),.UNSPECIFIED.);
#342=B_SPLINE_CURVE_WITH_KNOTS('',3,(#42384,#42385,#42386,#42387,#42388,
#42389,#42390,#42391,#42392,#42393,#42394,#42395,#42396,#42397,#42398,#42399,
#42400,#42401,#42402,#42403,#42404,#42405,#42406,#42407,#42408,#42409,#42410,
#42411,#42412,#42413,#42414,#42415,#42416,#42417,#42418,#42419,#42420,#42421,
#42422,#42423,#42424,#42425,#42426),.UNSPECIFIED.,.F.,.F.,(4,3,3,3,3,3,
3,3,3,3,3,3,3,3,4),(120.495402845628,120.650981398842,121.147487495134,
121.643993591425,122.140499687717,122.637005784008,123.1335118803,123.630017976591,
124.126524072883,124.623030169174,125.119536265466,125.616042361757,126.112548458049,
126.60905455434,126.778588152808),.UNSPECIFIED.);
#343=B_SPLINE_CURVE_WITH_KNOTS('',3,(#42432,#42433,#42434,#42435,#42436,
#42437,#42438,#42439,#42440,#42441,#42442),.UNSPECIFIED.,.F.,.F.,(4,1,1,
1,1,1,1,1,4),(135.088484104361,135.244748524516,135.741254620807,136.237760717099,
136.73426681339,137.230772909682,137.727279005973,138.223785102265,138.639793508071),
 .UNSPECIFIED.);
#344=B_SPLINE_CURVE_WITH_KNOTS('',3,(#42445,#42446,#42447,#42448,#42449,
#42450,#42451,#42452),.UNSPECIFIED.,.F.,.F.,(4,1,1,1,1,4),(135.088484104361,
135.415456602185,135.911962698477,136.408468794768,136.90497489106,137.401480987351),
 .UNSPECIFIED.);
#345=B_SPLINE_CURVE_WITH_KNOTS('',3,(#42457,#42458,#42459,#42460,#42461,
#42462,#42463,#42464,#42465,#42466,#42467,#42468,#42469,#42470,#42471,#42472),
 .UNSPECIFIED.,.F.,.F.,(4,1,1,1,1,1,1,1,1,1,1,1,1,4),(128.805298797182,
129.286675369017,129.783181465309,130.2796875616,130.776193657892,131.272699754183,
131.769205850475,132.265711946766,132.762218043058,133.258724139349,133.755230235641,
134.251736331932,134.748242428224,135.088484104361),.UNSPECIFIED.);
#346=B_SPLINE_CURVE_WITH_KNOTS('',3,(#42473,#42474,#42475,#42476,#42477,
#42478,#42479,#42480,#42481,#42482,#42483,#42484,#42485,#42486,#42487,#42488,
#42489),.UNSPECIFIED.,.F.,.F.,(4,1,1,1,1,1,1,1,1,1,1,1,1,1,4),(128.805298797182,
128.960877350395,129.457383446687,129.953889542979,130.45039563927,130.946901735562,
131.443407831853,131.939913928145,132.436420024436,132.932926120728,133.429432217019,
133.925938313311,134.422444409602,134.918950505894,135.088484104361),
 .UNSPECIFIED.);
#347=B_SPLINE_CURVE_WITH_KNOTS('',3,(#42494,#42495,#42496,#42497,#42498,
#42499,#42500,#42501,#42502,#42503,#42504,#42505,#42506,#42507,#42508,#42509,
#42510),.UNSPECIFIED.,.F.,.F.,(4,1,1,1,1,1,1,1,1,1,1,1,1,1,4),(122.522113490002,
122.832096117227,123.328602213519,123.82510830981,124.321614406102,124.818120502393,
125.314626598685,125.811132694976,126.307638791268,126.804144887559,127.300650983851,
127.797157080143,128.293663176434,128.790169272726,128.805298797182),
 .UNSPECIFIED.);
#348=B_SPLINE_CURVE_WITH_KNOTS('',3,(#42511,#42512,#42513,#42514,#42515,
#42516,#42517,#42518,#42519,#42520,#42521,#42522,#42523,#42524,#42525,#42526),
 .UNSPECIFIED.,.F.,.F.,(4,1,1,1,1,1,1,1,1,1,1,1,1,4),(122.522113490002,
123.002804194897,123.499310291189,123.99581638748,124.492322483772,124.988828580063,
125.485334676355,125.981840772646,126.478346868938,126.974852965229,127.471359061521,
127.967865157812,128.464371254104,128.805298797182),.UNSPECIFIED.);
#349=B_SPLINE_CURVE_WITH_KNOTS('',3,(#42531,#42532,#42533,#42534,#42535,
#42536,#42537,#42538,#42539,#42540,#42541,#42542,#42543,#42544,#42545,#42546,
#42547),.UNSPECIFIED.,.F.,.F.,(4,1,1,1,1,1,1,1,1,1,1,1,1,1,4),(116.238928182822,
116.377516865437,116.874022961729,117.37052905802,117.867035154312,118.363541250603,
118.860047346895,119.356553443186,119.853059539478,120.34956563577,120.846071732061,
121.342577828353,121.839083924644,122.335590020936,122.522113490002),
 .UNSPECIFIED.);
#350=B_SPLINE_CURVE_WITH_KNOTS('',3,(#42548,#42549,#42550,#42551,#42552,
#42553,#42554,#42555,#42556,#42557,#42558,#42559,#42560,#42561,#42562,#42563,
#42564),.UNSPECIFIED.,.F.,.F.,(4,1,1,1,1,1,1,1,1,1,1,1,1,1,4),(116.238928182822,
116.548224943107,117.044731039399,117.54123713569,118.037743231982,118.534249328273,
119.030755424565,119.527261520856,120.023767617148,120.520273713439,121.016779809731,
121.513285906022,122.009792002314,122.506298098606,122.522113490002),
 .UNSPECIFIED.);
#351=B_SPLINE_CURVE_WITH_KNOTS('',3,(#42569,#42570,#42571,#42572,#42573,
#42574,#42575,#42576,#42577,#42578,#42579,#42580,#42581,#42582,#42583,#42584),
 .UNSPECIFIED.,.F.,.F.,(4,1,1,1,1,1,1,1,1,1,1,1,1,4),(109.955742875643,
110.419443709939,110.91594980623,111.412455902522,111.908961998814,112.405468095105,
112.901974191397,113.398480287688,113.89498638398,114.391492480271,114.887998576563,
115.384504672854,115.881010769146,116.238928182822),.UNSPECIFIED.);
#352=B_SPLINE_CURVE_WITH_KNOTS('',3,(#42585,#42586,#42587,#42588,#42589,
#42590,#42591,#42592,#42593,#42594,#42595,#42596,#42597,#42598,#42599,#42600,
#42601),.UNSPECIFIED.,.F.,.F.,(4,1,1,1,1,1,1,1,1,1,1,1,1,1,4),(109.955742875643,
110.093645691317,110.590151787609,111.0866578839,111.583163980192,112.079670076483,
112.576176172775,113.072682269066,113.569188365358,114.06569446165,114.562200557941,
115.058706654233,115.555212750524,116.051718846816,116.238928182822),
 .UNSPECIFIED.);
#353=B_SPLINE_CURVE_WITH_KNOTS('',3,(#42606,#42607,#42608,#42609,#42610,
#42611,#42612,#42613,#42614,#42615,#42616,#42617,#42618,#42619,#42620,#42621,
#42622),.UNSPECIFIED.,.F.,.F.,(4,1,1,1,1,1,1,1,1,1,1,1,1,1,4),(103.672557568463,
103.964864458149,104.461370554441,104.957876650732,105.454382747024,105.950888843315,
106.447394939607,106.943901035898,107.44040713219,107.936913228481,108.433419324773,
108.929925421064,109.426431517356,109.922937613647,109.955742875643),
 .UNSPECIFIED.);
#354=B_SPLINE_CURVE_WITH_KNOTS('',3,(#42623,#42624,#42625,#42626,#42627,
#42628,#42629,#42630,#42631,#42632,#42633,#42634,#42635,#42636,#42637,#42638),
 .UNSPECIFIED.,.F.,.F.,(4,1,1,1,1,1,1,1,1,1,1,1,1,4),(103.672557568463,
104.135572535819,104.63207863211,105.128584728402,105.625090824693,106.121596920985,
106.618103017277,107.114609113568,107.61111520986,108.107621306151,108.604127402443,
109.100633498734,109.597139595026,109.955742875643),.UNSPECIFIED.);
#355=B_SPLINE_CURVE_WITH_KNOTS('',3,(#42643,#42644,#42645,#42646,#42647,
#42648,#42649,#42650,#42651,#42652,#42653,#42654,#42655,#42656,#42657,#42658,
#42659),.UNSPECIFIED.,.F.,.F.,(4,1,1,1,1,1,1,1,1,1,1,1,1,1,4),(97.3893722612836,
97.5102852063591,98.0067913026507,98.5032973989422,98.9998034952337,99.4963095915253,
99.9928156878168,100.489321784108,100.9858278804,101.482333976691,101.978840072983,
102.475346169274,102.971852265566,103.468358361857,103.672557568463),
 .UNSPECIFIED.);
#356=B_SPLINE_CURVE_WITH_KNOTS('',3,(#42660,#42661,#42662,#42663,#42664,
#42665,#42666,#42667,#42668,#42669,#42670,#42671,#42672,#42673,#42674,#42675,
#42676),.UNSPECIFIED.,.F.,.F.,(4,1,1,1,1,1,1,1,1,1,1,1,1,1,4),(97.3893722612836,
97.680993284029,98.1774993803205,98.6740054766121,99.1705115729036,99.6670176691951,
100.163523765487,100.660029861778,101.15653595807,101.653042054361,102.149548150653,
102.646054246944,103.142560343236,103.639066439527,103.672557568463),
 .UNSPECIFIED.);
#357=B_SPLINE_CURVE_WITH_KNOTS('',3,(#42681,#42682,#42683,#42684,#42685,
#42686,#42687,#42688,#42689,#42690,#42691,#42692,#42693,#42694,#42695,#42696),
 .UNSPECIFIED.,.F.,.F.,(4,1,1,1,1,1,1,1,1,1,1,1,1,4),(91.106186954104,91.5522120508608,
92.0487181471523,92.5452242434438,93.0417303397354,93.5382364360269,94.0347425323184,
94.5312486286099,95.0277547249015,95.524260821193,96.0207669174845,96.5172730137761,
97.0137791100676,97.3893722612836),.UNSPECIFIED.);
#358=B_SPLINE_CURVE_WITH_KNOTS('',3,(#42697,#42698,#42699,#42700,#42701,
#42702,#42703,#42704,#42705,#42706,#42707,#42708,#42709,#42710,#42711,#42712,
#42713),.UNSPECIFIED.,.F.,.F.,(4,1,1,1,1,1,1,1,1,1,1,1,1,1,4),(91.106186954104,
91.2264140322391,91.7229201285306,92.2194262248221,92.7159323211137,93.2124384174052,
93.7089445136967,94.2054506099883,94.7019567062798,95.1984628025713,95.6949688988629,
96.1914749951544,96.6879810914459,97.1844871877375,97.3893722612836),
 .UNSPECIFIED.);
#359=B_SPLINE_CURVE_WITH_KNOTS('',3,(#42718,#42719,#42720,#42721,#42722,
#42723,#42724,#42725,#42726,#42727,#42728,#42729,#42730,#42731,#42732,#42733,
#42734),.UNSPECIFIED.,.F.,.F.,(4,1,1,1,1,1,1,1,1,1,1,1,1,1,4),(84.8230016469244,
85.0976327990709,85.5941388953624,86.0906449916539,86.5871510879454,87.083657184237,
87.5801632805285,88.07666937682,88.5731754731116,89.0696815694031,89.5661876656946,
90.0626937619862,90.5591998582777,91.0557059545692,91.106186954104),
 .UNSPECIFIED.);
#360=B_SPLINE_CURVE_WITH_KNOTS('',3,(#42735,#42736,#42737,#42738,#42739,
#42740,#42741,#42742,#42743,#42744,#42745,#42746,#42747,#42748,#42749,#42750),
 .UNSPECIFIED.,.F.,.F.,(4,1,1,1,1,1,1,1,1,1,1,1,1,4),(84.8230016469244,
85.2683408767407,85.7648469730322,86.2613530693238,86.7578591656153,87.2543652619068,
87.7508713581984,88.2473774544899,88.7438835507814,89.240389647073,89.7368957433645,
90.233401839656,90.7299079359476,91.106186954104),.UNSPECIFIED.);
#361=B_SPLINE_CURVE_WITH_KNOTS('',3,(#42755,#42756,#42757,#42758,#42759,
#42760,#42761,#42762,#42763,#42764,#42765,#42766),.UNSPECIFIED.,.F.,.F.,
(4,1,1,1,1,1,1,1,1,4),(78.5398163397448,79.1395596435725,80.1325718361555,
81.1255840287386,82.1185962213217,83.1116084139047,83.6081145101963,84.1046206064878,
84.6011267027793,84.8230016469244),.UNSPECIFIED.);
#362=B_SPLINE_CURVE_WITH_KNOTS('',3,(#42767,#42768,#42769,#42770,#42771,
#42772,#42773,#42774,#42775,#42776,#42777,#42778,#42779,#42780,#42781),
 .UNSPECIFIED.,.F.,.F.,(4,1,1,1,1,1,1,1,1,1,1,1,4),(78.5398163397448,78.8137616249508,
79.8067738175339,80.7997860101169,81.2962921064085,81.7927982027,82.2893042989915,
82.7858103952831,83.2823164915746,83.7788225878661,84.2753286841576,84.7718347804492,
84.8230016469244),.UNSPECIFIED.);
#363=B_SPLINE_CURVE_WITH_KNOTS('',3,(#42786,#42787,#42788,#42789,#42790,
#42791,#42792,#42793,#42794,#42795),.UNSPECIFIED.,.F.,.F.,(4,1,1,1,1,1,
1,4),(72.2566310325652,73.1814864880741,74.1744986806572,75.1675108732402,
76.1605230658233,77.1535352584064,78.1465474509894,78.5398163397448),
 .UNSPECIFIED.);
#364=B_SPLINE_CURVE_WITH_KNOTS('',3,(#42796,#42797,#42798,#42799,#42800,
#42801,#42802,#42803,#42804,#42805),.UNSPECIFIED.,.F.,.F.,(4,1,1,1,1,1,
1,4),(72.2566310325652,72.8556884694524,73.8487006620355,74.8417128546185,
75.8347250472016,76.8277372397847,77.8207494323677,78.5398163397448),
 .UNSPECIFIED.);
#365=B_SPLINE_CURVE_WITH_KNOTS('',3,(#42810,#42811,#42812,#42813,#42814,
#42815,#42816,#42817,#42818,#42819,#42820,#42821,#42822,#42823),
 .UNSPECIFIED.,.F.,.F.,(4,1,1,1,1,1,1,1,1,1,1,4),(65.9734457253856,66.2304011399927,
66.7269072362842,67.2234133325757,67.7199194288673,68.2164255251588,68.7129316214503,
69.2094377177418,70.2024499103249,71.195462102908,72.188474295491,72.2566310325652),
 .UNSPECIFIED.);
#366=B_SPLINE_CURVE_WITH_KNOTS('',3,(#42824,#42825,#42826,#42827,#42828,
#42829,#42830,#42831,#42832,#42833),.UNSPECIFIED.,.F.,.F.,(4,1,1,1,1,1,
1,4),(65.9734457253856,66.897615313954,67.8906275065371,68.8836396991202,
69.8766518917032,70.8696640842863,71.8626762768694,72.2566310325652),
 .UNSPECIFIED.);
#367=B_SPLINE_CURVE_WITH_KNOTS('',3,(#42838,#42839,#42840,#42841,#42842,
#42843,#42844,#42845,#42846,#42847,#42848,#42849,#42850,#42851,#42852,#42853,
#42854),.UNSPECIFIED.,.F.,.F.,(4,1,1,1,1,1,1,1,1,1,1,1,1,1,4),(59.6902604182061,
59.7758218882027,60.2723279844943,60.7688340807858,61.2653401770773,61.7618462733689,
62.2583523696604,62.7548584659519,63.2513645622435,63.747870658535,64.2443767548265,
64.7408828511181,65.2373889474096,65.7338950437011,65.9734457253856),
 .UNSPECIFIED.);
#368=B_SPLINE_CURVE_WITH_KNOTS('',3,(#42855,#42856,#42857,#42858,#42859,
#42860,#42861,#42862,#42863,#42864,#42865,#42866,#42867,#42868,#42869,#42870),
 .UNSPECIFIED.,.F.,.F.,(4,1,1,1,1,1,1,1,1,1,1,1,1,4),(59.690260418206,59.9465299658726,
60.4430360621641,60.9395421584557,61.4360482547472,61.9325543510387,62.4290604473303,
62.9255665436218,63.4220726399133,63.9185787362049,64.4150848324964,64.9115909287879,
65.904603121371,65.9734457253856),.UNSPECIFIED.);
#369=B_SPLINE_CURVE_WITH_KNOTS('',3,(#42875,#42876,#42877,#42878,#42879,
#42880,#42881,#42882,#42883,#42884,#42885,#42886,#42887,#42888,#42889,#42890),
 .UNSPECIFIED.,.F.,.F.,(4,1,1,1,1,1,1,1,1,1,1,1,1,4),(53.4070751110264,
53.8177487327044,54.3142548289959,54.8107609252874,55.307267021579,55.8037731178705,
56.300279214162,56.7967853104536,57.2932914067451,57.7897975030366,58.2863035993281,
58.7828096956197,59.2793157919112,59.6902604182061),.UNSPECIFIED.);
#370=B_SPLINE_CURVE_WITH_KNOTS('',3,(#42891,#42892,#42893,#42894,#42895,
#42896,#42897,#42898,#42899,#42900,#42901,#42902,#42903,#42904,#42905,#42906,
#42907),.UNSPECIFIED.,.F.,.F.,(4,1,1,1,1,1,1,1,1,1,1,1,1,1,4),(53.4070751110264,
53.4919507140827,53.9884568103742,54.4849629066658,54.9814690029573,55.4779750992488,
55.9744811955404,56.4709872918319,56.9674933881234,57.463999484415,57.9605055807065,
58.457011676998,58.9535177732896,59.4500238695811,59.690260418206),
 .UNSPECIFIED.);
#371=B_SPLINE_CURVE_WITH_KNOTS('',3,(#42912,#42913,#42914,#42915,#42916,
#42917,#42918,#42919,#42920,#42921,#42922,#42923,#42924,#42925,#42926,#42927,
#42928),.UNSPECIFIED.,.F.,.F.,(4,1,1,1,1,1,1,1,1,1,1,1,1,1,4),(47.1238898038469,
47.3631694809145,47.859675577206,48.3561816734975,48.8526877697891,49.3491938660806,
49.8456999623721,50.3422060586636,50.8387121549552,51.3352182512467,51.8317243475382,
52.3282304438298,52.8247365401213,53.3212426364128,53.4070751110264),
 .UNSPECIFIED.);
#372=B_SPLINE_CURVE_WITH_KNOTS('',3,(#42929,#42930,#42931,#42932,#42933,
#42934,#42935,#42936,#42937,#42938,#42939,#42940,#42941,#42942,#42943,#42944),
 .UNSPECIFIED.,.F.,.F.,(4,1,1,1,1,1,1,1,1,1,1,1,1,4),(47.1238898038468,
47.5338775585843,48.0303836548759,48.5268897511674,49.0233958474589,49.5199019437505,
50.016408040042,50.5129141363335,51.0094202326251,51.5059263289166,52.0024324252081,
52.4989385214996,52.9954446177912,53.4070751110264),.UNSPECIFIED.);
#373=B_SPLINE_CURVE_WITH_KNOTS('',3,(#42949,#42950,#42951,#42952,#42953,
#42954,#42955,#42956,#42957,#42958,#42959,#42960,#42961,#42962,#42963,#42964,
#42965),.UNSPECIFIED.,.F.,.F.,(4,1,1,1,1,1,1,1,1,1,1,1,1,1,4),(40.8407044966673,
40.9085902291246,41.4050963254161,41.9016024217076,42.3981085179991,42.8946146142907,
43.3911207105822,43.8876268068737,44.3841329031653,44.8806389994568,45.3771450957483,
45.8736511920399,46.3701572883314,46.8666633846229,47.1238898038469),
 .UNSPECIFIED.);
#374=B_SPLINE_CURVE_WITH_KNOTS('',3,(#42966,#42967,#42968,#42969,#42970,
#42971,#42972,#42973,#42974,#42975,#42976,#42977,#42978,#42979,#42980,#42981,
#42982),.UNSPECIFIED.,.F.,.F.,(4,1,1,1,1,1,1,1,1,1,1,1,1,1,4),(40.8407044966672,
41.0792983067944,41.575804403086,42.0723104993775,42.568816595669,43.0653226919606,
43.5618287882521,44.0583348845436,44.5548409808351,45.0513470771267,45.5478531734182,
46.0443592697097,46.5408653660013,47.0373714622928,47.1238898038468),
 .UNSPECIFIED.);
#375=B_SPLINE_CURVE_WITH_KNOTS('',3,(#42987,#42988,#42989,#42990,#42991,
#42992,#42993,#42994,#42995,#42996,#42997,#42998,#42999,#43000,#43001,#43002),
 .UNSPECIFIED.,.F.,.F.,(4,1,1,1,1,1,1,1,1,1,1,1,1,4),(34.5575191894877,
34.9505170736262,35.4470231699177,35.9435292662092,36.4400353625008,36.9365414587923,
37.4330475550838,37.9295536513754,38.4260597476669,38.9225658439584,39.41907194025,
39.9155780365415,40.412084132833,40.8407044966673),.UNSPECIFIED.);
#376=B_SPLINE_CURVE_WITH_KNOTS('',3,(#43003,#43004,#43005,#43006,#43007,
#43008,#43009,#43010,#43011,#43012,#43013,#43014,#43015,#43016,#43017,#43018,
#43019),.UNSPECIFIED.,.F.,.F.,(4,1,1,1,1,1,1,1,1,1,1,1,1,1,4),(34.5575191894876,
34.6247190550045,35.1212251512961,35.6177312475876,36.1142373438791,36.6107434401706,
37.1072495364622,37.6037556327537,38.1002617290452,38.5967678253368,39.0932739216283,
39.5897800179198,40.0862861142114,40.5827922105029,40.8407044966672),
 .UNSPECIFIED.);
#377=B_SPLINE_CURVE_WITH_KNOTS('',3,(#43024,#43025,#43026,#43027,#43028,
#43029,#43030,#43031,#43032,#43033,#43034,#43035,#43036,#43037,#43038,#43039,
#43040),.UNSPECIFIED.,.F.,.F.,(4,1,1,1,1,1,1,1,1,1,1,1,1,1,4),(28.2743338823081,
28.4959378218363,28.9924439181278,29.4889500144193,29.9854561107109,30.4819622070024,
30.9784683032939,31.4749743995855,31.971480495877,32.4679865921685,32.9644926884601,
33.4609987847516,33.9575048810431,34.4540109773346,34.5575191894877),
 .UNSPECIFIED.);
#378=B_SPLINE_CURVE_WITH_KNOTS('',3,(#43041,#43042,#43043,#43044,#43045,
#43046,#43047,#43048,#43049,#43050,#43051,#43052,#43053,#43054,#43055,#43056),
 .UNSPECIFIED.,.F.,.F.,(4,1,1,1,1,1,1,1,1,1,1,1,1,4),(28.274333882308,28.6666458995061,
29.1631519957977,29.6596580920892,30.1561641883807,30.6526702846723,31.1491763809638,
31.6456824772553,32.1421885735469,32.6386946698384,33.1352007661299,33.6317068624215,
34.128212958713,34.5575191894876),.UNSPECIFIED.);
#379=B_SPLINE_CURVE_WITH_KNOTS('',3,(#43061,#43062,#43063,#43064,#43065,
#43066,#43067,#43068,#43069,#43070,#43071,#43072,#43073,#43074,#43075,#43076,
#43077),.UNSPECIFIED.,.F.,.F.,(4,1,1,1,1,1,1,1,1,1,1,1,1,1,4),(21.9911485751285,
22.0413585700464,22.5378646663379,23.0343707626294,23.530876858921,24.0273829552125,
24.523889051504,25.0203951477956,25.5169012440871,26.0134073403786,26.5099134366701,
27.0064195329617,27.5029256292532,27.9994317255447,28.2743338823081),
 .UNSPECIFIED.);
#380=B_SPLINE_CURVE_WITH_KNOTS('',3,(#43078,#43079,#43080,#43081,#43082,
#43083,#43084,#43085,#43086,#43087,#43088,#43089,#43090,#43091,#43092,#43093,
#43094),.UNSPECIFIED.,.F.,.F.,(4,1,1,1,1,1,1,1,1,1,1,1,1,1,4),(21.9911485751285,
22.2120666477162,22.7085727440078,23.2050788402993,23.7015849365908,24.1980910328824,
24.6945971291739,25.1911032254654,25.687609321757,26.1841154180485,26.68062151434,
27.1771276106316,27.6736337069231,28.1701398032146,28.274333882308),
 .UNSPECIFIED.);
#381=B_SPLINE_CURVE_WITH_KNOTS('',3,(#43099,#43100,#43101,#43102,#43103,
#43104,#43105,#43106,#43107,#43108,#43109,#43110,#43111,#43112,#43113,#43114),
 .UNSPECIFIED.,.F.,.F.,(4,1,1,1,1,1,1,1,1,1,1,1,1,4),(15.7079632679489,
16.083285414548,16.5797915108395,17.0762976071311,17.5728037034226,18.0693097997141,
18.5658158960056,19.0623219922972,19.5588280885887,20.0553341848802,20.5518402811718,
21.0483463774633,21.5448524737548,21.9911485751285),.UNSPECIFIED.);
#382=B_SPLINE_CURVE_WITH_KNOTS('',3,(#43115,#43116,#43117,#43118,#43119,
#43120,#43121,#43122,#43123,#43124,#43125,#43126,#43127,#43128,#43129,#43130,
#43131),.UNSPECIFIED.,.F.,.F.,(4,1,1,1,1,1,1,1,1,1,1,1,1,1,4),(15.7079632679489,
15.7574873959263,16.2539934922179,16.7504995885094,17.2470056848009,17.7435117810925,
18.240017877384,18.7365239736755,19.2330300699671,19.7295361662586,20.2260422625501,
20.7225483588416,21.2190544551332,21.7155605514247,21.9911485751285),
 .UNSPECIFIED.);
#383=B_SPLINE_CURVE_WITH_KNOTS('',3,(#43133,#43134,#43135,#43136,#43137,
#43138,#43139,#43140,#43141,#43142,#43143,#43144,#43145,#43146,#43147,#43148,
#43149,#43150,#43151,#43152,#43153,#43154,#43155,#43156,#43157,#43158,#43159,
#43160,#43161,#43162,#43163,#43164,#43165,#43166,#43167,#43168,#43169,#43170,
#43171,#43172,#43173,#43174,#43175,#43176,#43177,#43178,#43179,#43180,#43181,
#43182,#43183,#43184,#43185,#43186,#43187,#43188,#43189,#43190,#43191,#43192,
#43193,#43194,#43195,#43196,#43197,#43198,#43199,#43200,#43201,#43202,#43203,
#43204,#43205,#43206,#43207,#43208,#43209,#43210,#43211,#43212,#43213,#43214,
#43215,#43216,#43217,#43218,#43219,#43220,#43221,#43222,#43223,#43224,#43225,
#43226,#43227,#43228,#43229,#43230,#43231,#43232,#43233,#43234,#43235),
 .UNSPECIFIED.,.F.,.F.,(4,3,3,3,3,3,3,3,3,3,3,3,3,3,3,3,3,3,3,3,3,3,3,3,
3,3,3,3,3,3,3,3,3,3,4),(-0.937740963081824,-0.904523217505006,-0.866625128668399,
-0.845007794788879,-0.830203217768472,-0.823788649298019,-0.784867066646426,
-0.745695756246804,-0.730731146380581,-0.722415114958876,-0.713900080041304,
-0.693686457632239,-0.654578468140619,-0.614852605890178,-0.579246347886379,
-0.552541654383529,-0.547074308466247,-0.506129338035449,-0.472427573874981,
-0.431684200951587,-0.390608431412487,-0.376471022267793,-0.370730708360049,
-0.329054764822938,-0.285097860757189,-0.24114095669144,-0.21099833710501,
-0.197810941035947,-0.189566456838293,-0.18424425154934,-0.141986144540954,
-0.0988362730036117,-0.0555327093168028,-0.0126020697380223,0.),
 .UNSPECIFIED.);
#384=B_SPLINE_CURVE_WITH_KNOTS('',3,(#43238,#43239,#43240,#43241,#43242,
#43243,#43244,#43245,#43246,#43247,#43248,#43249,#43250,#43251,#43252,#43253,
#43254,#43255,#43256,#43257,#43258,#43259,#43260,#43261,#43262,#43263,#43264,
#43265,#43266,#43267,#43268,#43269,#43270,#43271,#43272,#43273,#43274,#43275,
#43276,#43277,#43278,#43279,#43280,#43281,#43282,#43283,#43284,#43285,#43286,
#43287,#43288,#43289,#43290,#43291,#43292,#43293,#43294,#43295,#43296,#43297,
#43298,#43299,#43300,#43301,#43302,#43303,#43304,#43305,#43306,#43307,#43308,
#43309,#43310,#43311,#43312,#43313,#43314,#43315,#43316,#43317,#43318,#43319,
#43320,#43321,#43322,#43323,#43324,#43325,#43326,#43327,#43328,#43329,#43330,
#43331,#43332,#43333,#43334,#43335,#43336,#43337,#43338,#43339,#43340),
 .UNSPECIFIED.,.F.,.F.,(4,3,3,3,3,3,3,3,3,3,3,3,3,3,3,3,3,3,3,3,3,3,3,3,
3,3,3,3,3,3,3,3,3,3,4),(-0.93397589402309,-0.894422503905188,-0.851092289922783,
-0.826729421212481,-0.807865956409088,-0.801823722421914,-0.759290601264971,
-0.717093733962539,-0.686641537101452,-0.680702739992375,-0.656189340240365,
-0.614616501183358,-0.572941838791487,-0.536581284129042,-0.509310868132208,
-0.503319094267446,-0.498509563752087,-0.458073882399315,-0.427499620141708,
-0.386898349768095,-0.346636041099517,-0.332619841408937,-0.324859429439165,
-0.285375022877491,-0.246326502361671,-0.208719056729236,-0.182629174638081,
-0.169421423696199,-0.162163161061763,-0.157293280629028,-0.117969960471771,
-0.079679826239659,-0.0398399131198295,-0.00282314033426902,0.),
 .UNSPECIFIED.);
#385=B_SPLINE_CURVE_WITH_KNOTS('',3,(#44329,#44330,#44331,#44332),
 .UNSPECIFIED.,.F.,.F.,(4,4),(126.778588152808,127.025062960147),
 .UNSPECIFIED.);
#386=B_SPLINE_CURVE_WITH_KNOTS('',3,(#44334,#44335,#44336,#44337,#44338,
#44339,#44340,#44341,#44342,#44343,#44344,#44345,#44346,#44347,#44348,#44349,
#44350,#44351,#44352,#44353,#44354,#44355,#44356,#44357,#44358,#44359,#44360,
#44361,#44362,#44363,#44364,#44365,#44366,#44367,#44368,#44369,#44370,#44371,
#44372,#44373,#44374,#44375,#44376,#44377,#44378,#44379,#44380,#44381,#44382,
#44383,#44384,#44385,#44386,#44387,#44388,#44389,#44390,#44391,#44392,#44393,
#44394,#44395,#44396,#44397,#44398,#44399,#44400,#44401,#44402,#44403,#44404,
#44405,#44406,#44407,#44408,#44409,#44410,#44411,#44412,#44413,#44414,#44415,
#44416,#44417,#44418,#44419,#44420,#44421,#44422,#44423,#44424,#44425,#44426,
#44427,#44428,#44429,#44430,#44431,#44432,#44433,#44434,#44435,#44436),
 .UNSPECIFIED.,.F.,.F.,(4,3,3,3,3,3,3,3,3,3,3,3,3,3,3,3,3,3,3,3,3,3,3,3,
3,3,3,3,3,3,3,3,3,3,4),(-0.937740963081816,-0.904523217504992,-0.866625127455818,
-0.845007793727865,-0.830203217197392,-0.823788648517869,-0.784867065183403,
-0.745695754812804,-0.73073114487324,-0.722415112751658,-0.713900080444087,
-0.693686457632193,-0.654578469885656,-0.614852608246762,-0.579246349653809,
-0.552541655709094,-0.547074309750651,-0.506129339576615,-0.472427573874949,
-0.431684202389108,-0.390608433430914,-0.376471029494825,-0.370730712409322,
-0.329054770401609,-0.285097863546512,-0.241140956691414,-0.210998337104987,
-0.197810941035925,-0.189566457200723,-0.18424425222828,-0.141986138823205,
-0.0988362638567851,-0.0555327002774816,-0.0126020669544512,0.),
 .UNSPECIFIED.);
#387=B_SPLINE_CURVE_WITH_KNOTS('',3,(#44437,#44438,#44439,#44440,#44441,
#44442,#44443,#44444,#44445,#44446,#44447,#44448,#44449,#44450),
 .UNSPECIFIED.,.F.,.F.,(4,1,1,1,1,1,1,1,1,1,1,4),(10.3764180272042,10.792426433011,
11.2889325293026,11.7854386255941,12.2819447218856,12.7784508181771,13.2749569144687,
13.7714630107602,14.2679691070517,14.7644752033433,15.2609812996348,15.7079632679489),
 .UNSPECIFIED.);
#388=B_SPLINE_CURVE_WITH_KNOTS('',3,(#44456,#44457,#44458,#44459,#44460,
#44461,#44462,#44463,#44464,#44465,#44466,#44467,#44468,#44469,#44470,#44471,
#44472,#44473,#44474,#44475,#44476,#44477,#44478,#44479,#44480,#44481,#44482,
#44483,#44484,#44485,#44486,#44487,#44488,#44489,#44490,#44491,#44492,#44493,
#44494,#44495,#44496,#44497,#44498,#44499,#44500,#44501,#44502,#44503,#44504,
#44505,#44506,#44507,#44508,#44509,#44510,#44511,#44512,#44513,#44514,#44515,
#44516,#44517,#44518,#44519,#44520,#44521,#44522,#44523,#44524,#44525,#44526,
#44527,#44528,#44529,#44530,#44531,#44532,#44533,#44534,#44535,#44536,#44537,
#44538,#44539,#44540,#44541,#44542,#44543,#44544,#44545,#44546,#44547,#44548,
#44549,#44550,#44551,#44552,#44553,#44554,#44555,#44556,#44557,#44558),
 .UNSPECIFIED.,.F.,.F.,(4,3,3,3,3,3,3,3,3,3,3,3,3,3,3,3,3,3,3,3,3,3,3,3,
3,3,3,3,3,3,3,3,3,3,4),(-0.933975894023135,-0.894422503905226,-0.851092289888165,
-0.826729421182192,-0.807865956515983,-0.801823722677367,-0.759290601541375,
-0.717093734614832,-0.686641537427605,-0.68070274056291,-0.656189340240378,
-0.614616501299998,-0.572941837912828,-0.536581283470049,-0.509310867637965,
-0.503319090789543,-0.498509560266509,-0.458073876993764,-0.427499620141712,
-0.386898351256557,-0.346636047946469,-0.332619869734945,-0.324859425120058,
-0.28537502006118,-0.246326506168717,-0.208719056729237,-0.182629174638083,
-0.169421424350286,-0.162163163629911,-0.15729328458594,-0.117969963439455,
-0.079679824896869,-0.0398399124484345,-0.00282312955145499,0.),
 .UNSPECIFIED.);
#389=B_SPLINE_CURVE_WITH_KNOTS('',3,(#44561,#44562,#44563,#44564,#44565,
#44566,#44567,#44568,#44569,#44570,#44571,#44572),.UNSPECIFIED.,.F.,.F.,
(4,1,1,1,1,1,1,1,1,4),(11.6147305479242,12.1112366442157,12.6077427405073,
13.1042488367988,13.6007549330903,14.0972610293819,14.5937671256734,15.0902732219649,
15.5867793182565,15.7079632679489),.UNSPECIFIED.);
#398=B_SPLINE_SURFACE_WITH_KNOTS('',3,3,((#43341,#43342,#43343,#43344,#43345,
#43346,#43347,#43348,#43349,#43350,#43351,#43352,#43353,#43354,#43355,#43356,
#43357,#43358,#43359,#43360,#43361,#43362,#43363,#43364,#43365,#43366,#43367,
#43368,#43369,#43370,#43371,#43372,#43373,#43374,#43375,#43376,#43377,#43378,
#43379,#43380,#43381,#43382,#43383,#43384,#43385,#43386,#43387,#43388,#43389,
#43390,#43391,#43392,#43393,#43394,#43395,#43396,#43397,#43398,#43399,#43400,
#43401,#43402,#43403,#43404,#43405,#43406,#43407,#43408,#43409,#43410,#43411,
#43412,#43413,#43414,#43415,#43416,#43417,#43418,#43419,#43420,#43421,#43422,
#43423,#43424,#43425,#43426,#43427,#43428,#43429,#43430,#43431,#43432,#43433,
#43434,#43435,#43436,#43437,#43438,#43439,#43440,#43441,#43442,#43443,#43444,
#43445,#43446,#43447,#43448,#43449,#43450,#43451,#43452,#43453,#43454,#43455,
#43456,#43457,#43458,#43459,#43460,#43461,#43462,#43463,#43464,#43465,#43466,
#43467,#43468,#43469,#43470,#43471,#43472,#43473,#43474,#43475,#43476,#43477,
#43478,#43479,#43480,#43481,#43482,#43483,#43484,#43485,#43486,#43487,#43488,
#43489,#43490,#43491,#43492,#43493,#43494,#43495,#43496,#43497,#43498,#43499,
#43500,#43501,#43502,#43503,#43504,#43505,#43506,#43507,#43508,#43509,#43510,
#43511,#43512,#43513,#43514,#43515,#43516,#43517,#43518,#43519,#43520,#43521,
#43522,#43523,#43524,#43525,#43526,#43527,#43528,#43529,#43530,#43531,#43532,
#43533,#43534,#43535,#43536,#43537,#43538,#43539,#43540,#43541,#43542,#43543,
#43544,#43545,#43546,#43547,#43548,#43549,#43550,#43551,#43552,#43553,#43554,
#43555,#43556,#43557,#43558,#43559,#43560,#43561,#43562,#43563,#43564,#43565,
#43566,#43567,#43568,#43569,#43570,#43571,#43572,#43573,#43574,#43575,#43576,
#43577,#43578,#43579,#43580,#43581,#43582,#43583,#43584,#43585,#43586,#43587),
(#43588,#43589,#43590,#43591,#43592,#43593,#43594,#43595,#43596,#43597,
#43598,#43599,#43600,#43601,#43602,#43603,#43604,#43605,#43606,#43607,#43608,
#43609,#43610,#43611,#43612,#43613,#43614,#43615,#43616,#43617,#43618,#43619,
#43620,#43621,#43622,#43623,#43624,#43625,#43626,#43627,#43628,#43629,#43630,
#43631,#43632,#43633,#43634,#43635,#43636,#43637,#43638,#43639,#43640,#43641,
#43642,#43643,#43644,#43645,#43646,#43647,#43648,#43649,#43650,#43651,#43652,
#43653,#43654,#43655,#43656,#43657,#43658,#43659,#43660,#43661,#43662,#43663,
#43664,#43665,#43666,#43667,#43668,#43669,#43670,#43671,#43672,#43673,#43674,
#43675,#43676,#43677,#43678,#43679,#43680,#43681,#43682,#43683,#43684,#43685,
#43686,#43687,#43688,#43689,#43690,#43691,#43692,#43693,#43694,#43695,#43696,
#43697,#43698,#43699,#43700,#43701,#43702,#43703,#43704,#43705,#43706,#43707,
#43708,#43709,#43710,#43711,#43712,#43713,#43714,#43715,#43716,#43717,#43718,
#43719,#43720,#43721,#43722,#43723,#43724,#43725,#43726,#43727,#43728,#43729,
#43730,#43731,#43732,#43733,#43734,#43735,#43736,#43737,#43738,#43739,#43740,
#43741,#43742,#43743,#43744,#43745,#43746,#43747,#43748,#43749,#43750,#43751,
#43752,#43753,#43754,#43755,#43756,#43757,#43758,#43759,#43760,#43761,#43762,
#43763,#43764,#43765,#43766,#43767,#43768,#43769,#43770,#43771,#43772,#43773,
#43774,#43775,#43776,#43777,#43778,#43779,#43780,#43781,#43782,#43783,#43784,
#43785,#43786,#43787,#43788,#43789,#43790,#43791,#43792,#43793,#43794,#43795,
#43796,#43797,#43798,#43799,#43800,#43801,#43802,#43803,#43804,#43805,#43806,
#43807,#43808,#43809,#43810,#43811,#43812,#43813,#43814,#43815,#43816,#43817,
#43818,#43819,#43820,#43821,#43822,#43823,#43824,#43825,#43826,#43827,#43828,
#43829,#43830,#43831,#43832,#43833,#43834),(#43835,#43836,#43837,#43838,
#43839,#43840,#43841,#43842,#43843,#43844,#43845,#43846,#43847,#43848,#43849,
#43850,#43851,#43852,#43853,#43854,#43855,#43856,#43857,#43858,#43859,#43860,
#43861,#43862,#43863,#43864,#43865,#43866,#43867,#43868,#43869,#43870,#43871,
#43872,#43873,#43874,#43875,#43876,#43877,#43878,#43879,#43880,#43881,#43882,
#43883,#43884,#43885,#43886,#43887,#43888,#43889,#43890,#43891,#43892,#43893,
#43894,#43895,#43896,#43897,#43898,#43899,#43900,#43901,#43902,#43903,#43904,
#43905,#43906,#43907,#43908,#43909,#43910,#43911,#43912,#43913,#43914,#43915,
#43916,#43917,#43918,#43919,#43920,#43921,#43922,#43923,#43924,#43925,#43926,
#43927,#43928,#43929,#43930,#43931,#43932,#43933,#43934,#43935,#43936,#43937,
#43938,#43939,#43940,#43941,#43942,#43943,#43944,#43945,#43946,#43947,#43948,
#43949,#43950,#43951,#43952,#43953,#43954,#43955,#43956,#43957,#43958,#43959,
#43960,#43961,#43962,#43963,#43964,#43965,#43966,#43967,#43968,#43969,#43970,
#43971,#43972,#43973,#43974,#43975,#43976,#43977,#43978,#43979,#43980,#43981,
#43982,#43983,#43984,#43985,#43986,#43987,#43988,#43989,#43990,#43991,#43992,
#43993,#43994,#43995,#43996,#43997,#43998,#43999,#44000,#44001,#44002,#44003,
#44004,#44005,#44006,#44007,#44008,#44009,#44010,#44011,#44012,#44013,#44014,
#44015,#44016,#44017,#44018,#44019,#44020,#44021,#44022,#44023,#44024,#44025,
#44026,#44027,#44028,#44029,#44030,#44031,#44032,#44033,#44034,#44035,#44036,
#44037,#44038,#44039,#44040,#44041,#44042,#44043,#44044,#44045,#44046,#44047,
#44048,#44049,#44050,#44051,#44052,#44053,#44054,#44055,#44056,#44057,#44058,
#44059,#44060,#44061,#44062,#44063,#44064,#44065,#44066,#44067,#44068,#44069,
#44070,#44071,#44072,#44073,#44074,#44075,#44076,#44077,#44078,#44079,#44080,
#44081),(#44082,#44083,#44084,#44085,#44086,#44087,#44088,#44089,#44090,
#44091,#44092,#44093,#44094,#44095,#44096,#44097,#44098,#44099,#44100,#44101,
#44102,#44103,#44104,#44105,#44106,#44107,#44108,#44109,#44110,#44111,#44112,
#44113,#44114,#44115,#44116,#44117,#44118,#44119,#44120,#44121,#44122,#44123,
#44124,#44125,#44126,#44127,#44128,#44129,#44130,#44131,#44132,#44133,#44134,
#44135,#44136,#44137,#44138,#44139,#44140,#44141,#44142,#44143,#44144,#44145,
#44146,#44147,#44148,#44149,#44150,#44151,#44152,#44153,#44154,#44155,#44156,
#44157,#44158,#44159,#44160,#44161,#44162,#44163,#44164,#44165,#44166,#44167,
#44168,#44169,#44170,#44171,#44172,#44173,#44174,#44175,#44176,#44177,#44178,
#44179,#44180,#44181,#44182,#44183,#44184,#44185,#44186,#44187,#44188,#44189,
#44190,#44191,#44192,#44193,#44194,#44195,#44196,#44197,#44198,#44199,#44200,
#44201,#44202,#44203,#44204,#44205,#44206,#44207,#44208,#44209,#44210,#44211,
#44212,#44213,#44214,#44215,#44216,#44217,#44218,#44219,#44220,#44221,#44222,
#44223,#44224,#44225,#44226,#44227,#44228,#44229,#44230,#44231,#44232,#44233,
#44234,#44235,#44236,#44237,#44238,#44239,#44240,#44241,#44242,#44243,#44244,
#44245,#44246,#44247,#44248,#44249,#44250,#44251,#44252,#44253,#44254,#44255,
#44256,#44257,#44258,#44259,#44260,#44261,#44262,#44263,#44264,#44265,#44266,
#44267,#44268,#44269,#44270,#44271,#44272,#44273,#44274,#44275,#44276,#44277,
#44278,#44279,#44280,#44281,#44282,#44283,#44284,#44285,#44286,#44287,#44288,
#44289,#44290,#44291,#44292,#44293,#44294,#44295,#44296,#44297,#44298,#44299,
#44300,#44301,#44302,#44303,#44304,#44305,#44306,#44307,#44308,#44309,#44310,
#44311,#44312,#44313,#44314,#44315,#44316,#44317,#44318,#44319,#44320,#44321,
#44322,#44323,#44324,#44325,#44326,#44327,#44328)),.UNSPECIFIED.,.F.,.F.,
 .F.,(4,4),(4,1,1,1,1,1,1,1,1,1,1,1,1,1,1,1,1,1,1,1,1,1,1,1,1,1,1,1,1,1,
1,1,1,1,1,1,1,1,1,1,1,1,1,1,1,1,1,1,1,1,1,1,1,1,1,1,1,1,1,1,1,1,1,1,1,1,
1,1,1,1,1,1,1,1,1,1,1,1,1,1,1,1,1,1,1,1,1,1,1,1,1,1,1,1,1,1,1,1,1,1,1,1,
1,1,1,1,1,1,1,1,1,1,1,1,1,1,1,1,1,1,1,1,1,1,1,1,1,1,1,1,1,1,1,1,1,1,1,1,
1,1,1,1,1,1,1,1,1,1,1,1,1,1,1,1,1,1,1,1,1,1,1,1,1,1,1,1,1,1,1,1,1,1,1,1,
1,1,1,1,1,1,1,1,1,1,1,1,1,1,1,1,1,1,1,1,1,1,1,1,1,1,1,1,1,1,1,1,1,1,1,1,
1,1,1,1,1,1,1,1,1,1,1,1,1,1,1,1,1,1,1,1,1,1,1,1,1,1,1,1,1,1,1,1,1,1,4),
(0.,0.0986691610045074),(8.30989595155336,8.80640204784489,9.30290814413643,
9.79941424042796,10.2959203367195,10.792426433011,11.2889325293026,11.7854386255941,
12.2819447218856,12.7784508181771,13.2749569144687,13.7714630107602,14.2679691070517,
14.7644752033433,15.2609812996348,15.7574873959263,16.2539934922179,16.7504995885094,
17.2470056848009,17.7435117810925,18.240017877384,18.7365239736755,19.2330300699671,
19.7295361662586,20.2260422625501,20.7225483588416,21.2190544551332,21.7155605514247,
22.2120666477162,22.7085727440078,23.2050788402993,23.7015849365908,24.1980910328824,
24.6945971291739,25.1911032254654,25.687609321757,26.1841154180485,26.68062151434,
27.1771276106316,27.6736337069231,28.1701398032146,28.6666458995061,29.1631519957977,
29.6596580920892,30.1561641883807,30.6526702846723,31.1491763809638,31.6456824772553,
32.1421885735469,32.6386946698384,33.1352007661299,33.6317068624215,34.128212958713,
34.6247190550045,35.1212251512961,35.6177312475876,36.1142373438791,36.6107434401706,
37.1072495364622,37.6037556327537,38.1002617290452,38.5967678253368,39.0932739216283,
39.5897800179198,40.0862861142114,40.5827922105029,41.0792983067944,41.575804403086,
42.0723104993775,42.568816595669,43.0653226919606,43.5618287882521,44.0583348845436,
44.5548409808351,45.0513470771267,45.5478531734182,46.0443592697097,46.5408653660013,
47.0373714622928,47.5338775585843,48.0303836548759,48.5268897511674,49.0233958474589,
49.5199019437505,50.016408040042,50.5129141363335,51.0094202326251,51.5059263289166,
52.0024324252081,52.4989385214996,52.9954446177912,53.4919507140827,53.9884568103742,
54.4849629066658,54.9814690029573,55.4779750992488,55.9744811955404,56.4709872918319,
56.9674933881234,57.463999484415,57.9605055807065,58.457011676998,58.9535177732896,
59.4500238695811,59.9465299658726,60.4430360621641,60.9395421584557,61.4360482547472,
61.9325543510387,62.4290604473303,62.9255665436218,63.4220726399133,63.9185787362049,
64.4150848324964,64.9115909287879,65.904603121371,66.897615313954,67.8906275065371,
68.8836396991202,69.8766518917032,70.8696640842863,71.8626762768694,72.8556884694524,
73.8487006620355,74.8417128546185,75.8347250472016,76.8277372397847,77.8207494323677,
78.8137616249508,79.8067738175339,80.7997860101169,81.2962921064085,81.7927982027,
82.2893042989915,82.7858103952831,83.2823164915746,83.7788225878661,84.2753286841576,
84.7718347804492,85.2683408767407,85.7648469730322,86.2613530693238,86.7578591656153,
87.2543652619068,87.7508713581984,88.2473774544899,88.7438835507814,89.240389647073,
89.7368957433645,90.233401839656,90.7299079359476,91.2264140322391,91.7229201285306,
92.2194262248221,92.7159323211137,93.2124384174052,93.7089445136967,94.2054506099883,
94.7019567062798,95.1984628025713,95.6949688988629,96.1914749951544,96.6879810914459,
97.1844871877375,97.680993284029,98.1774993803205,98.6740054766121,99.1705115729036,
99.6670176691951,100.163523765487,100.660029861778,101.15653595807,101.653042054361,
102.149548150653,102.646054246944,103.142560343236,103.639066439527,104.135572535819,
104.63207863211,105.128584728402,105.625090824693,106.121596920985,106.618103017277,
107.114609113568,107.61111520986,108.107621306151,108.604127402443,109.100633498734,
109.597139595026,110.093645691317,110.590151787609,111.0866578839,111.583163980192,
112.079670076483,112.576176172775,113.072682269066,113.569188365358,114.06569446165,
114.562200557941,115.058706654233,115.555212750524,116.051718846816,116.548224943107,
117.044731039399,117.54123713569,118.037743231982,118.534249328273,119.030755424565,
119.527261520856,120.023767617148,120.520273713439,121.016779809731,121.513285906022,
122.009792002314,122.506298098606,123.002804194897,123.499310291189,123.99581638748,
124.492322483772,124.988828580063,125.485334676355,125.981840772646,126.478346868938,
126.974852965229,127.471359061521,127.967865157812,128.464371254104,128.960877350395,
129.457383446687,129.953889542979,130.45039563927,130.946901735562,131.443407831853,
131.939913928145,132.436420024436,132.932926120728,133.429432217019,133.925938313311,
134.422444409602,134.918950505894,135.415456602185,135.911962698477,136.408468794768,
136.90497489106,137.401480987351),.UNSPECIFIED.);
#399=B_SPLINE_SURFACE_WITH_KNOTS('',3,3,((#44573,#44574,#44575,#44576,#44577,
#44578,#44579,#44580,#44581,#44582,#44583,#44584,#44585,#44586,#44587,#44588,
#44589,#44590,#44591,#44592,#44593,#44594,#44595,#44596,#44597,#44598,#44599,
#44600,#44601,#44602,#44603,#44604,#44605,#44606,#44607,#44608,#44609,#44610,
#44611,#44612,#44613,#44614,#44615,#44616,#44617,#44618,#44619,#44620,#44621,
#44622,#44623,#44624,#44625,#44626,#44627,#44628,#44629,#44630,#44631,#44632,
#44633,#44634,#44635,#44636,#44637,#44638,#44639,#44640,#44641,#44642,#44643,
#44644,#44645,#44646,#44647,#44648,#44649,#44650,#44651,#44652,#44653,#44654,
#44655,#44656,#44657,#44658,#44659,#44660,#44661,#44662,#44663,#44664,#44665,
#44666,#44667,#44668,#44669,#44670,#44671,#44672,#44673,#44674,#44675,#44676,
#44677,#44678,#44679,#44680,#44681,#44682,#44683,#44684,#44685,#44686,#44687,
#44688,#44689,#44690,#44691,#44692,#44693,#44694,#44695,#44696,#44697,#44698,
#44699,#44700,#44701,#44702,#44703,#44704,#44705,#44706,#44707,#44708,#44709,
#44710,#44711,#44712,#44713,#44714,#44715,#44716,#44717,#44718,#44719,#44720,
#44721,#44722,#44723,#44724,#44725,#44726,#44727,#44728,#44729,#44730,#44731,
#44732,#44733,#44734,#44735,#44736,#44737,#44738,#44739,#44740,#44741,#44742,
#44743,#44744,#44745,#44746,#44747,#44748,#44749,#44750,#44751,#44752,#44753,
#44754,#44755,#44756,#44757,#44758,#44759,#44760,#44761,#44762,#44763,#44764,
#44765,#44766,#44767,#44768,#44769,#44770,#44771,#44772,#44773,#44774,#44775,
#44776,#44777,#44778,#44779,#44780,#44781,#44782,#44783,#44784,#44785,#44786,
#44787,#44788,#44789,#44790,#44791,#44792,#44793,#44794,#44795,#44796,#44797,
#44798,#44799,#44800,#44801,#44802,#44803,#44804,#44805,#44806,#44807,#44808,
#44809,#44810,#44811,#44812,#44813,#44814,#44815,#44816,#44817,#44818,#44819,
#44820,#44821),(#44822,#44823,#44824,#44825,#44826,#44827,#44828,#44829,
#44830,#44831,#44832,#44833,#44834,#44835,#44836,#44837,#44838,#44839,#44840,
#44841,#44842,#44843,#44844,#44845,#44846,#44847,#44848,#44849,#44850,#44851,
#44852,#44853,#44854,#44855,#44856,#44857,#44858,#44859,#44860,#44861,#44862,
#44863,#44864,#44865,#44866,#44867,#44868,#44869,#44870,#44871,#44872,#44873,
#44874,#44875,#44876,#44877,#44878,#44879,#44880,#44881,#44882,#44883,#44884,
#44885,#44886,#44887,#44888,#44889,#44890,#44891,#44892,#44893,#44894,#44895,
#44896,#44897,#44898,#44899,#44900,#44901,#44902,#44903,#44904,#44905,#44906,
#44907,#44908,#44909,#44910,#44911,#44912,#44913,#44914,#44915,#44916,#44917,
#44918,#44919,#44920,#44921,#44922,#44923,#44924,#44925,#44926,#44927,#44928,
#44929,#44930,#44931,#44932,#44933,#44934,#44935,#44936,#44937,#44938,#44939,
#44940,#44941,#44942,#44943,#44944,#44945,#44946,#44947,#44948,#44949,#44950,
#44951,#44952,#44953,#44954,#44955,#44956,#44957,#44958,#44959,#44960,#44961,
#44962,#44963,#44964,#44965,#44966,#44967,#44968,#44969,#44970,#44971,#44972,
#44973,#44974,#44975,#44976,#44977,#44978,#44979,#44980,#44981,#44982,#44983,
#44984,#44985,#44986,#44987,#44988,#44989,#44990,#44991,#44992,#44993,#44994,
#44995,#44996,#44997,#44998,#44999,#45000,#45001,#45002,#45003,#45004,#45005,
#45006,#45007,#45008,#45009,#45010,#45011,#45012,#45013,#45014,#45015,#45016,
#45017,#45018,#45019,#45020,#45021,#45022,#45023,#45024,#45025,#45026,#45027,
#45028,#45029,#45030,#45031,#45032,#45033,#45034,#45035,#45036,#45037,#45038,
#45039,#45040,#45041,#45042,#45043,#45044,#45045,#45046,#45047,#45048,#45049,
#45050,#45051,#45052,#45053,#45054,#45055,#45056,#45057,#45058,#45059,#45060,
#45061,#45062,#45063,#45064,#45065,#45066,#45067,#45068,#45069,#45070),
(#45071,#45072,#45073,#45074,#45075,#45076,#45077,#45078,#45079,#45080,
#45081,#45082,#45083,#45084,#45085,#45086,#45087,#45088,#45089,#45090,#45091,
#45092,#45093,#45094,#45095,#45096,#45097,#45098,#45099,#45100,#45101,#45102,
#45103,#45104,#45105,#45106,#45107,#45108,#45109,#45110,#45111,#45112,#45113,
#45114,#45115,#45116,#45117,#45118,#45119,#45120,#45121,#45122,#45123,#45124,
#45125,#45126,#45127,#45128,#45129,#45130,#45131,#45132,#45133,#45134,#45135,
#45136,#45137,#45138,#45139,#45140,#45141,#45142,#45143,#45144,#45145,#45146,
#45147,#45148,#45149,#45150,#45151,#45152,#45153,#45154,#45155,#45156,#45157,
#45158,#45159,#45160,#45161,#45162,#45163,#45164,#45165,#45166,#45167,#45168,
#45169,#45170,#45171,#45172,#45173,#45174,#45175,#45176,#45177,#45178,#45179,
#45180,#45181,#45182,#45183,#45184,#45185,#45186,#45187,#45188,#45189,#45190,
#45191,#45192,#45193,#45194,#45195,#45196,#45197,#45198,#45199,#45200,#45201,
#45202,#45203,#45204,#45205,#45206,#45207,#45208,#45209,#45210,#45211,#45212,
#45213,#45214,#45215,#45216,#45217,#45218,#45219,#45220,#45221,#45222,#45223,
#45224,#45225,#45226,#45227,#45228,#45229,#45230,#45231,#45232,#45233,#45234,
#45235,#45236,#45237,#45238,#45239,#45240,#45241,#45242,#45243,#45244,#45245,
#45246,#45247,#45248,#45249,#45250,#45251,#45252,#45253,#45254,#45255,#45256,
#45257,#45258,#45259,#45260,#45261,#45262,#45263,#45264,#45265,#45266,#45267,
#45268,#45269,#45270,#45271,#45272,#45273,#45274,#45275,#45276,#45277,#45278,
#45279,#45280,#45281,#45282,#45283,#45284,#45285,#45286,#45287,#45288,#45289,
#45290,#45291,#45292,#45293,#45294,#45295,#45296,#45297,#45298,#45299,#45300,
#45301,#45302,#45303,#45304,#45305,#45306,#45307,#45308,#45309,#45310,#45311,
#45312,#45313,#45314,#45315,#45316,#45317,#45318,#45319),(#45320,#45321,
#45322,#45323,#45324,#45325,#45326,#45327,#45328,#45329,#45330,#45331,#45332,
#45333,#45334,#45335,#45336,#45337,#45338,#45339,#45340,#45341,#45342,#45343,
#45344,#45345,#45346,#45347,#45348,#45349,#45350,#45351,#45352,#45353,#45354,
#45355,#45356,#45357,#45358,#45359,#45360,#45361,#45362,#45363,#45364,#45365,
#45366,#45367,#45368,#45369,#45370,#45371,#45372,#45373,#45374,#45375,#45376,
#45377,#45378,#45379,#45380,#45381,#45382,#45383,#45384,#45385,#45386,#45387,
#45388,#45389,#45390,#45391,#45392,#45393,#45394,#45395,#45396,#45397,#45398,
#45399,#45400,#45401,#45402,#45403,#45404,#45405,#45406,#45407,#45408,#45409,
#45410,#45411,#45412,#45413,#45414,#45415,#45416,#45417,#45418,#45419,#45420,
#45421,#45422,#45423,#45424,#45425,#45426,#45427,#45428,#45429,#45430,#45431,
#45432,#45433,#45434,#45435,#45436,#45437,#45438,#45439,#45440,#45441,#45442,
#45443,#45444,#45445,#45446,#45447,#45448,#45449,#45450,#45451,#45452,#45453,
#45454,#45455,#45456,#45457,#45458,#45459,#45460,#45461,#45462,#45463,#45464,
#45465,#45466,#45467,#45468,#45469,#45470,#45471,#45472,#45473,#45474,#45475,
#45476,#45477,#45478,#45479,#45480,#45481,#45482,#45483,#45484,#45485,#45486,
#45487,#45488,#45489,#45490,#45491,#45492,#45493,#45494,#45495,#45496,#45497,
#45498,#45499,#45500,#45501,#45502,#45503,#45504,#45505,#45506,#45507,#45508,
#45509,#45510,#45511,#45512,#45513,#45514,#45515,#45516,#45517,#45518,#45519,
#45520,#45521,#45522,#45523,#45524,#45525,#45526,#45527,#45528,#45529,#45530,
#45531,#45532,#45533,#45534,#45535,#45536,#45537,#45538,#45539,#45540,#45541,
#45542,#45543,#45544,#45545,#45546,#45547,#45548,#45549,#45550,#45551,#45552,
#45553,#45554,#45555,#45556,#45557,#45558,#45559,#45560,#45561,#45562,#45563,
#45564,#45565,#45566,#45567,#45568)),.UNSPECIFIED.,.F.,.F.,.F.,(4,4),(4,
1,1,1,1,1,1,1,1,1,1,1,1,1,1,1,1,1,1,1,1,1,1,1,1,1,1,1,1,1,1,1,1,1,1,1,1,
1,1,1,1,1,1,1,1,1,1,1,1,1,1,1,1,1,1,1,1,1,1,1,1,1,1,1,1,1,1,1,1,1,1,1,1,
1,1,1,1,1,1,1,1,1,1,1,1,1,1,1,1,1,1,1,1,1,1,1,1,1,1,1,1,1,1,1,1,1,1,1,1,
1,1,1,1,1,1,1,1,1,1,1,1,1,1,1,1,1,1,1,1,1,1,1,1,1,1,1,1,1,1,1,1,1,1,1,1,
1,1,1,1,1,1,1,1,1,1,1,1,1,1,1,1,1,1,1,1,1,1,1,1,1,1,1,1,1,1,1,1,1,1,1,1,
1,1,1,1,1,1,1,1,1,1,1,1,1,1,1,1,1,1,1,1,1,1,1,1,1,1,1,1,1,1,1,1,1,1,1,1,
1,1,1,1,1,1,1,1,1,1,1,1,1,1,1,1,1,1,1,1,1,1,1,1,1,1,1,1,1,4),(0.,0.0986691610045074),
(11.6147305479242,12.1112366442157,12.6077427405073,13.1042488367988,13.6007549330903,
14.0972610293819,14.5937671256734,15.0902732219649,15.5867793182565,16.083285414548,
16.5797915108395,17.0762976071311,17.5728037034226,18.0693097997141,18.5658158960056,
19.0623219922972,19.5588280885887,20.0553341848802,20.5518402811718,21.0483463774633,
21.5448524737548,22.0413585700464,22.5378646663379,23.0343707626294,23.530876858921,
24.0273829552125,24.523889051504,25.0203951477956,25.5169012440871,26.0134073403786,
26.5099134366701,27.0064195329617,27.5029256292532,27.9994317255447,28.4959378218363,
28.9924439181278,29.4889500144193,29.9854561107109,30.4819622070024,30.9784683032939,
31.4749743995855,31.971480495877,32.4679865921685,32.9644926884601,33.4609987847516,
33.9575048810431,34.4540109773346,34.9505170736262,35.4470231699177,35.9435292662092,
36.4400353625008,36.9365414587923,37.4330475550838,37.9295536513754,38.4260597476669,
38.9225658439584,39.41907194025,39.9155780365415,40.412084132833,40.9085902291246,
41.4050963254161,41.9016024217076,42.3981085179991,42.8946146142907,43.3911207105822,
43.8876268068737,44.3841329031653,44.8806389994568,45.3771450957483,45.8736511920399,
46.3701572883314,46.8666633846229,47.3631694809145,47.859675577206,48.3561816734975,
48.8526877697891,49.3491938660806,49.8456999623721,50.3422060586636,50.8387121549552,
51.3352182512467,51.8317243475382,52.3282304438298,52.8247365401213,53.3212426364128,
53.8177487327044,54.3142548289959,54.8107609252874,55.307267021579,55.8037731178705,
56.300279214162,56.7967853104536,57.2932914067451,57.7897975030366,58.2863035993281,
58.7828096956197,59.2793157919112,59.7758218882027,60.2723279844943,60.7688340807858,
61.2653401770773,61.7618462733689,62.2583523696604,62.7548584659519,63.2513645622435,
63.747870658535,64.2443767548265,64.7408828511181,65.2373889474096,65.7338950437011,
66.2304011399927,66.7269072362842,67.2234133325757,67.7199194288673,68.2164255251588,
68.7129316214503,69.2094377177418,70.2024499103249,71.195462102908,72.188474295491,
73.1814864880741,74.1744986806572,75.1675108732402,76.1605230658233,77.1535352584064,
78.1465474509894,79.1395596435725,80.1325718361555,81.1255840287386,82.1185962213217,
83.1116084139047,83.6081145101963,84.1046206064878,84.6011267027793,85.0976327990709,
85.5941388953624,86.0906449916539,86.5871510879454,87.083657184237,87.5801632805285,
88.07666937682,88.5731754731116,89.0696815694031,89.5661876656946,90.0626937619862,
90.5591998582777,91.0557059545692,91.5522120508608,92.0487181471523,92.5452242434438,
93.0417303397354,93.5382364360269,94.0347425323184,94.5312486286099,95.0277547249015,
95.524260821193,96.0207669174845,96.5172730137761,97.0137791100676,97.5102852063591,
98.0067913026507,98.5032973989422,98.9998034952337,99.4963095915253,99.9928156878168,
100.489321784108,100.9858278804,101.482333976691,101.978840072983,102.475346169274,
102.971852265566,103.468358361857,103.964864458149,104.461370554441,104.957876650732,
105.454382747024,105.950888843315,106.447394939607,106.943901035898,107.44040713219,
107.936913228481,108.433419324773,108.929925421064,109.426431517356,109.922937613647,
110.419443709939,110.91594980623,111.412455902522,111.908961998814,112.405468095105,
112.901974191397,113.398480287688,113.89498638398,114.391492480271,114.887998576563,
115.384504672854,115.881010769146,116.377516865437,116.874022961729,117.37052905802,
117.867035154312,118.363541250603,118.860047346895,119.356553443186,119.853059539478,
120.34956563577,120.846071732061,121.342577828353,121.839083924644,122.335590020936,
122.832096117227,123.328602213519,123.82510830981,124.321614406102,124.818120502393,
125.314626598685,125.811132694976,126.307638791268,126.804144887559,127.300650983851,
127.797157080143,128.293663176434,128.790169272726,129.286675369017,129.783181465309,
130.2796875616,130.776193657892,131.272699754183,131.769205850475,132.265711946766,
132.762218043058,133.258724139349,133.755230235641,134.251736331932,134.748242428224,
135.244748524516,135.741254620807,136.237760717099,136.73426681339,137.230772909682,
137.727279005973,138.223785102265,138.720291198556,139.216797294848,139.713303391139,
140.209809487431,140.706315583722),.UNSPECIFIED.);
#540=CYLINDRICAL_SURFACE('',#26606,4.925);
#541=CYLINDRICAL_SURFACE('',#26608,4.925);
#542=CYLINDRICAL_SURFACE('',#26609,4.925);
#543=CYLINDRICAL_SURFACE('',#26610,4.925);
#544=CYLINDRICAL_SURFACE('',#26611,4.925);
#545=CYLINDRICAL_SURFACE('',#26612,4.925);
#546=CYLINDRICAL_SURFACE('',#26613,4.925);
#547=CYLINDRICAL_SURFACE('',#26614,4.925);
#548=CYLINDRICAL_SURFACE('',#26615,4.925);
#549=CYLINDRICAL_SURFACE('',#26616,4.925);
#550=CYLINDRICAL_SURFACE('',#26617,4.925);
#551=CYLINDRICAL_SURFACE('',#26618,4.925);
#552=CYLINDRICAL_SURFACE('',#26619,4.925);
#553=CYLINDRICAL_SURFACE('',#26620,4.925);
#554=CYLINDRICAL_SURFACE('',#26621,4.925);
#555=CYLINDRICAL_SURFACE('',#26622,4.925);
#556=CYLINDRICAL_SURFACE('',#26623,4.925);
#557=CYLINDRICAL_SURFACE('',#26624,4.925);
#558=CYLINDRICAL_SURFACE('',#26625,4.925);
#559=CYLINDRICAL_SURFACE('',#26626,4.925);
#560=CYLINDRICAL_SURFACE('',#26627,4.925);
#561=CYLINDRICAL_SURFACE('',#26629,4.0705);
#562=CYLINDRICAL_SURFACE('',#26631,4.0705);
#563=CYLINDRICAL_SURFACE('',#26632,4.0705);
#564=CYLINDRICAL_SURFACE('',#26633,4.0705);
#565=CYLINDRICAL_SURFACE('',#26634,4.0705);
#566=CYLINDRICAL_SURFACE('',#26635,4.0705);
#567=CYLINDRICAL_SURFACE('',#26636,4.0705);
#568=CYLINDRICAL_SURFACE('',#26637,4.0705);
#569=CYLINDRICAL_SURFACE('',#26638,4.0705);
#570=CYLINDRICAL_SURFACE('',#26639,4.0705);
#571=CYLINDRICAL_SURFACE('',#26640,4.0705);
#572=CYLINDRICAL_SURFACE('',#26641,4.0705);
#573=CYLINDRICAL_SURFACE('',#26642,4.0705);
#574=CYLINDRICAL_SURFACE('',#26643,4.0705);
#575=CYLINDRICAL_SURFACE('',#26644,4.0705);
#576=CYLINDRICAL_SURFACE('',#26645,4.0705);
#577=CYLINDRICAL_SURFACE('',#26646,4.0705);
#578=CYLINDRICAL_SURFACE('',#26647,4.0705);
#579=CYLINDRICAL_SURFACE('',#26648,4.0705);
#580=CYLINDRICAL_SURFACE('',#26649,4.0705);
#581=CYLINDRICAL_SURFACE('',#26656,4.0705);
#582=CYLINDRICAL_SURFACE('',#26885,4.925);
#583=CYLINDRICAL_SURFACE('',#26889,4.95);
#584=CYLINDRICAL_SURFACE('',#26893,8.);
#674=FACE_BOUND('',#4489,.T.);
#675=FACE_BOUND('',#4491,.T.);
#676=FACE_BOUND('',#4492,.T.);
#677=FACE_BOUND('',#4493,.T.);
#678=FACE_BOUND('',#4494,.T.);
#679=FACE_BOUND('',#4495,.T.);
#680=FACE_BOUND('',#4496,.T.);
#681=FACE_BOUND('',#4497,.T.);
#682=FACE_BOUND('',#4498,.T.);
#683=FACE_BOUND('',#4499,.T.);
#684=FACE_BOUND('',#4500,.T.);
#685=FACE_BOUND('',#4501,.T.);
#686=FACE_BOUND('',#4502,.T.);
#687=FACE_BOUND('',#4503,.T.);
#688=FACE_BOUND('',#4504,.T.);
#689=FACE_BOUND('',#4505,.T.);
#690=FACE_BOUND('',#4506,.T.);
#691=FACE_BOUND('',#4507,.T.);
#692=FACE_BOUND('',#4508,.T.);
#693=FACE_BOUND('',#4509,.T.);
#694=FACE_BOUND('',#4510,.T.);
#695=FACE_BOUND('',#4511,.T.);
#696=FACE_BOUND('',#4512,.T.);
#697=FACE_BOUND('',#4513,.T.);
#698=FACE_BOUND('',#4514,.T.);
#699=FACE_BOUND('',#4515,.T.);
#700=FACE_BOUND('',#4516,.T.);
#701=FACE_BOUND('',#4517,.T.);
#702=FACE_BOUND('',#4518,.T.);
#703=FACE_BOUND('',#4519,.T.);
#704=FACE_BOUND('',#4520,.T.);
#705=FACE_BOUND('',#4521,.T.);
#706=FACE_BOUND('',#4522,.T.);
#707=FACE_BOUND('',#4523,.T.);
#708=FACE_BOUND('',#4524,.T.);
#709=FACE_BOUND('',#4525,.T.);
#710=FACE_BOUND('',#4528,.T.);
#1589=PLANE('',#26650);
#1590=PLANE('',#26652);
#1591=PLANE('',#26657);
#1592=PLANE('',#26658);
#1593=PLANE('',#26660);
#1594=PLANE('',#26661);
#1595=PLANE('',#26663);
#1596=PLANE('',#26664);
#1597=PLANE('',#26666);
#1598=PLANE('',#26667);
#1599=PLANE('',#26669);
#1600=PLANE('',#26670);
#1601=PLANE('',#26672);
#1602=PLANE('',#26673);
#1603=PLANE('',#26675);
#1604=PLANE('',#26676);
#1605=PLANE('',#26678);
#1606=PLANE('',#26679);
#1607=PLANE('',#26681);
#1608=PLANE('',#26682);
#1609=PLANE('',#26684);
#1610=PLANE('',#26685);
#1611=PLANE('',#26687);
#1612=PLANE('',#26688);
#1613=PLANE('',#26690);
#1614=PLANE('',#26691);
#1615=PLANE('',#26693);
#1616=PLANE('',#26694);
#1617=PLANE('',#26696);
#1618=PLANE('',#26697);
#1619=PLANE('',#26699);
#1620=PLANE('',#26700);
#1621=PLANE('',#26702);
#1622=PLANE('',#26703);
#1623=PLANE('',#26705);
#1624=PLANE('',#26706);
#1625=PLANE('',#26708);
#1626=PLANE('',#26709);
#1627=PLANE('',#26711);
#1628=PLANE('',#26712);
#1629=PLANE('',#26714);
#1630=PLANE('',#26715);
#1631=PLANE('',#26717);
#1632=PLANE('',#26718);
#1633=PLANE('',#26720);
#1634=PLANE('',#26721);
#1635=PLANE('',#26723);
#1636=PLANE('',#26724);
#1637=PLANE('',#26726);
#1638=PLANE('',#26727);
#1639=PLANE('',#26729);
#1640=PLANE('',#26730);
#1641=PLANE('',#26732);
#1642=PLANE('',#26733);
#1643=PLANE('',#26735);
#1644=PLANE('',#26736);
#1645=PLANE('',#26738);
#1646=PLANE('',#26739);
#1647=PLANE('',#26741);
#1648=PLANE('',#26742);
#1649=PLANE('',#26744);
#1650=PLANE('',#26745);
#1651=PLANE('',#26747);
#1652=PLANE('',#26748);
#1653=PLANE('',#26750);
#1654=PLANE('',#26751);
#1655=PLANE('',#26753);
#1656=PLANE('',#26754);
#1657=PLANE('',#26756);
#1658=PLANE('',#26757);
#1659=PLANE('',#26759);
#1660=PLANE('',#26760);
#1661=PLANE('',#26763);
#1662=PLANE('',#26764);
#1663=PLANE('',#26767);
#1664=PLANE('',#26768);
#1665=PLANE('',#26770);
#1666=PLANE('',#26771);
#1667=PLANE('',#26773);
#1668=PLANE('',#26774);
#1669=PLANE('',#26776);
#1670=PLANE('',#26777);
#1671=PLANE('',#26779);
#1672=PLANE('',#26780);
#1673=PLANE('',#26782);
#1674=PLANE('',#26783);
#1675=PLANE('',#26785);
#1676=PLANE('',#26786);
#1677=PLANE('',#26788);
#1678=PLANE('',#26789);
#1679=PLANE('',#26791);
#1680=PLANE('',#26792);
#1681=PLANE('',#26794);
#1682=PLANE('',#26795);
#1683=PLANE('',#26797);
#1684=PLANE('',#26798);
#1685=PLANE('',#26800);
#1686=PLANE('',#26801);
#1687=PLANE('',#26803);
#1688=PLANE('',#26804);
#1689=PLANE('',#26806);
#1690=PLANE('',#26807);
#1691=PLANE('',#26809);
#1692=PLANE('',#26810);
#1693=PLANE('',#26812);
#1694=PLANE('',#26813);
#1695=PLANE('',#26815);
#1696=PLANE('',#26816);
#1697=PLANE('',#26818);
#1698=PLANE('',#26819);
#1699=PLANE('',#26821);
#1700=PLANE('',#26822);
#1701=PLANE('',#26824);
#1702=PLANE('',#26825);
#1703=PLANE('',#26827);
#1704=PLANE('',#26828);
#1705=PLANE('',#26830);
#1706=PLANE('',#26831);
#1707=PLANE('',#26833);
#1708=PLANE('',#26834);
#1709=PLANE('',#26836);
#1710=PLANE('',#26837);
#1711=PLANE('',#26839);
#1712=PLANE('',#26840);
#1713=PLANE('',#26842);
#1714=PLANE('',#26843);
#1715=PLANE('',#26845);
#1716=PLANE('',#26846);
#1717=PLANE('',#26848);
#1718=PLANE('',#26849);
#1719=PLANE('',#26851);
#1720=PLANE('',#26852);
#1721=PLANE('',#26854);
#1722=PLANE('',#26855);
#1723=PLANE('',#26857);
#1724=PLANE('',#26858);
#1725=PLANE('',#26860);
#1726=PLANE('',#26861);
#1727=PLANE('',#26863);
#1728=PLANE('',#26864);
#1729=PLANE('',#26866);
#1730=PLANE('',#26867);
#1731=PLANE('',#26869);
#1732=PLANE('',#26870);
#1733=PLANE('',#26872);
#1734=PLANE('',#26873);
#1735=PLANE('',#26875);
#1736=PLANE('',#26876);
#1737=PLANE('',#26877);
#1738=PLANE('',#26878);
#1739=PLANE('',#26879);
#1740=PLANE('',#26880);
#1741=PLANE('',#26881);
#1742=PLANE('',#26882);
#1743=PLANE('',#26891);
#1744=PLANE('',#26897);
#2867=FACE_OUTER_BOUND('',#4286,.T.);
#2868=FACE_OUTER_BOUND('',#4287,.T.);
#2869=FACE_OUTER_BOUND('',#4288,.T.);
#2870=FACE_OUTER_BOUND('',#4289,.T.);
#2871=FACE_OUTER_BOUND('',#4290,.T.);
#2872=FACE_OUTER_BOUND('',#4291,.T.);
#2873=FACE_OUTER_BOUND('',#4292,.T.);
#2874=FACE_OUTER_BOUND('',#4293,.T.);
#2875=FACE_OUTER_BOUND('',#4294,.T.);
#2876=FACE_OUTER_BOUND('',#4295,.T.);
#2877=FACE_OUTER_BOUND('',#4296,.T.);
#2878=FACE_OUTER_BOUND('',#4297,.T.);
#2879=FACE_OUTER_BOUND('',#4298,.T.);
#2880=FACE_OUTER_BOUND('',#4299,.T.);
#2881=FACE_OUTER_BOUND('',#4300,.T.);
#2882=FACE_OUTER_BOUND('',#4301,.T.);
#2883=FACE_OUTER_BOUND('',#4302,.T.);
#2884=FACE_OUTER_BOUND('',#4303,.T.);
#2885=FACE_OUTER_BOUND('',#4304,.T.);
#2886=FACE_OUTER_BOUND('',#4305,.T.);
#2887=FACE_OUTER_BOUND('',#4306,.T.);
#2888=FACE_OUTER_BOUND('',#4307,.T.);
#2889=FACE_OUTER_BOUND('',#4308,.T.);
#2890=FACE_OUTER_BOUND('',#4309,.T.);
#2891=FACE_OUTER_BOUND('',#4310,.T.);
#2892=FACE_OUTER_BOUND('',#4311,.T.);
#2893=FACE_OUTER_BOUND('',#4312,.T.);
#2894=FACE_OUTER_BOUND('',#4313,.T.);
#2895=FACE_OUTER_BOUND('',#4314,.T.);
#2896=FACE_OUTER_BOUND('',#4315,.T.);
#2897=FACE_OUTER_BOUND('',#4316,.T.);
#2898=FACE_OUTER_BOUND('',#4317,.T.);
#2899=FACE_OUTER_BOUND('',#4318,.T.);
#2900=FACE_OUTER_BOUND('',#4319,.T.);
#2901=FACE_OUTER_BOUND('',#4320,.T.);
#2902=FACE_OUTER_BOUND('',#4321,.T.);
#2903=FACE_OUTER_BOUND('',#4322,.T.);
#2904=FACE_OUTER_BOUND('',#4323,.T.);
#2905=FACE_OUTER_BOUND('',#4324,.T.);
#2906=FACE_OUTER_BOUND('',#4325,.T.);
#2907=FACE_OUTER_BOUND('',#4326,.T.);
#2908=FACE_OUTER_BOUND('',#4327,.T.);
#2909=FACE_OUTER_BOUND('',#4328,.T.);
#2910=FACE_OUTER_BOUND('',#4329,.T.);
#2911=FACE_OUTER_BOUND('',#4330,.T.);
#2912=FACE_OUTER_BOUND('',#4331,.T.);
#2913=FACE_OUTER_BOUND('',#4332,.T.);
#2914=FACE_OUTER_BOUND('',#4333,.T.);
#2915=FACE_OUTER_BOUND('',#4334,.T.);
#2916=FACE_OUTER_BOUND('',#4335,.T.);
#2917=FACE_OUTER_BOUND('',#4336,.T.);
#2918=FACE_OUTER_BOUND('',#4337,.T.);
#2919=FACE_OUTER_BOUND('',#4338,.T.);
#2920=FACE_OUTER_BOUND('',#4339,.T.);
#2921=FACE_OUTER_BOUND('',#4340,.T.);
#2922=FACE_OUTER_BOUND('',#4341,.T.);
#2923=FACE_OUTER_BOUND('',#4342,.T.);
#2924=FACE_OUTER_BOUND('',#4343,.T.);
#2925=FACE_OUTER_BOUND('',#4344,.T.);
#2926=FACE_OUTER_BOUND('',#4345,.T.);
#2927=FACE_OUTER_BOUND('',#4346,.T.);
#2928=FACE_OUTER_BOUND('',#4347,.T.);
#2929=FACE_OUTER_BOUND('',#4348,.T.);
#2930=FACE_OUTER_BOUND('',#4349,.T.);
#2931=FACE_OUTER_BOUND('',#4350,.T.);
#2932=FACE_OUTER_BOUND('',#4351,.T.);
#2933=FACE_OUTER_BOUND('',#4352,.T.);
#2934=FACE_OUTER_BOUND('',#4353,.T.);
#2935=FACE_OUTER_BOUND('',#4354,.T.);
#2936=FACE_OUTER_BOUND('',#4355,.T.);
#2937=FACE_OUTER_BOUND('',#4356,.T.);
#2938=FACE_OUTER_BOUND('',#4357,.T.);
#2939=FACE_OUTER_BOUND('',#4358,.T.);
#2940=FACE_OUTER_BOUND('',#4359,.T.);
#2941=FACE_OUTER_BOUND('',#4360,.T.);
#2942=FACE_OUTER_BOUND('',#4361,.T.);
#2943=FACE_OUTER_BOUND('',#4362,.T.);
#2944=FACE_OUTER_BOUND('',#4363,.T.);
#2945=FACE_OUTER_BOUND('',#4364,.T.);
#2946=FACE_OUTER_BOUND('',#4365,.T.);
#2947=FACE_OUTER_BOUND('',#4366,.T.);
#2948=FACE_OUTER_BOUND('',#4367,.T.);
#2949=FACE_OUTER_BOUND('',#4368,.T.);
#2950=FACE_OUTER_BOUND('',#4369,.T.);
#2951=FACE_OUTER_BOUND('',#4370,.T.);
#2952=FACE_OUTER_BOUND('',#4371,.T.);
#2953=FACE_OUTER_BOUND('',#4372,.T.);
#2954=FACE_OUTER_BOUND('',#4373,.T.);
#2955=FACE_OUTER_BOUND('',#4374,.T.);
#2956=FACE_OUTER_BOUND('',#4375,.T.);
#2957=FACE_OUTER_BOUND('',#4376,.T.);
#2958=FACE_OUTER_BOUND('',#4377,.T.);
#2959=FACE_OUTER_BOUND('',#4378,.T.);
#2960=FACE_OUTER_BOUND('',#4379,.T.);
#2961=FACE_OUTER_BOUND('',#4380,.T.);
#2962=FACE_OUTER_BOUND('',#4381,.T.);
#2963=FACE_OUTER_BOUND('',#4382,.T.);
#2964=FACE_OUTER_BOUND('',#4383,.T.);
#2965=FACE_OUTER_BOUND('',#4384,.T.);
#2966=FACE_OUTER_BOUND('',#4385,.T.);
#2967=FACE_OUTER_BOUND('',#4386,.T.);
#2968=FACE_OUTER_BOUND('',#4387,.T.);
#2969=FACE_OUTER_BOUND('',#4388,.T.);
#2970=FACE_OUTER_BOUND('',#4389,.T.);
#2971=FACE_OUTER_BOUND('',#4390,.T.);
#2972=FACE_OUTER_BOUND('',#4391,.T.);
#2973=FACE_OUTER_BOUND('',#4392,.T.);
#2974=FACE_OUTER_BOUND('',#4393,.T.);
#2975=FACE_OUTER_BOUND('',#4394,.T.);
#2976=FACE_OUTER_BOUND('',#4395,.T.);
#2977=FACE_OUTER_BOUND('',#4396,.T.);
#2978=FACE_OUTER_BOUND('',#4397,.T.);
#2979=FACE_OUTER_BOUND('',#4398,.T.);
#2980=FACE_OUTER_BOUND('',#4399,.T.);
#2981=FACE_OUTER_BOUND('',#4400,.T.);
#2982=FACE_OUTER_BOUND('',#4401,.T.);
#2983=FACE_OUTER_BOUND('',#4402,.T.);
#2984=FACE_OUTER_BOUND('',#4403,.T.);
#2985=FACE_OUTER_BOUND('',#4404,.T.);
#2986=FACE_OUTER_BOUND('',#4405,.T.);
#2987=FACE_OUTER_BOUND('',#4406,.T.);
#2988=FACE_OUTER_BOUND('',#4407,.T.);
#2989=FACE_OUTER_BOUND('',#4408,.T.);
#2990=FACE_OUTER_BOUND('',#4409,.T.);
#2991=FACE_OUTER_BOUND('',#4410,.T.);
#2992=FACE_OUTER_BOUND('',#4411,.T.);
#2993=FACE_OUTER_BOUND('',#4412,.T.);
#2994=FACE_OUTER_BOUND('',#4413,.T.);
#2995=FACE_OUTER_BOUND('',#4414,.T.);
#2996=FACE_OUTER_BOUND('',#4415,.T.);
#2997=FACE_OUTER_BOUND('',#4416,.T.);
#2998=FACE_OUTER_BOUND('',#4417,.T.);
#2999=FACE_OUTER_BOUND('',#4418,.T.);
#3000=FACE_OUTER_BOUND('',#4419,.T.);
#3001=FACE_OUTER_BOUND('',#4420,.T.);
#3002=FACE_OUTER_BOUND('',#4421,.T.);
#3003=FACE_OUTER_BOUND('',#4422,.T.);
#3004=FACE_OUTER_BOUND('',#4423,.T.);
#3005=FACE_OUTER_BOUND('',#4424,.T.);
#3006=FACE_OUTER_BOUND('',#4425,.T.);
#3007=FACE_OUTER_BOUND('',#4426,.T.);
#3008=FACE_OUTER_BOUND('',#4427,.T.);
#3009=FACE_OUTER_BOUND('',#4428,.T.);
#3010=FACE_OUTER_BOUND('',#4429,.T.);
#3011=FACE_OUTER_BOUND('',#4430,.T.);
#3012=FACE_OUTER_BOUND('',#4431,.T.);
#3013=FACE_OUTER_BOUND('',#4432,.T.);
#3014=FACE_OUTER_BOUND('',#4433,.T.);
#3015=FACE_OUTER_BOUND('',#4434,.T.);
#3016=FACE_OUTER_BOUND('',#4435,.T.);
#3017=FACE_OUTER_BOUND('',#4436,.T.);
#3018=FACE_OUTER_BOUND('',#4437,.T.);
#3019=FACE_OUTER_BOUND('',#4438,.T.);
#3020=FACE_OUTER_BOUND('',#4439,.T.);
#3021=FACE_OUTER_BOUND('',#4440,.T.);
#3022=FACE_OUTER_BOUND('',#4441,.T.);
#3023=FACE_OUTER_BOUND('',#4442,.T.);
#3024=FACE_OUTER_BOUND('',#4443,.T.);
#3025=FACE_OUTER_BOUND('',#4444,.T.);
#3026=FACE_OUTER_BOUND('',#4445,.T.);
#3027=FACE_OUTER_BOUND('',#4446,.T.);
#3028=FACE_OUTER_BOUND('',#4447,.T.);
#3029=FACE_OUTER_BOUND('',#4448,.T.);
#3030=FACE_OUTER_BOUND('',#4449,.T.);
#3031=FACE_OUTER_BOUND('',#4450,.T.);
#3032=FACE_OUTER_BOUND('',#4451,.T.);
#3033=FACE_OUTER_BOUND('',#4452,.T.);
#3034=FACE_OUTER_BOUND('',#4453,.T.);
#3035=FACE_OUTER_BOUND('',#4454,.T.);
#3036=FACE_OUTER_BOUND('',#4455,.T.);
#3037=FACE_OUTER_BOUND('',#4456,.T.);
#3038=FACE_OUTER_BOUND('',#4457,.T.);
#3039=FACE_OUTER_BOUND('',#4458,.T.);
#3040=FACE_OUTER_BOUND('',#4459,.T.);
#3041=FACE_OUTER_BOUND('',#4460,.T.);
#3042=FACE_OUTER_BOUND('',#4461,.T.);
#3043=FACE_OUTER_BOUND('',#4462,.T.);
#3044=FACE_OUTER_BOUND('',#4463,.T.);
#3045=FACE_OUTER_BOUND('',#4464,.T.);
#3046=FACE_OUTER_BOUND('',#4465,.T.);
#3047=FACE_OUTER_BOUND('',#4466,.T.);
#3048=FACE_OUTER_BOUND('',#4467,.T.);
#3049=FACE_OUTER_BOUND('',#4468,.T.);
#3050=FACE_OUTER_BOUND('',#4469,.T.);
#3051=FACE_OUTER_BOUND('',#4470,.T.);
#3052=FACE_OUTER_BOUND('',#4471,.T.);
#3053=FACE_OUTER_BOUND('',#4472,.T.);
#3054=FACE_OUTER_BOUND('',#4473,.T.);
#3055=FACE_OUTER_BOUND('',#4474,.T.);
#3056=FACE_OUTER_BOUND('',#4475,.T.);
#3057=FACE_OUTER_BOUND('',#4476,.T.);
#3058=FACE_OUTER_BOUND('',#4477,.T.);
#3059=FACE_OUTER_BOUND('',#4478,.T.);
#3060=FACE_OUTER_BOUND('',#4479,.T.);
#3061=FACE_OUTER_BOUND('',#4480,.T.);
#3062=FACE_OUTER_BOUND('',#4481,.T.);
#3063=FACE_OUTER_BOUND('',#4482,.T.);
#3064=FACE_OUTER_BOUND('',#4483,.T.);
#3065=FACE_OUTER_BOUND('',#4484,.T.);
#3066=FACE_OUTER_BOUND('',#4485,.T.);
#3067=FACE_OUTER_BOUND('',#4486,.T.);
#3068=FACE_OUTER_BOUND('',#4487,.T.);
#3069=FACE_OUTER_BOUND('',#4488,.T.);
#3070=FACE_OUTER_BOUND('',#4490,.T.);
#3071=FACE_OUTER_BOUND('',#4526,.T.);
#3072=FACE_OUTER_BOUND('',#4527,.T.);
#4286=EDGE_LOOP('',(#22548,#22549,#22550,#22551));
#4287=EDGE_LOOP('',(#22552,#22553,#22554,#22555));
#4288=EDGE_LOOP('',(#22556,#22557,#22558,#22559));
#4289=EDGE_LOOP('',(#22560,#22561,#22562,#22563));
#4290=EDGE_LOOP('',(#22564,#22565,#22566,#22567));
#4291=EDGE_LOOP('',(#22568,#22569,#22570,#22571));
#4292=EDGE_LOOP('',(#22572,#22573,#22574,#22575));
#4293=EDGE_LOOP('',(#22576,#22577,#22578,#22579));
#4294=EDGE_LOOP('',(#22580,#22581,#22582,#22583));
#4295=EDGE_LOOP('',(#22584,#22585,#22586,#22587));
#4296=EDGE_LOOP('',(#22588,#22589,#22590,#22591));
#4297=EDGE_LOOP('',(#22592,#22593,#22594,#22595));
#4298=EDGE_LOOP('',(#22596,#22597,#22598,#22599));
#4299=EDGE_LOOP('',(#22600,#22601,#22602,#22603));
#4300=EDGE_LOOP('',(#22604,#22605,#22606,#22607));
#4301=EDGE_LOOP('',(#22608,#22609,#22610,#22611));
#4302=EDGE_LOOP('',(#22612,#22613,#22614,#22615));
#4303=EDGE_LOOP('',(#22616,#22617,#22618,#22619));
#4304=EDGE_LOOP('',(#22620,#22621,#22622,#22623));
#4305=EDGE_LOOP('',(#22624,#22625,#22626,#22627));
#4306=EDGE_LOOP('',(#22628,#22629,#22630,#22631,#22632));
#4307=EDGE_LOOP('',(#22633,#22634,#22635,#22636));
#4308=EDGE_LOOP('',(#22637,#22638,#22639,#22640));
#4309=EDGE_LOOP('',(#22641,#22642,#22643,#22644));
#4310=EDGE_LOOP('',(#22645,#22646,#22647,#22648));
#4311=EDGE_LOOP('',(#22649,#22650,#22651,#22652));
#4312=EDGE_LOOP('',(#22653,#22654,#22655,#22656));
#4313=EDGE_LOOP('',(#22657,#22658,#22659,#22660));
#4314=EDGE_LOOP('',(#22661,#22662,#22663,#22664));
#4315=EDGE_LOOP('',(#22665,#22666,#22667,#22668));
#4316=EDGE_LOOP('',(#22669,#22670,#22671,#22672));
#4317=EDGE_LOOP('',(#22673,#22674,#22675,#22676));
#4318=EDGE_LOOP('',(#22677,#22678,#22679,#22680));
#4319=EDGE_LOOP('',(#22681,#22682,#22683,#22684));
#4320=EDGE_LOOP('',(#22685,#22686,#22687,#22688));
#4321=EDGE_LOOP('',(#22689,#22690,#22691,#22692));
#4322=EDGE_LOOP('',(#22693,#22694,#22695,#22696));
#4323=EDGE_LOOP('',(#22697,#22698,#22699,#22700));
#4324=EDGE_LOOP('',(#22701,#22702,#22703,#22704));
#4325=EDGE_LOOP('',(#22705,#22706,#22707,#22708));
#4326=EDGE_LOOP('',(#22709,#22710,#22711,#22712));
#4327=EDGE_LOOP('',(#22713,#22714,#22715,#22716));
#4328=EDGE_LOOP('',(#22717,#22718,#22719,#22720,#22721,#22722,#22723,#22724,
#22725,#22726,#22727,#22728,#22729,#22730,#22731,#22732,#22733,#22734,#22735,
#22736,#22737,#22738,#22739,#22740,#22741,#22742,#22743,#22744,#22745,#22746,
#22747,#22748,#22749,#22750,#22751,#22752,#22753,#22754,#22755,#22756,#22757,
#22758,#22759,#22760,#22761));
#4329=EDGE_LOOP('',(#22762,#22763,#22764,#22765,#22766));
#4330=EDGE_LOOP('',(#22767,#22768,#22769,#22770));
#4331=EDGE_LOOP('',(#22771,#22772,#22773,#22774,#22775,#22776,#22777,#22778,
#22779,#22780,#22781,#22782,#22783,#22784,#22785,#22786,#22787,#22788,#22789,
#22790,#22791,#22792,#22793,#22794,#22795,#22796,#22797,#22798,#22799,#22800,
#22801,#22802,#22803,#22804,#22805,#22806,#22807,#22808,#22809,#22810,#22811,
#22812,#22813,#22814));
#4332=EDGE_LOOP('',(#22815,#22816,#22817,#22818));
#4333=EDGE_LOOP('',(#22819,#22820,#22821));
#4334=EDGE_LOOP('',(#22822,#22823,#22824,#22825));
#4335=EDGE_LOOP('',(#22826,#22827,#22828));
#4336=EDGE_LOOP('',(#22829,#22830,#22831,#22832));
#4337=EDGE_LOOP('',(#22833,#22834,#22835));
#4338=EDGE_LOOP('',(#22836,#22837,#22838,#22839));
#4339=EDGE_LOOP('',(#22840,#22841,#22842));
#4340=EDGE_LOOP('',(#22843,#22844,#22845,#22846));
#4341=EDGE_LOOP('',(#22847,#22848,#22849));
#4342=EDGE_LOOP('',(#22850,#22851,#22852,#22853));
#4343=EDGE_LOOP('',(#22854,#22855,#22856));
#4344=EDGE_LOOP('',(#22857,#22858,#22859,#22860));
#4345=EDGE_LOOP('',(#22861,#22862,#22863));
#4346=EDGE_LOOP('',(#22864,#22865,#22866,#22867));
#4347=EDGE_LOOP('',(#22868,#22869,#22870));
#4348=EDGE_LOOP('',(#22871,#22872,#22873,#22874));
#4349=EDGE_LOOP('',(#22875,#22876,#22877));
#4350=EDGE_LOOP('',(#22878,#22879,#22880,#22881));
#4351=EDGE_LOOP('',(#22882,#22883,#22884));
#4352=EDGE_LOOP('',(#22885,#22886,#22887,#22888));
#4353=EDGE_LOOP('',(#22889,#22890,#22891));
#4354=EDGE_LOOP('',(#22892,#22893,#22894,#22895));
#4355=EDGE_LOOP('',(#22896,#22897,#22898));
#4356=EDGE_LOOP('',(#22899,#22900,#22901,#22902));
#4357=EDGE_LOOP('',(#22903,#22904,#22905));
#4358=EDGE_LOOP('',(#22906,#22907,#22908,#22909));
#4359=EDGE_LOOP('',(#22910,#22911,#22912));
#4360=EDGE_LOOP('',(#22913,#22914,#22915,#22916));
#4361=EDGE_LOOP('',(#22917,#22918,#22919));
#4362=EDGE_LOOP('',(#22920,#22921,#22922,#22923));
#4363=EDGE_LOOP('',(#22924,#22925,#22926));
#4364=EDGE_LOOP('',(#22927,#22928,#22929,#22930));
#4365=EDGE_LOOP('',(#22931,#22932,#22933));
#4366=EDGE_LOOP('',(#22934,#22935,#22936,#22937));
#4367=EDGE_LOOP('',(#22938,#22939,#22940));
#4368=EDGE_LOOP('',(#22941,#22942,#22943,#22944));
#4369=EDGE_LOOP('',(#22945,#22946,#22947));
#4370=EDGE_LOOP('',(#22948,#22949,#22950,#22951));
#4371=EDGE_LOOP('',(#22952,#22953,#22954));
#4372=EDGE_LOOP('',(#22955,#22956,#22957,#22958));
#4373=EDGE_LOOP('',(#22959,#22960,#22961));
#4374=EDGE_LOOP('',(#22962,#22963,#22964,#22965));
#4375=EDGE_LOOP('',(#22966,#22967,#22968));
#4376=EDGE_LOOP('',(#22969,#22970,#22971,#22972));
#4377=EDGE_LOOP('',(#22973,#22974,#22975));
#4378=EDGE_LOOP('',(#22976,#22977,#22978,#22979));
#4379=EDGE_LOOP('',(#22980,#22981,#22982));
#4380=EDGE_LOOP('',(#22983,#22984,#22985,#22986));
#4381=EDGE_LOOP('',(#22987,#22988,#22989));
#4382=EDGE_LOOP('',(#22990,#22991,#22992,#22993));
#4383=EDGE_LOOP('',(#22994,#22995,#22996));
#4384=EDGE_LOOP('',(#22997,#22998,#22999,#23000));
#4385=EDGE_LOOP('',(#23001,#23002,#23003));
#4386=EDGE_LOOP('',(#23004,#23005,#23006,#23007));
#4387=EDGE_LOOP('',(#23008,#23009,#23010));
#4388=EDGE_LOOP('',(#23011,#23012,#23013,#23014));
#4389=EDGE_LOOP('',(#23015,#23016,#23017));
#4390=EDGE_LOOP('',(#23018,#23019,#23020,#23021));
#4391=EDGE_LOOP('',(#23022,#23023,#23024));
#4392=EDGE_LOOP('',(#23025,#23026,#23027,#23028));
#4393=EDGE_LOOP('',(#23029,#23030,#23031));
#4394=EDGE_LOOP('',(#23032,#23033,#23034,#23035));
#4395=EDGE_LOOP('',(#23036,#23037,#23038));
#4396=EDGE_LOOP('',(#23039,#23040,#23041,#23042));
#4397=EDGE_LOOP('',(#23043,#23044,#23045));
#4398=EDGE_LOOP('',(#23046,#23047,#23048,#23049));
#4399=EDGE_LOOP('',(#23050,#23051,#23052));
#4400=EDGE_LOOP('',(#23053,#23054,#23055,#23056));
#4401=EDGE_LOOP('',(#23057,#23058,#23059,#23060));
#4402=EDGE_LOOP('',(#23061,#23062,#23063,#23064));
#4403=EDGE_LOOP('',(#23065,#23066,#23067,#23068));
#4404=EDGE_LOOP('',(#23069,#23070,#23071,#23072));
#4405=EDGE_LOOP('',(#23073,#23074,#23075));
#4406=EDGE_LOOP('',(#23076,#23077,#23078,#23079));
#4407=EDGE_LOOP('',(#23080,#23081,#23082));
#4408=EDGE_LOOP('',(#23083,#23084,#23085,#23086));
#4409=EDGE_LOOP('',(#23087,#23088,#23089));
#4410=EDGE_LOOP('',(#23090,#23091,#23092,#23093));
#4411=EDGE_LOOP('',(#23094,#23095,#23096));
#4412=EDGE_LOOP('',(#23097,#23098,#23099,#23100));
#4413=EDGE_LOOP('',(#23101,#23102,#23103));
#4414=EDGE_LOOP('',(#23104,#23105,#23106,#23107));
#4415=EDGE_LOOP('',(#23108,#23109,#23110));
#4416=EDGE_LOOP('',(#23111,#23112,#23113,#23114));
#4417=EDGE_LOOP('',(#23115,#23116,#23117));
#4418=EDGE_LOOP('',(#23118,#23119,#23120,#23121));
#4419=EDGE_LOOP('',(#23122,#23123,#23124));
#4420=EDGE_LOOP('',(#23125,#23126,#23127,#23128));
#4421=EDGE_LOOP('',(#23129,#23130,#23131));
#4422=EDGE_LOOP('',(#23132,#23133,#23134,#23135));
#4423=EDGE_LOOP('',(#23136,#23137,#23138));
#4424=EDGE_LOOP('',(#23139,#23140,#23141,#23142));
#4425=EDGE_LOOP('',(#23143,#23144,#23145));
#4426=EDGE_LOOP('',(#23146,#23147,#23148,#23149));
#4427=EDGE_LOOP('',(#23150,#23151,#23152));
#4428=EDGE_LOOP('',(#23153,#23154,#23155,#23156));
#4429=EDGE_LOOP('',(#23157,#23158,#23159));
#4430=EDGE_LOOP('',(#23160,#23161,#23162,#23163));
#4431=EDGE_LOOP('',(#23164,#23165,#23166));
#4432=EDGE_LOOP('',(#23167,#23168,#23169,#23170));
#4433=EDGE_LOOP('',(#23171,#23172,#23173));
#4434=EDGE_LOOP('',(#23174,#23175,#23176,#23177));
#4435=EDGE_LOOP('',(#23178,#23179,#23180));
#4436=EDGE_LOOP('',(#23181,#23182,#23183,#23184));
#4437=EDGE_LOOP('',(#23185,#23186,#23187));
#4438=EDGE_LOOP('',(#23188,#23189,#23190,#23191));
#4439=EDGE_LOOP('',(#23192,#23193,#23194));
#4440=EDGE_LOOP('',(#23195,#23196,#23197,#23198));
#4441=EDGE_LOOP('',(#23199,#23200,#23201));
#4442=EDGE_LOOP('',(#23202,#23203,#23204,#23205));
#4443=EDGE_LOOP('',(#23206,#23207,#23208));
#4444=EDGE_LOOP('',(#23209,#23210,#23211,#23212));
#4445=EDGE_LOOP('',(#23213,#23214,#23215));
#4446=EDGE_LOOP('',(#23216,#23217,#23218,#23219));
#4447=EDGE_LOOP('',(#23220,#23221,#23222));
#4448=EDGE_LOOP('',(#23223,#23224,#23225,#23226));
#4449=EDGE_LOOP('',(#23227,#23228,#23229));
#4450=EDGE_LOOP('',(#23230,#23231,#23232,#23233));
#4451=EDGE_LOOP('',(#23234,#23235,#23236));
#4452=EDGE_LOOP('',(#23237,#23238,#23239,#23240));
#4453=EDGE_LOOP('',(#23241,#23242,#23243));
#4454=EDGE_LOOP('',(#23244,#23245,#23246,#23247));
#4455=EDGE_LOOP('',(#23248,#23249,#23250));
#4456=EDGE_LOOP('',(#23251,#23252,#23253,#23254));
#4457=EDGE_LOOP('',(#23255,#23256,#23257));
#4458=EDGE_LOOP('',(#23258,#23259,#23260,#23261));
#4459=EDGE_LOOP('',(#23262,#23263,#23264));
#4460=EDGE_LOOP('',(#23265,#23266,#23267,#23268));
#4461=EDGE_LOOP('',(#23269,#23270,#23271));
#4462=EDGE_LOOP('',(#23272,#23273,#23274,#23275));
#4463=EDGE_LOOP('',(#23276,#23277,#23278));
#4464=EDGE_LOOP('',(#23279,#23280,#23281,#23282));
#4465=EDGE_LOOP('',(#23283,#23284,#23285));
#4466=EDGE_LOOP('',(#23286,#23287,#23288,#23289));
#4467=EDGE_LOOP('',(#23290,#23291,#23292));
#4468=EDGE_LOOP('',(#23293,#23294,#23295,#23296));
#4469=EDGE_LOOP('',(#23297,#23298,#23299));
#4470=EDGE_LOOP('',(#23300,#23301,#23302,#23303));
#4471=EDGE_LOOP('',(#23304,#23305,#23306));
#4472=EDGE_LOOP('',(#23307,#23308,#23309,#23310));
#4473=EDGE_LOOP('',(#23311,#23312,#23313));
#4474=EDGE_LOOP('',(#23314,#23315,#23316,#23317));
#4475=EDGE_LOOP('',(#23318,#23319,#23320));
#4476=EDGE_LOOP('',(#23321,#23322,#23323,#23324));
#4477=EDGE_LOOP('',(#23325,#23326,#23327,#23328));
#4478=EDGE_LOOP('',(#23329,#23330,#23331,#23332));
#4479=EDGE_LOOP('',(#23333,#23334,#23335,#23336));
#4480=EDGE_LOOP('',(#23337,#23338,#23339,#23340));
#4481=EDGE_LOOP('',(#23341,#23342,#23343,#23344));
#4482=EDGE_LOOP('',(#23345,#23346,#23347,#23348,#23349,#23350));
#4483=EDGE_LOOP('',(#23351));
#4484=EDGE_LOOP('',(#23352,#23353,#23354,#23355,#23356,#23357));
#4485=EDGE_LOOP('',(#23358,#23359,#23360));
#4486=EDGE_LOOP('',(#23361,#23362,#23363,#23364,#23365,#23366));
#4487=EDGE_LOOP('',(#23367,#23368,#23369,#23370));
#4488=EDGE_LOOP('',(#23371));
#4489=EDGE_LOOP('',(#23372));
#4490=EDGE_LOOP('',(#23373,#23374,#23375,#23376,#23377,#23378,#23379,#23380,
#23381,#23382,#23383,#23384));
#4491=EDGE_LOOP('',(#23385,#23386,#23387,#23388));
#4492=EDGE_LOOP('',(#23389,#23390,#23391,#23392));
#4493=EDGE_LOOP('',(#23393,#23394,#23395,#23396));
#4494=EDGE_LOOP('',(#23397,#23398,#23399,#23400));
#4495=EDGE_LOOP('',(#23401,#23402,#23403,#23404));
#4496=EDGE_LOOP('',(#23405,#23406,#23407,#23408));
#4497=EDGE_LOOP('',(#23409,#23410,#23411,#23412));
#4498=EDGE_LOOP('',(#23413,#23414,#23415,#23416));
#4499=EDGE_LOOP('',(#23417,#23418,#23419,#23420));
#4500=EDGE_LOOP('',(#23421,#23422,#23423,#23424));
#4501=EDGE_LOOP('',(#23425,#23426,#23427,#23428));
#4502=EDGE_LOOP('',(#23429,#23430,#23431,#23432));
#4503=EDGE_LOOP('',(#23433,#23434,#23435,#23436));
#4504=EDGE_LOOP('',(#23437,#23438,#23439,#23440));
#4505=EDGE_LOOP('',(#23441,#23442,#23443,#23444));
#4506=EDGE_LOOP('',(#23445,#23446,#23447,#23448));
#4507=EDGE_LOOP('',(#23449,#23450,#23451,#23452));
#4508=EDGE_LOOP('',(#23453,#23454,#23455,#23456));
#4509=EDGE_LOOP('',(#23457,#23458,#23459,#23460));
#4510=EDGE_LOOP('',(#23461,#23462,#23463,#23464));
#4511=EDGE_LOOP('',(#23465,#23466,#23467,#23468));
#4512=EDGE_LOOP('',(#23469,#23470,#23471,#23472));
#4513=EDGE_LOOP('',(#23473,#23474,#23475,#23476));
#4514=EDGE_LOOP('',(#23477,#23478,#23479,#23480));
#4515=EDGE_LOOP('',(#23481,#23482,#23483,#23484));
#4516=EDGE_LOOP('',(#23485,#23486,#23487,#23488));
#4517=EDGE_LOOP('',(#23489,#23490,#23491,#23492));
#4518=EDGE_LOOP('',(#23493,#23494,#23495,#23496));
#4519=EDGE_LOOP('',(#23497,#23498,#23499,#23500));
#4520=EDGE_LOOP('',(#23501,#23502,#23503,#23504));
#4521=EDGE_LOOP('',(#23505,#23506,#23507,#23508));
#4522=EDGE_LOOP('',(#23509,#23510,#23511,#23512));
#4523=EDGE_LOOP('',(#23513,#23514,#23515,#23516));
#4524=EDGE_LOOP('',(#23517,#23518,#23519,#23520));
#4525=EDGE_LOOP('',(#23521,#23522,#23523,#23524));
#4526=EDGE_LOOP('',(#23525,#23526,#23527,#23528));
#4527=EDGE_LOOP('',(#23529));
#4528=EDGE_LOOP('',(#23530,#23531,#23532,#23533,#23534,#23535));
#7083=LINE('',#40733,#9952);
#7084=LINE('',#40766,#9953);
#7085=LINE('',#40850,#9954);
#7086=LINE('',#40940,#9955);
#7087=LINE('',#41030,#9956);
#7088=LINE('',#41114,#9957);
#7089=LINE('',#41204,#9958);
#7090=LINE('',#41294,#9959);
#7091=LINE('',#41378,#9960);
#7092=LINE('',#41468,#9961);
#7093=LINE('',#41546,#9962);
#7094=LINE('',#41594,#9963);
#7095=LINE('',#41648,#9964);
#7096=LINE('',#41732,#9965);
#7097=LINE('',#41816,#9966);
#7098=LINE('',#41906,#9967);
#7099=LINE('',#41996,#9968);
#7100=LINE('',#42080,#9969);
#7101=LINE('',#42170,#9970);
#7102=LINE('',#42260,#9971);
#7103=LINE('',#42344,#9972);
#7104=LINE('',#42430,#9973);
#7105=LINE('',#42456,#9974);
#7106=LINE('',#42493,#9975);
#7107=LINE('',#42530,#9976);
#7108=LINE('',#42568,#9977);
#7109=LINE('',#42605,#9978);
#7110=LINE('',#42642,#9979);
#7111=LINE('',#42680,#9980);
#7112=LINE('',#42717,#9981);
#7113=LINE('',#42754,#9982);
#7114=LINE('',#42785,#9983);
#7115=LINE('',#42809,#9984);
#7116=LINE('',#42837,#9985);
#7117=LINE('',#42874,#9986);
#7118=LINE('',#42911,#9987);
#7119=LINE('',#42948,#9988);
#7120=LINE('',#42986,#9989);
#7121=LINE('',#43023,#9990);
#7122=LINE('',#43060,#9991);
#7123=LINE('',#43098,#9992);
#7124=LINE('',#45572,#9993);
#7125=LINE('',#45574,#9994);
#7126=LINE('',#45576,#9995);
#7127=LINE('',#45577,#9996);
#7128=LINE('',#45581,#9997);
#7129=LINE('',#45584,#9998);
#7130=LINE('',#45585,#9999);
#7131=LINE('',#45591,#10000);
#7132=LINE('',#45593,#10001);
#7133=LINE('',#45595,#10002);
#7134=LINE('',#45596,#10003);
#7135=LINE('',#45600,#10004);
#7136=LINE('',#45603,#10005);
#7137=LINE('',#45604,#10006);
#7138=LINE('',#45610,#10007);
#7139=LINE('',#45612,#10008);
#7140=LINE('',#45614,#10009);
#7141=LINE('',#45615,#10010);
#7142=LINE('',#45619,#10011);
#7143=LINE('',#45622,#10012);
#7144=LINE('',#45623,#10013);
#7145=LINE('',#45629,#10014);
#7146=LINE('',#45631,#10015);
#7147=LINE('',#45633,#10016);
#7148=LINE('',#45634,#10017);
#7149=LINE('',#45638,#10018);
#7150=LINE('',#45641,#10019);
#7151=LINE('',#45642,#10020);
#7152=LINE('',#45648,#10021);
#7153=LINE('',#45650,#10022);
#7154=LINE('',#45652,#10023);
#7155=LINE('',#45653,#10024);
#7156=LINE('',#45657,#10025);
#7157=LINE('',#45660,#10026);
#7158=LINE('',#45661,#10027);
#7159=LINE('',#45667,#10028);
#7160=LINE('',#45669,#10029);
#7161=LINE('',#45671,#10030);
#7162=LINE('',#45672,#10031);
#7163=LINE('',#45676,#10032);
#7164=LINE('',#45679,#10033);
#7165=LINE('',#45680,#10034);
#7166=LINE('',#45686,#10035);
#7167=LINE('',#45688,#10036);
#7168=LINE('',#45690,#10037);
#7169=LINE('',#45691,#10038);
#7170=LINE('',#45695,#10039);
#7171=LINE('',#45698,#10040);
#7172=LINE('',#45699,#10041);
#7173=LINE('',#45705,#10042);
#7174=LINE('',#45707,#10043);
#7175=LINE('',#45709,#10044);
#7176=LINE('',#45710,#10045);
#7177=LINE('',#45714,#10046);
#7178=LINE('',#45717,#10047);
#7179=LINE('',#45718,#10048);
#7180=LINE('',#45724,#10049);
#7181=LINE('',#45726,#10050);
#7182=LINE('',#45728,#10051);
#7183=LINE('',#45729,#10052);
#7184=LINE('',#45733,#10053);
#7185=LINE('',#45736,#10054);
#7186=LINE('',#45737,#10055);
#7187=LINE('',#45743,#10056);
#7188=LINE('',#45745,#10057);
#7189=LINE('',#45747,#10058);
#7190=LINE('',#45748,#10059);
#7191=LINE('',#45752,#10060);
#7192=LINE('',#45755,#10061);
#7193=LINE('',#45756,#10062);
#7194=LINE('',#45762,#10063);
#7195=LINE('',#45764,#10064);
#7196=LINE('',#45766,#10065);
#7197=LINE('',#45767,#10066);
#7198=LINE('',#45771,#10067);
#7199=LINE('',#45774,#10068);
#7200=LINE('',#45775,#10069);
#7201=LINE('',#45781,#10070);
#7202=LINE('',#45783,#10071);
#7203=LINE('',#45785,#10072);
#7204=LINE('',#45786,#10073);
#7205=LINE('',#45790,#10074);
#7206=LINE('',#45793,#10075);
#7207=LINE('',#45794,#10076);
#7208=LINE('',#45800,#10077);
#7209=LINE('',#45802,#10078);
#7210=LINE('',#45804,#10079);
#7211=LINE('',#45805,#10080);
#7212=LINE('',#45809,#10081);
#7213=LINE('',#45812,#10082);
#7214=LINE('',#45813,#10083);
#7215=LINE('',#45819,#10084);
#7216=LINE('',#45821,#10085);
#7217=LINE('',#45823,#10086);
#7218=LINE('',#45824,#10087);
#7219=LINE('',#45828,#10088);
#7220=LINE('',#45831,#10089);
#7221=LINE('',#45832,#10090);
#7222=LINE('',#45838,#10091);
#7223=LINE('',#45840,#10092);
#7224=LINE('',#45842,#10093);
#7225=LINE('',#45843,#10094);
#7226=LINE('',#45847,#10095);
#7227=LINE('',#45850,#10096);
#7228=LINE('',#45851,#10097);
#7229=LINE('',#45857,#10098);
#7230=LINE('',#45859,#10099);
#7231=LINE('',#45861,#10100);
#7232=LINE('',#45862,#10101);
#7233=LINE('',#45866,#10102);
#7234=LINE('',#45869,#10103);
#7235=LINE('',#45870,#10104);
#7236=LINE('',#45876,#10105);
#7237=LINE('',#45878,#10106);
#7238=LINE('',#45880,#10107);
#7239=LINE('',#45881,#10108);
#7240=LINE('',#45885,#10109);
#7241=LINE('',#45888,#10110);
#7242=LINE('',#45889,#10111);
#7243=LINE('',#45895,#10112);
#7244=LINE('',#45897,#10113);
#7245=LINE('',#45899,#10114);
#7246=LINE('',#45900,#10115);
#7247=LINE('',#45905,#10116);
#7248=LINE('',#45909,#10117);
#7249=LINE('',#45910,#10118);
#7250=LINE('',#45918,#10119);
#7251=LINE('',#45920,#10120);
#7252=LINE('',#45922,#10121);
#7253=LINE('',#45923,#10122);
#7254=LINE('',#45927,#10123);
#7255=LINE('',#45930,#10124);
#7256=LINE('',#45931,#10125);
#7257=LINE('',#45937,#10126);
#7258=LINE('',#45939,#10127);
#7259=LINE('',#45941,#10128);
#7260=LINE('',#45942,#10129);
#7261=LINE('',#45946,#10130);
#7262=LINE('',#45949,#10131);
#7263=LINE('',#45950,#10132);
#7264=LINE('',#45956,#10133);
#7265=LINE('',#45958,#10134);
#7266=LINE('',#45960,#10135);
#7267=LINE('',#45961,#10136);
#7268=LINE('',#45965,#10137);
#7269=LINE('',#45968,#10138);
#7270=LINE('',#45969,#10139);
#7271=LINE('',#45975,#10140);
#7272=LINE('',#45977,#10141);
#7273=LINE('',#45979,#10142);
#7274=LINE('',#45980,#10143);
#7275=LINE('',#45984,#10144);
#7276=LINE('',#45987,#10145);
#7277=LINE('',#45988,#10146);
#7278=LINE('',#45994,#10147);
#7279=LINE('',#45996,#10148);
#7280=LINE('',#45998,#10149);
#7281=LINE('',#45999,#10150);
#7282=LINE('',#46003,#10151);
#7283=LINE('',#46006,#10152);
#7284=LINE('',#46007,#10153);
#7285=LINE('',#46013,#10154);
#7286=LINE('',#46015,#10155);
#7287=LINE('',#46017,#10156);
#7288=LINE('',#46018,#10157);
#7289=LINE('',#46022,#10158);
#7290=LINE('',#46025,#10159);
#7291=LINE('',#46026,#10160);
#7292=LINE('',#46032,#10161);
#7293=LINE('',#46034,#10162);
#7294=LINE('',#46036,#10163);
#7295=LINE('',#46037,#10164);
#7296=LINE('',#46041,#10165);
#7297=LINE('',#46044,#10166);
#7298=LINE('',#46045,#10167);
#7299=LINE('',#46051,#10168);
#7300=LINE('',#46053,#10169);
#7301=LINE('',#46055,#10170);
#7302=LINE('',#46056,#10171);
#7303=LINE('',#46060,#10172);
#7304=LINE('',#46063,#10173);
#7305=LINE('',#46064,#10174);
#7306=LINE('',#46070,#10175);
#7307=LINE('',#46072,#10176);
#7308=LINE('',#46074,#10177);
#7309=LINE('',#46075,#10178);
#7310=LINE('',#46079,#10179);
#7311=LINE('',#46082,#10180);
#7312=LINE('',#46083,#10181);
#7313=LINE('',#46089,#10182);
#7314=LINE('',#46091,#10183);
#7315=LINE('',#46093,#10184);
#7316=LINE('',#46094,#10185);
#7317=LINE('',#46098,#10186);
#7318=LINE('',#46101,#10187);
#7319=LINE('',#46102,#10188);
#7320=LINE('',#46108,#10189);
#7321=LINE('',#46110,#10190);
#7322=LINE('',#46112,#10191);
#7323=LINE('',#46113,#10192);
#7324=LINE('',#46117,#10193);
#7325=LINE('',#46120,#10194);
#7326=LINE('',#46121,#10195);
#7327=LINE('',#46127,#10196);
#7328=LINE('',#46129,#10197);
#7329=LINE('',#46131,#10198);
#7330=LINE('',#46132,#10199);
#7331=LINE('',#46136,#10200);
#7332=LINE('',#46139,#10201);
#7333=LINE('',#46140,#10202);
#7334=LINE('',#46146,#10203);
#7335=LINE('',#46148,#10204);
#7336=LINE('',#46150,#10205);
#7337=LINE('',#46151,#10206);
#7338=LINE('',#46155,#10207);
#7339=LINE('',#46158,#10208);
#7340=LINE('',#46159,#10209);
#7341=LINE('',#46165,#10210);
#7342=LINE('',#46167,#10211);
#7343=LINE('',#46169,#10212);
#7344=LINE('',#46170,#10213);
#7345=LINE('',#46174,#10214);
#7346=LINE('',#46177,#10215);
#7347=LINE('',#46178,#10216);
#7348=LINE('',#46184,#10217);
#7349=LINE('',#46186,#10218);
#7350=LINE('',#46188,#10219);
#7351=LINE('',#46189,#10220);
#7352=LINE('',#46193,#10221);
#7353=LINE('',#46196,#10222);
#7354=LINE('',#46197,#10223);
#7355=LINE('',#46203,#10224);
#7356=LINE('',#46205,#10225);
#7357=LINE('',#46207,#10226);
#7358=LINE('',#46208,#10227);
#7359=LINE('',#46212,#10228);
#7360=LINE('',#46215,#10229);
#7361=LINE('',#46216,#10230);
#7362=LINE('',#46222,#10231);
#7363=LINE('',#46224,#10232);
#7364=LINE('',#46226,#10233);
#7365=LINE('',#46227,#10234);
#7366=LINE('',#46231,#10235);
#7367=LINE('',#46234,#10236);
#7368=LINE('',#46235,#10237);
#7369=LINE('',#46241,#10238);
#7370=LINE('',#46243,#10239);
#7371=LINE('',#46245,#10240);
#7372=LINE('',#46246,#10241);
#7373=LINE('',#46250,#10242);
#7374=LINE('',#46253,#10243);
#7375=LINE('',#46254,#10244);
#7376=LINE('',#46260,#10245);
#7377=LINE('',#46262,#10246);
#7378=LINE('',#46264,#10247);
#7379=LINE('',#46265,#10248);
#7380=LINE('',#46268,#10249);
#7381=LINE('',#46270,#10250);
#7382=LINE('',#46271,#10251);
#7383=LINE('',#46274,#10252);
#7384=LINE('',#46276,#10253);
#7385=LINE('',#46277,#10254);
#7386=LINE('',#46280,#10255);
#7387=LINE('',#46282,#10256);
#7388=LINE('',#46283,#10257);
#7389=LINE('',#46286,#10258);
#7390=LINE('',#46288,#10259);
#7391=LINE('',#46289,#10260);
#7392=LINE('',#46291,#10261);
#7393=LINE('',#46292,#10262);
#7394=LINE('',#46298,#10263);
#7395=LINE('',#46304,#10264);
#7396=LINE('',#46308,#10265);
#7397=LINE('',#46315,#10266);
#7398=LINE('',#46316,#10267);
#7399=LINE('',#46320,#10268);
#9952=VECTOR('',#32484,5.);
#9953=VECTOR('',#32489,5.);
#9954=VECTOR('',#32492,5.);
#9955=VECTOR('',#32495,5.);
#9956=VECTOR('',#32498,5.);
#9957=VECTOR('',#32501,5.);
#9958=VECTOR('',#32504,5.);
#9959=VECTOR('',#32507,5.);
#9960=VECTOR('',#32510,5.);
#9961=VECTOR('',#32513,5.);
#9962=VECTOR('',#32516,5.);
#9963=VECTOR('',#32519,5.);
#9964=VECTOR('',#32522,5.);
#9965=VECTOR('',#32525,5.);
#9966=VECTOR('',#32528,5.);
#9967=VECTOR('',#32531,5.);
#9968=VECTOR('',#32534,5.);
#9969=VECTOR('',#32537,5.);
#9970=VECTOR('',#32540,5.);
#9971=VECTOR('',#32543,5.);
#9972=VECTOR('',#32546,5.);
#9973=VECTOR('',#32551,4.0705);
#9974=VECTOR('',#32556,4.0705);
#9975=VECTOR('',#32559,4.0705);
#9976=VECTOR('',#32562,4.0705);
#9977=VECTOR('',#32565,4.0705);
#9978=VECTOR('',#32568,4.0705);
#9979=VECTOR('',#32571,4.0705);
#9980=VECTOR('',#32574,4.0705);
#9981=VECTOR('',#32577,4.0705);
#9982=VECTOR('',#32580,4.0705);
#9983=VECTOR('',#32583,4.0705);
#9984=VECTOR('',#32586,4.0705);
#9985=VECTOR('',#32589,4.0705);
#9986=VECTOR('',#32592,4.0705);
#9987=VECTOR('',#32595,4.0705);
#9988=VECTOR('',#32598,4.0705);
#9989=VECTOR('',#32601,4.0705);
#9990=VECTOR('',#32604,4.0705);
#9991=VECTOR('',#32607,4.0705);
#9992=VECTOR('',#32610,4.0705);
#9993=VECTOR('',#32627,10.);
#9994=VECTOR('',#32628,10.);
#9995=VECTOR('',#32629,10.);
#9996=VECTOR('',#32630,10.);
#9997=VECTOR('',#32635,10.);
#9998=VECTOR('',#32638,10.);
#9999=VECTOR('',#32639,10.);
#10000=VECTOR('',#32646,10.);
#10001=VECTOR('',#32647,10.);
#10002=VECTOR('',#32648,10.);
#10003=VECTOR('',#32649,10.);
#10004=VECTOR('',#32654,10.);
#10005=VECTOR('',#32657,10.);
#10006=VECTOR('',#32658,10.);
#10007=VECTOR('',#32665,10.);
#10008=VECTOR('',#32666,10.);
#10009=VECTOR('',#32667,10.);
#10010=VECTOR('',#32668,10.);
#10011=VECTOR('',#32673,10.);
#10012=VECTOR('',#32676,10.);
#10013=VECTOR('',#32677,10.);
#10014=VECTOR('',#32684,10.);
#10015=VECTOR('',#32685,10.);
#10016=VECTOR('',#32686,10.);
#10017=VECTOR('',#32687,10.);
#10018=VECTOR('',#32692,10.);
#10019=VECTOR('',#32695,10.);
#10020=VECTOR('',#32696,10.);
#10021=VECTOR('',#32703,10.);
#10022=VECTOR('',#32704,10.);
#10023=VECTOR('',#32705,10.);
#10024=VECTOR('',#32706,10.);
#10025=VECTOR('',#32711,10.);
#10026=VECTOR('',#32714,10.);
#10027=VECTOR('',#32715,10.);
#10028=VECTOR('',#32722,10.);
#10029=VECTOR('',#32723,10.);
#10030=VECTOR('',#32724,10.);
#10031=VECTOR('',#32725,10.);
#10032=VECTOR('',#32730,10.);
#10033=VECTOR('',#32733,10.);
#10034=VECTOR('',#32734,10.);
#10035=VECTOR('',#32741,10.);
#10036=VECTOR('',#32742,10.);
#10037=VECTOR('',#32743,10.);
#10038=VECTOR('',#32744,10.);
#10039=VECTOR('',#32749,10.);
#10040=VECTOR('',#32752,10.);
#10041=VECTOR('',#32753,10.);
#10042=VECTOR('',#32760,10.);
#10043=VECTOR('',#32761,10.);
#10044=VECTOR('',#32762,10.);
#10045=VECTOR('',#32763,10.);
#10046=VECTOR('',#32768,10.);
#10047=VECTOR('',#32771,10.);
#10048=VECTOR('',#32772,10.);
#10049=VECTOR('',#32779,10.);
#10050=VECTOR('',#32780,10.);
#10051=VECTOR('',#32781,10.);
#10052=VECTOR('',#32782,10.);
#10053=VECTOR('',#32787,10.);
#10054=VECTOR('',#32790,10.);
#10055=VECTOR('',#32791,10.);
#10056=VECTOR('',#32798,10.);
#10057=VECTOR('',#32799,10.);
#10058=VECTOR('',#32800,10.);
#10059=VECTOR('',#32801,10.);
#10060=VECTOR('',#32806,10.);
#10061=VECTOR('',#32809,10.);
#10062=VECTOR('',#32810,10.);
#10063=VECTOR('',#32817,10.);
#10064=VECTOR('',#32818,10.);
#10065=VECTOR('',#32819,10.);
#10066=VECTOR('',#32820,10.);
#10067=VECTOR('',#32825,10.);
#10068=VECTOR('',#32828,10.);
#10069=VECTOR('',#32829,10.);
#10070=VECTOR('',#32836,10.);
#10071=VECTOR('',#32837,10.);
#10072=VECTOR('',#32838,10.);
#10073=VECTOR('',#32839,10.);
#10074=VECTOR('',#32844,10.);
#10075=VECTOR('',#32847,10.);
#10076=VECTOR('',#32848,10.);
#10077=VECTOR('',#32855,10.);
#10078=VECTOR('',#32856,10.);
#10079=VECTOR('',#32857,10.);
#10080=VECTOR('',#32858,10.);
#10081=VECTOR('',#32863,10.);
#10082=VECTOR('',#32866,10.);
#10083=VECTOR('',#32867,10.);
#10084=VECTOR('',#32874,10.);
#10085=VECTOR('',#32875,10.);
#10086=VECTOR('',#32876,10.);
#10087=VECTOR('',#32877,10.);
#10088=VECTOR('',#32882,10.);
#10089=VECTOR('',#32885,10.);
#10090=VECTOR('',#32886,10.);
#10091=VECTOR('',#32893,10.);
#10092=VECTOR('',#32894,10.);
#10093=VECTOR('',#32895,10.);
#10094=VECTOR('',#32896,10.);
#10095=VECTOR('',#32901,10.);
#10096=VECTOR('',#32904,10.);
#10097=VECTOR('',#32905,10.);
#10098=VECTOR('',#32912,10.);
#10099=VECTOR('',#32913,10.);
#10100=VECTOR('',#32914,10.);
#10101=VECTOR('',#32915,10.);
#10102=VECTOR('',#32920,10.);
#10103=VECTOR('',#32923,10.);
#10104=VECTOR('',#32924,10.);
#10105=VECTOR('',#32931,10.);
#10106=VECTOR('',#32932,10.);
#10107=VECTOR('',#32933,10.);
#10108=VECTOR('',#32934,10.);
#10109=VECTOR('',#32939,10.);
#10110=VECTOR('',#32942,10.);
#10111=VECTOR('',#32943,10.);
#10112=VECTOR('',#32950,10.);
#10113=VECTOR('',#32951,10.);
#10114=VECTOR('',#32952,10.);
#10115=VECTOR('',#32953,10.);
#10116=VECTOR('',#32958,10.);
#10117=VECTOR('',#32963,10.);
#10118=VECTOR('',#32964,10.);
#10119=VECTOR('',#32973,10.);
#10120=VECTOR('',#32974,10.);
#10121=VECTOR('',#32975,10.);
#10122=VECTOR('',#32976,10.);
#10123=VECTOR('',#32981,10.);
#10124=VECTOR('',#32984,10.);
#10125=VECTOR('',#32985,10.);
#10126=VECTOR('',#32992,10.);
#10127=VECTOR('',#32993,10.);
#10128=VECTOR('',#32994,10.);
#10129=VECTOR('',#32995,10.);
#10130=VECTOR('',#33000,10.);
#10131=VECTOR('',#33003,10.);
#10132=VECTOR('',#33004,10.);
#10133=VECTOR('',#33011,10.);
#10134=VECTOR('',#33012,10.);
#10135=VECTOR('',#33013,10.);
#10136=VECTOR('',#33014,10.);
#10137=VECTOR('',#33019,10.);
#10138=VECTOR('',#33022,10.);
#10139=VECTOR('',#33023,10.);
#10140=VECTOR('',#33030,10.);
#10141=VECTOR('',#33031,10.);
#10142=VECTOR('',#33032,10.);
#10143=VECTOR('',#33033,10.);
#10144=VECTOR('',#33038,10.);
#10145=VECTOR('',#33041,10.);
#10146=VECTOR('',#33042,10.);
#10147=VECTOR('',#33049,10.);
#10148=VECTOR('',#33050,10.);
#10149=VECTOR('',#33051,10.);
#10150=VECTOR('',#33052,10.);
#10151=VECTOR('',#33057,10.);
#10152=VECTOR('',#33060,10.);
#10153=VECTOR('',#33061,10.);
#10154=VECTOR('',#33068,10.);
#10155=VECTOR('',#33069,10.);
#10156=VECTOR('',#33070,10.);
#10157=VECTOR('',#33071,10.);
#10158=VECTOR('',#33076,10.);
#10159=VECTOR('',#33079,10.);
#10160=VECTOR('',#33080,10.);
#10161=VECTOR('',#33087,10.);
#10162=VECTOR('',#33088,10.);
#10163=VECTOR('',#33089,10.);
#10164=VECTOR('',#33090,10.);
#10165=VECTOR('',#33095,10.);
#10166=VECTOR('',#33098,10.);
#10167=VECTOR('',#33099,10.);
#10168=VECTOR('',#33106,10.);
#10169=VECTOR('',#33107,10.);
#10170=VECTOR('',#33108,10.);
#10171=VECTOR('',#33109,10.);
#10172=VECTOR('',#33114,10.);
#10173=VECTOR('',#33117,10.);
#10174=VECTOR('',#33118,10.);
#10175=VECTOR('',#33125,10.);
#10176=VECTOR('',#33126,10.);
#10177=VECTOR('',#33127,10.);
#10178=VECTOR('',#33128,10.);
#10179=VECTOR('',#33133,10.);
#10180=VECTOR('',#33136,10.);
#10181=VECTOR('',#33137,10.);
#10182=VECTOR('',#33144,10.);
#10183=VECTOR('',#33145,10.);
#10184=VECTOR('',#33146,10.);
#10185=VECTOR('',#33147,10.);
#10186=VECTOR('',#33152,10.);
#10187=VECTOR('',#33155,10.);
#10188=VECTOR('',#33156,10.);
#10189=VECTOR('',#33163,10.);
#10190=VECTOR('',#33164,10.);
#10191=VECTOR('',#33165,10.);
#10192=VECTOR('',#33166,10.);
#10193=VECTOR('',#33171,10.);
#10194=VECTOR('',#33174,10.);
#10195=VECTOR('',#33175,10.);
#10196=VECTOR('',#33182,10.);
#10197=VECTOR('',#33183,10.);
#10198=VECTOR('',#33184,10.);
#10199=VECTOR('',#33185,10.);
#10200=VECTOR('',#33190,10.);
#10201=VECTOR('',#33193,10.);
#10202=VECTOR('',#33194,10.);
#10203=VECTOR('',#33201,10.);
#10204=VECTOR('',#33202,10.);
#10205=VECTOR('',#33203,10.);
#10206=VECTOR('',#33204,10.);
#10207=VECTOR('',#33209,10.);
#10208=VECTOR('',#33212,10.);
#10209=VECTOR('',#33213,10.);
#10210=VECTOR('',#33220,10.);
#10211=VECTOR('',#33221,10.);
#10212=VECTOR('',#33222,10.);
#10213=VECTOR('',#33223,10.);
#10214=VECTOR('',#33228,10.);
#10215=VECTOR('',#33231,10.);
#10216=VECTOR('',#33232,10.);
#10217=VECTOR('',#33239,10.);
#10218=VECTOR('',#33240,10.);
#10219=VECTOR('',#33241,10.);
#10220=VECTOR('',#33242,10.);
#10221=VECTOR('',#33247,10.);
#10222=VECTOR('',#33250,10.);
#10223=VECTOR('',#33251,10.);
#10224=VECTOR('',#33258,10.);
#10225=VECTOR('',#33259,10.);
#10226=VECTOR('',#33260,10.);
#10227=VECTOR('',#33261,10.);
#10228=VECTOR('',#33266,10.);
#10229=VECTOR('',#33269,10.);
#10230=VECTOR('',#33270,10.);
#10231=VECTOR('',#33277,10.);
#10232=VECTOR('',#33278,10.);
#10233=VECTOR('',#33279,10.);
#10234=VECTOR('',#33280,10.);
#10235=VECTOR('',#33285,10.);
#10236=VECTOR('',#33288,10.);
#10237=VECTOR('',#33289,10.);
#10238=VECTOR('',#33296,10.);
#10239=VECTOR('',#33297,10.);
#10240=VECTOR('',#33298,10.);
#10241=VECTOR('',#33299,10.);
#10242=VECTOR('',#33304,10.);
#10243=VECTOR('',#33307,10.);
#10244=VECTOR('',#33308,10.);
#10245=VECTOR('',#33315,10.);
#10246=VECTOR('',#33316,10.);
#10247=VECTOR('',#33317,10.);
#10248=VECTOR('',#33318,10.);
#10249=VECTOR('',#33321,10.);
#10250=VECTOR('',#33322,10.);
#10251=VECTOR('',#33323,10.);
#10252=VECTOR('',#33326,10.);
#10253=VECTOR('',#33327,10.);
#10254=VECTOR('',#33328,10.);
#10255=VECTOR('',#33331,10.);
#10256=VECTOR('',#33332,10.);
#10257=VECTOR('',#33333,10.);
#10258=VECTOR('',#33336,10.);
#10259=VECTOR('',#33337,10.);
#10260=VECTOR('',#33338,10.);
#10261=VECTOR('',#33341,10.);
#10262=VECTOR('',#33342,10.);
#10263=VECTOR('',#33351,4.75);
#10264=VECTOR('',#33360,4.975);
#10265=VECTOR('',#33365,4.95);
#10266=VECTOR('',#33374,8.);
#10267=VECTOR('',#33375,8.);
#10268=VECTOR('',#33380,7.75);
#10642=CIRCLE('',#26607,4.925);
#10643=CIRCLE('',#26628,4.925);
#10644=CIRCLE('',#26630,4.0705);
#10645=CIRCLE('',#26651,4.925);
#10646=CIRCLE('',#26653,4.925);
#10647=CIRCLE('',#26654,4.925);
#10648=CIRCLE('',#26655,4.0705);
#10649=CIRCLE('',#26659,8.);
#10650=CIRCLE('',#26662,8.);
#10651=CIRCLE('',#26665,8.);
#10652=CIRCLE('',#26668,8.);
#10653=CIRCLE('',#26671,8.);
#10654=CIRCLE('',#26674,8.);
#10655=CIRCLE('',#26677,8.);
#10656=CIRCLE('',#26680,8.);
#10657=CIRCLE('',#26683,8.);
#10658=CIRCLE('',#26686,8.);
#10659=CIRCLE('',#26689,8.);
#10660=CIRCLE('',#26692,8.);
#10661=CIRCLE('',#26695,8.);
#10662=CIRCLE('',#26698,8.);
#10663=CIRCLE('',#26701,8.);
#10664=CIRCLE('',#26704,8.);
#10665=CIRCLE('',#26707,8.);
#10666=CIRCLE('',#26710,8.);
#10667=CIRCLE('',#26713,8.);
#10668=CIRCLE('',#26716,8.);
#10669=CIRCLE('',#26719,8.);
#10670=CIRCLE('',#26722,8.);
#10671=CIRCLE('',#26725,8.);
#10672=CIRCLE('',#26728,8.);
#10673=CIRCLE('',#26731,8.);
#10674=CIRCLE('',#26734,8.);
#10675=CIRCLE('',#26737,8.);
#10676=CIRCLE('',#26740,8.);
#10677=CIRCLE('',#26743,8.);
#10678=CIRCLE('',#26746,8.);
#10679=CIRCLE('',#26749,8.);
#10680=CIRCLE('',#26752,8.);
#10681=CIRCLE('',#26755,8.);
#10682=CIRCLE('',#26758,8.);
#10683=CIRCLE('',#26761,8.);
#10684=CIRCLE('',#26762,8.);
#10685=CIRCLE('',#26765,8.);
#10686=CIRCLE('',#26766,8.);
#10687=CIRCLE('',#26769,8.);
#10688=CIRCLE('',#26772,8.);
#10689=CIRCLE('',#26775,8.);
#10690=CIRCLE('',#26778,8.);
#10691=CIRCLE('',#26781,8.);
#10692=CIRCLE('',#26784,8.);
#10693=CIRCLE('',#26787,8.);
#10694=CIRCLE('',#26790,8.);
#10695=CIRCLE('',#26793,8.);
#10696=CIRCLE('',#26796,8.);
#10697=CIRCLE('',#26799,8.);
#10698=CIRCLE('',#26802,8.);
#10699=CIRCLE('',#26805,8.);
#10700=CIRCLE('',#26808,8.);
#10701=CIRCLE('',#26811,8.);
#10702=CIRCLE('',#26814,8.);
#10703=CIRCLE('',#26817,8.);
#10704=CIRCLE('',#26820,8.);
#10705=CIRCLE('',#26823,8.);
#10706=CIRCLE('',#26826,8.);
#10707=CIRCLE('',#26829,8.);
#10708=CIRCLE('',#26832,8.);
#10709=CIRCLE('',#26835,8.);
#10710=CIRCLE('',#26838,8.);
#10711=CIRCLE('',#26841,8.);
#10712=CIRCLE('',#26844,8.);
#10713=CIRCLE('',#26847,8.);
#10714=CIRCLE('',#26850,8.);
#10715=CIRCLE('',#26853,8.);
#10716=CIRCLE('',#26856,8.);
#10717=CIRCLE('',#26859,8.);
#10718=CIRCLE('',#26862,8.);
#10719=CIRCLE('',#26865,8.);
#10720=CIRCLE('',#26868,8.);
#10721=CIRCLE('',#26871,8.);
#10722=CIRCLE('',#26874,8.);
#10723=CIRCLE('',#26883,4.5);
#10724=CIRCLE('',#26886,4.925);
#10725=CIRCLE('',#26888,4.95);
#10726=CIRCLE('',#26890,4.95);
#10727=CIRCLE('',#26892,8.);
#10728=CIRCLE('',#26894,8.);
#10729=CIRCLE('',#26896,7.5);
#12686=VERTEX_POINT('',#40731);
#12687=VERTEX_POINT('',#40732);
#12688=VERTEX_POINT('',#40734);
#12689=VERTEX_POINT('',#40751);
#12690=VERTEX_POINT('',#40764);
#12691=VERTEX_POINT('',#40765);
#12692=VERTEX_POINT('',#40848);
#12693=VERTEX_POINT('',#40849);
#12694=VERTEX_POINT('',#40938);
#12695=VERTEX_POINT('',#40939);
#12696=VERTEX_POINT('',#41028);
#12697=VERTEX_POINT('',#41029);
#12698=VERTEX_POINT('',#41112);
#12699=VERTEX_POINT('',#41113);
#12700=VERTEX_POINT('',#41202);
#12701=VERTEX_POINT('',#41203);
#12702=VERTEX_POINT('',#41292);
#12703=VERTEX_POINT('',#41293);
#12704=VERTEX_POINT('',#41376);
#12705=VERTEX_POINT('',#41377);
#12706=VERTEX_POINT('',#41466);
#12707=VERTEX_POINT('',#41467);
#12708=VERTEX_POINT('',#41544);
#12709=VERTEX_POINT('',#41545);
#12710=VERTEX_POINT('',#41592);
#12711=VERTEX_POINT('',#41593);
#12712=VERTEX_POINT('',#41646);
#12713=VERTEX_POINT('',#41647);
#12714=VERTEX_POINT('',#41730);
#12715=VERTEX_POINT('',#41731);
#12716=VERTEX_POINT('',#41814);
#12717=VERTEX_POINT('',#41815);
#12718=VERTEX_POINT('',#41904);
#12719=VERTEX_POINT('',#41905);
#12720=VERTEX_POINT('',#41994);
#12721=VERTEX_POINT('',#41995);
#12722=VERTEX_POINT('',#42078);
#12723=VERTEX_POINT('',#42079);
#12724=VERTEX_POINT('',#42168);
#12725=VERTEX_POINT('',#42169);
#12726=VERTEX_POINT('',#42258);
#12727=VERTEX_POINT('',#42259);
#12728=VERTEX_POINT('',#42342);
#12729=VERTEX_POINT('',#42343);
#12730=VERTEX_POINT('',#42345);
#12731=VERTEX_POINT('',#42428);
#12732=VERTEX_POINT('',#42429);
#12733=VERTEX_POINT('',#42431);
#12734=VERTEX_POINT('',#42443);
#12735=VERTEX_POINT('',#42454);
#12736=VERTEX_POINT('',#42455);
#12737=VERTEX_POINT('',#42491);
#12738=VERTEX_POINT('',#42492);
#12739=VERTEX_POINT('',#42528);
#12740=VERTEX_POINT('',#42529);
#12741=VERTEX_POINT('',#42566);
#12742=VERTEX_POINT('',#42567);
#12743=VERTEX_POINT('',#42603);
#12744=VERTEX_POINT('',#42604);
#12745=VERTEX_POINT('',#42640);
#12746=VERTEX_POINT('',#42641);
#12747=VERTEX_POINT('',#42678);
#12748=VERTEX_POINT('',#42679);
#12749=VERTEX_POINT('',#42715);
#12750=VERTEX_POINT('',#42716);
#12751=VERTEX_POINT('',#42752);
#12752=VERTEX_POINT('',#42753);
#12753=VERTEX_POINT('',#42783);
#12754=VERTEX_POINT('',#42784);
#12755=VERTEX_POINT('',#42807);
#12756=VERTEX_POINT('',#42808);
#12757=VERTEX_POINT('',#42835);
#12758=VERTEX_POINT('',#42836);
#12759=VERTEX_POINT('',#42872);
#12760=VERTEX_POINT('',#42873);
#12761=VERTEX_POINT('',#42909);
#12762=VERTEX_POINT('',#42910);
#12763=VERTEX_POINT('',#42946);
#12764=VERTEX_POINT('',#42947);
#12765=VERTEX_POINT('',#42984);
#12766=VERTEX_POINT('',#42985);
#12767=VERTEX_POINT('',#43021);
#12768=VERTEX_POINT('',#43022);
#12769=VERTEX_POINT('',#43058);
#12770=VERTEX_POINT('',#43059);
#12771=VERTEX_POINT('',#43096);
#12772=VERTEX_POINT('',#43097);
#12773=VERTEX_POINT('',#43236);
#12774=VERTEX_POINT('',#44333);
#12775=VERTEX_POINT('',#44452);
#12776=VERTEX_POINT('',#44455);
#12777=VERTEX_POINT('',#45570);
#12778=VERTEX_POINT('',#45571);
#12779=VERTEX_POINT('',#45573);
#12780=VERTEX_POINT('',#45575);
#12781=VERTEX_POINT('',#45579);
#12782=VERTEX_POINT('',#45583);
#12783=VERTEX_POINT('',#45589);
#12784=VERTEX_POINT('',#45590);
#12785=VERTEX_POINT('',#45592);
#12786=VERTEX_POINT('',#45594);
#12787=VERTEX_POINT('',#45598);
#12788=VERTEX_POINT('',#45602);
#12789=VERTEX_POINT('',#45608);
#12790=VERTEX_POINT('',#45609);
#12791=VERTEX_POINT('',#45611);
#12792=VERTEX_POINT('',#45613);
#12793=VERTEX_POINT('',#45617);
#12794=VERTEX_POINT('',#45621);
#12795=VERTEX_POINT('',#45627);
#12796=VERTEX_POINT('',#45628);
#12797=VERTEX_POINT('',#45630);
#12798=VERTEX_POINT('',#45632);
#12799=VERTEX_POINT('',#45636);
#12800=VERTEX_POINT('',#45640);
#12801=VERTEX_POINT('',#45646);
#12802=VERTEX_POINT('',#45647);
#12803=VERTEX_POINT('',#45649);
#12804=VERTEX_POINT('',#45651);
#12805=VERTEX_POINT('',#45655);
#12806=VERTEX_POINT('',#45659);
#12807=VERTEX_POINT('',#45665);
#12808=VERTEX_POINT('',#45666);
#12809=VERTEX_POINT('',#45668);
#12810=VERTEX_POINT('',#45670);
#12811=VERTEX_POINT('',#45674);
#12812=VERTEX_POINT('',#45678);
#12813=VERTEX_POINT('',#45684);
#12814=VERTEX_POINT('',#45685);
#12815=VERTEX_POINT('',#45687);
#12816=VERTEX_POINT('',#45689);
#12817=VERTEX_POINT('',#45693);
#12818=VERTEX_POINT('',#45697);
#12819=VERTEX_POINT('',#45703);
#12820=VERTEX_POINT('',#45704);
#12821=VERTEX_POINT('',#45706);
#12822=VERTEX_POINT('',#45708);
#12823=VERTEX_POINT('',#45712);
#12824=VERTEX_POINT('',#45716);
#12825=VERTEX_POINT('',#45722);
#12826=VERTEX_POINT('',#45723);
#12827=VERTEX_POINT('',#45725);
#12828=VERTEX_POINT('',#45727);
#12829=VERTEX_POINT('',#45731);
#12830=VERTEX_POINT('',#45735);
#12831=VERTEX_POINT('',#45741);
#12832=VERTEX_POINT('',#45742);
#12833=VERTEX_POINT('',#45744);
#12834=VERTEX_POINT('',#45746);
#12835=VERTEX_POINT('',#45750);
#12836=VERTEX_POINT('',#45754);
#12837=VERTEX_POINT('',#45760);
#12838=VERTEX_POINT('',#45761);
#12839=VERTEX_POINT('',#45763);
#12840=VERTEX_POINT('',#45765);
#12841=VERTEX_POINT('',#45769);
#12842=VERTEX_POINT('',#45773);
#12843=VERTEX_POINT('',#45779);
#12844=VERTEX_POINT('',#45780);
#12845=VERTEX_POINT('',#45782);
#12846=VERTEX_POINT('',#45784);
#12847=VERTEX_POINT('',#45788);
#12848=VERTEX_POINT('',#45792);
#12849=VERTEX_POINT('',#45798);
#12850=VERTEX_POINT('',#45799);
#12851=VERTEX_POINT('',#45801);
#12852=VERTEX_POINT('',#45803);
#12853=VERTEX_POINT('',#45807);
#12854=VERTEX_POINT('',#45811);
#12855=VERTEX_POINT('',#45817);
#12856=VERTEX_POINT('',#45818);
#12857=VERTEX_POINT('',#45820);
#12858=VERTEX_POINT('',#45822);
#12859=VERTEX_POINT('',#45826);
#12860=VERTEX_POINT('',#45830);
#12861=VERTEX_POINT('',#45836);
#12862=VERTEX_POINT('',#45837);
#12863=VERTEX_POINT('',#45839);
#12864=VERTEX_POINT('',#45841);
#12865=VERTEX_POINT('',#45845);
#12866=VERTEX_POINT('',#45849);
#12867=VERTEX_POINT('',#45855);
#12868=VERTEX_POINT('',#45856);
#12869=VERTEX_POINT('',#45858);
#12870=VERTEX_POINT('',#45860);
#12871=VERTEX_POINT('',#45864);
#12872=VERTEX_POINT('',#45868);
#12873=VERTEX_POINT('',#45874);
#12874=VERTEX_POINT('',#45875);
#12875=VERTEX_POINT('',#45877);
#12876=VERTEX_POINT('',#45879);
#12877=VERTEX_POINT('',#45883);
#12878=VERTEX_POINT('',#45887);
#12879=VERTEX_POINT('',#45893);
#12880=VERTEX_POINT('',#45894);
#12881=VERTEX_POINT('',#45896);
#12882=VERTEX_POINT('',#45898);
#12883=VERTEX_POINT('',#45902);
#12884=VERTEX_POINT('',#45904);
#12885=VERTEX_POINT('',#45908);
#12886=VERTEX_POINT('',#45912);
#12887=VERTEX_POINT('',#45916);
#12888=VERTEX_POINT('',#45917);
#12889=VERTEX_POINT('',#45919);
#12890=VERTEX_POINT('',#45921);
#12891=VERTEX_POINT('',#45925);
#12892=VERTEX_POINT('',#45929);
#12893=VERTEX_POINT('',#45935);
#12894=VERTEX_POINT('',#45936);
#12895=VERTEX_POINT('',#45938);
#12896=VERTEX_POINT('',#45940);
#12897=VERTEX_POINT('',#45944);
#12898=VERTEX_POINT('',#45948);
#12899=VERTEX_POINT('',#45954);
#12900=VERTEX_POINT('',#45955);
#12901=VERTEX_POINT('',#45957);
#12902=VERTEX_POINT('',#45959);
#12903=VERTEX_POINT('',#45963);
#12904=VERTEX_POINT('',#45967);
#12905=VERTEX_POINT('',#45973);
#12906=VERTEX_POINT('',#45974);
#12907=VERTEX_POINT('',#45976);
#12908=VERTEX_POINT('',#45978);
#12909=VERTEX_POINT('',#45982);
#12910=VERTEX_POINT('',#45986);
#12911=VERTEX_POINT('',#45992);
#12912=VERTEX_POINT('',#45993);
#12913=VERTEX_POINT('',#45995);
#12914=VERTEX_POINT('',#45997);
#12915=VERTEX_POINT('',#46001);
#12916=VERTEX_POINT('',#46005);
#12917=VERTEX_POINT('',#46011);
#12918=VERTEX_POINT('',#46012);
#12919=VERTEX_POINT('',#46014);
#12920=VERTEX_POINT('',#46016);
#12921=VERTEX_POINT('',#46020);
#12922=VERTEX_POINT('',#46024);
#12923=VERTEX_POINT('',#46030);
#12924=VERTEX_POINT('',#46031);
#12925=VERTEX_POINT('',#46033);
#12926=VERTEX_POINT('',#46035);
#12927=VERTEX_POINT('',#46039);
#12928=VERTEX_POINT('',#46043);
#12929=VERTEX_POINT('',#46049);
#12930=VERTEX_POINT('',#46050);
#12931=VERTEX_POINT('',#46052);
#12932=VERTEX_POINT('',#46054);
#12933=VERTEX_POINT('',#46058);
#12934=VERTEX_POINT('',#46062);
#12935=VERTEX_POINT('',#46068);
#12936=VERTEX_POINT('',#46069);
#12937=VERTEX_POINT('',#46071);
#12938=VERTEX_POINT('',#46073);
#12939=VERTEX_POINT('',#46077);
#12940=VERTEX_POINT('',#46081);
#12941=VERTEX_POINT('',#46087);
#12942=VERTEX_POINT('',#46088);
#12943=VERTEX_POINT('',#46090);
#12944=VERTEX_POINT('',#46092);
#12945=VERTEX_POINT('',#46096);
#12946=VERTEX_POINT('',#46100);
#12947=VERTEX_POINT('',#46106);
#12948=VERTEX_POINT('',#46107);
#12949=VERTEX_POINT('',#46109);
#12950=VERTEX_POINT('',#46111);
#12951=VERTEX_POINT('',#46115);
#12952=VERTEX_POINT('',#46119);
#12953=VERTEX_POINT('',#46125);
#12954=VERTEX_POINT('',#46126);
#12955=VERTEX_POINT('',#46128);
#12956=VERTEX_POINT('',#46130);
#12957=VERTEX_POINT('',#46134);
#12958=VERTEX_POINT('',#46138);
#12959=VERTEX_POINT('',#46144);
#12960=VERTEX_POINT('',#46145);
#12961=VERTEX_POINT('',#46147);
#12962=VERTEX_POINT('',#46149);
#12963=VERTEX_POINT('',#46153);
#12964=VERTEX_POINT('',#46157);
#12965=VERTEX_POINT('',#46163);
#12966=VERTEX_POINT('',#46164);
#12967=VERTEX_POINT('',#46166);
#12968=VERTEX_POINT('',#46168);
#12969=VERTEX_POINT('',#46172);
#12970=VERTEX_POINT('',#46176);
#12971=VERTEX_POINT('',#46182);
#12972=VERTEX_POINT('',#46183);
#12973=VERTEX_POINT('',#46185);
#12974=VERTEX_POINT('',#46187);
#12975=VERTEX_POINT('',#46191);
#12976=VERTEX_POINT('',#46195);
#12977=VERTEX_POINT('',#46201);
#12978=VERTEX_POINT('',#46202);
#12979=VERTEX_POINT('',#46204);
#12980=VERTEX_POINT('',#46206);
#12981=VERTEX_POINT('',#46210);
#12982=VERTEX_POINT('',#46214);
#12983=VERTEX_POINT('',#46220);
#12984=VERTEX_POINT('',#46221);
#12985=VERTEX_POINT('',#46223);
#12986=VERTEX_POINT('',#46225);
#12987=VERTEX_POINT('',#46229);
#12988=VERTEX_POINT('',#46233);
#12989=VERTEX_POINT('',#46239);
#12990=VERTEX_POINT('',#46240);
#12991=VERTEX_POINT('',#46242);
#12992=VERTEX_POINT('',#46244);
#12993=VERTEX_POINT('',#46248);
#12994=VERTEX_POINT('',#46252);
#12995=VERTEX_POINT('',#46258);
#12996=VERTEX_POINT('',#46259);
#12997=VERTEX_POINT('',#46261);
#12998=VERTEX_POINT('',#46263);
#12999=VERTEX_POINT('',#46267);
#13000=VERTEX_POINT('',#46269);
#13001=VERTEX_POINT('',#46273);
#13002=VERTEX_POINT('',#46275);
#13003=VERTEX_POINT('',#46279);
#13004=VERTEX_POINT('',#46281);
#13005=VERTEX_POINT('',#46285);
#13006=VERTEX_POINT('',#46287);
#13007=VERTEX_POINT('',#46295);
#13008=VERTEX_POINT('',#46302);
#13009=VERTEX_POINT('',#46306);
#13010=VERTEX_POINT('',#46310);
#13011=VERTEX_POINT('',#46313);
#13012=VERTEX_POINT('',#46318);
#16027=EDGE_CURVE('',#12686,#12687,#7083,.T.);
#16028=EDGE_CURVE('',#12686,#12688,#301,.T.);
#16029=EDGE_CURVE('',#12688,#12689,#10642,.T.);
#16030=EDGE_CURVE('',#12689,#12687,#302,.T.);
#16031=EDGE_CURVE('',#12690,#12691,#7084,.T.);
#16032=EDGE_CURVE('',#12690,#12686,#303,.T.);
#16033=EDGE_CURVE('',#12687,#12691,#304,.T.);
#16034=EDGE_CURVE('',#12692,#12693,#7085,.T.);
#16035=EDGE_CURVE('',#12692,#12690,#305,.T.);
#16036=EDGE_CURVE('',#12691,#12693,#306,.T.);
#16037=EDGE_CURVE('',#12694,#12695,#7086,.T.);
#16038=EDGE_CURVE('',#12694,#12692,#307,.T.);
#16039=EDGE_CURVE('',#12693,#12695,#308,.T.);
#16040=EDGE_CURVE('',#12696,#12697,#7087,.T.);
#16041=EDGE_CURVE('',#12696,#12694,#309,.T.);
#16042=EDGE_CURVE('',#12695,#12697,#310,.T.);
#16043=EDGE_CURVE('',#12698,#12699,#7088,.T.);
#16044=EDGE_CURVE('',#12698,#12696,#311,.T.);
#16045=EDGE_CURVE('',#12697,#12699,#312,.T.);
#16046=EDGE_CURVE('',#12700,#12701,#7089,.T.);
#16047=EDGE_CURVE('',#12700,#12698,#313,.T.);
#16048=EDGE_CURVE('',#12699,#12701,#314,.T.);
#16049=EDGE_CURVE('',#12702,#12703,#7090,.T.);
#16050=EDGE_CURVE('',#12702,#12700,#315,.T.);
#16051=EDGE_CURVE('',#12701,#12703,#316,.T.);
#16052=EDGE_CURVE('',#12704,#12705,#7091,.T.);
#16053=EDGE_CURVE('',#12704,#12702,#317,.T.);
#16054=EDGE_CURVE('',#12703,#12705,#318,.T.);
#16055=EDGE_CURVE('',#12706,#12707,#7092,.T.);
#16056=EDGE_CURVE('',#12706,#12704,#319,.T.);
#16057=EDGE_CURVE('',#12705,#12707,#320,.T.);
#16058=EDGE_CURVE('',#12708,#12709,#7093,.T.);
#16059=EDGE_CURVE('',#12708,#12706,#321,.T.);
#16060=EDGE_CURVE('',#12707,#12709,#322,.T.);
#16061=EDGE_CURVE('',#12710,#12711,#7094,.T.);
#16062=EDGE_CURVE('',#12710,#12708,#323,.T.);
#16063=EDGE_CURVE('',#12709,#12711,#324,.T.);
#16064=EDGE_CURVE('',#12712,#12713,#7095,.T.);
#16065=EDGE_CURVE('',#12712,#12710,#325,.T.);
#16066=EDGE_CURVE('',#12711,#12713,#326,.T.);
#16067=EDGE_CURVE('',#12714,#12715,#7096,.T.);
#16068=EDGE_CURVE('',#12714,#12712,#327,.T.);
#16069=EDGE_CURVE('',#12713,#12715,#328,.T.);
#16070=EDGE_CURVE('',#12716,#12717,#7097,.T.);
#16071=EDGE_CURVE('',#12716,#12714,#329,.T.);
#16072=EDGE_CURVE('',#12715,#12717,#330,.T.);
#16073=EDGE_CURVE('',#12718,#12719,#7098,.T.);
#16074=EDGE_CURVE('',#12718,#12716,#331,.T.);
#16075=EDGE_CURVE('',#12717,#12719,#332,.T.);
#16076=EDGE_CURVE('',#12720,#12721,#7099,.T.);
#16077=EDGE_CURVE('',#12720,#12718,#333,.T.);
#16078=EDGE_CURVE('',#12719,#12721,#334,.T.);
#16079=EDGE_CURVE('',#12722,#12723,#7100,.T.);
#16080=EDGE_CURVE('',#12722,#12720,#335,.T.);
#16081=EDGE_CURVE('',#12721,#12723,#336,.T.);
#16082=EDGE_CURVE('',#12724,#12725,#7101,.T.);
#16083=EDGE_CURVE('',#12724,#12722,#337,.T.);
#16084=EDGE_CURVE('',#12723,#12725,#338,.T.);
#16085=EDGE_CURVE('',#12726,#12727,#7102,.T.);
#16086=EDGE_CURVE('',#12726,#12724,#339,.T.);
#16087=EDGE_CURVE('',#12725,#12727,#340,.T.);
#16088=EDGE_CURVE('',#12728,#12729,#7103,.T.);
#16089=EDGE_CURVE('',#12730,#12728,#10643,.F.);
#16090=EDGE_CURVE('',#12730,#12726,#341,.T.);
#16091=EDGE_CURVE('',#12727,#12729,#342,.T.);
#16092=EDGE_CURVE('',#12731,#12732,#7104,.T.);
#16093=EDGE_CURVE('',#12731,#12733,#343,.T.);
#16094=EDGE_CURVE('',#12734,#12733,#10644,.T.);
#16095=EDGE_CURVE('',#12732,#12734,#344,.T.);
#16096=EDGE_CURVE('',#12735,#12736,#7105,.T.);
#16097=EDGE_CURVE('',#12735,#12731,#345,.T.);
#16098=EDGE_CURVE('',#12736,#12732,#346,.T.);
#16099=EDGE_CURVE('',#12737,#12738,#7106,.T.);
#16100=EDGE_CURVE('',#12737,#12735,#347,.T.);
#16101=EDGE_CURVE('',#12738,#12736,#348,.T.);
#16102=EDGE_CURVE('',#12739,#12740,#7107,.T.);
#16103=EDGE_CURVE('',#12739,#12737,#349,.T.);
#16104=EDGE_CURVE('',#12740,#12738,#350,.T.);
#16105=EDGE_CURVE('',#12741,#12742,#7108,.T.);
#16106=EDGE_CURVE('',#12741,#12739,#351,.T.);
#16107=EDGE_CURVE('',#12742,#12740,#352,.T.);
#16108=EDGE_CURVE('',#12743,#12744,#7109,.T.);
#16109=EDGE_CURVE('',#12743,#12741,#353,.T.);
#16110=EDGE_CURVE('',#12744,#12742,#354,.T.);
#16111=EDGE_CURVE('',#12745,#12746,#7110,.T.);
#16112=EDGE_CURVE('',#12745,#12743,#355,.T.);
#16113=EDGE_CURVE('',#12746,#12744,#356,.T.);
#16114=EDGE_CURVE('',#12747,#12748,#7111,.T.);
#16115=EDGE_CURVE('',#12747,#12745,#357,.T.);
#16116=EDGE_CURVE('',#12748,#12746,#358,.T.);
#16117=EDGE_CURVE('',#12749,#12750,#7112,.T.);
#16118=EDGE_CURVE('',#12749,#12747,#359,.T.);
#16119=EDGE_CURVE('',#12750,#12748,#360,.T.);
#16120=EDGE_CURVE('',#12751,#12752,#7113,.T.);
#16121=EDGE_CURVE('',#12751,#12749,#361,.T.);
#16122=EDGE_CURVE('',#12752,#12750,#362,.T.);
#16123=EDGE_CURVE('',#12753,#12754,#7114,.T.);
#16124=EDGE_CURVE('',#12753,#12751,#363,.T.);
#16125=EDGE_CURVE('',#12754,#12752,#364,.T.);
#16126=EDGE_CURVE('',#12755,#12756,#7115,.T.);
#16127=EDGE_CURVE('',#12755,#12753,#365,.T.);
#16128=EDGE_CURVE('',#12756,#12754,#366,.T.);
#16129=EDGE_CURVE('',#12757,#12758,#7116,.T.);
#16130=EDGE_CURVE('',#12757,#12755,#367,.T.);
#16131=EDGE_CURVE('',#12758,#12756,#368,.T.);
#16132=EDGE_CURVE('',#12759,#12760,#7117,.T.);
#16133=EDGE_CURVE('',#12759,#12757,#369,.T.);
#16134=EDGE_CURVE('',#12760,#12758,#370,.T.);
#16135=EDGE_CURVE('',#12761,#12762,#7118,.T.);
#16136=EDGE_CURVE('',#12761,#12759,#371,.T.);
#16137=EDGE_CURVE('',#12762,#12760,#372,.T.);
#16138=EDGE_CURVE('',#12763,#12764,#7119,.T.);
#16139=EDGE_CURVE('',#12763,#12761,#373,.T.);
#16140=EDGE_CURVE('',#12764,#12762,#374,.T.);
#16141=EDGE_CURVE('',#12765,#12766,#7120,.T.);
#16142=EDGE_CURVE('',#12765,#12763,#375,.T.);
#16143=EDGE_CURVE('',#12766,#12764,#376,.T.);
#16144=EDGE_CURVE('',#12767,#12768,#7121,.T.);
#16145=EDGE_CURVE('',#12767,#12765,#377,.T.);
#16146=EDGE_CURVE('',#12768,#12766,#378,.T.);
#16147=EDGE_CURVE('',#12769,#12770,#7122,.T.);
#16148=EDGE_CURVE('',#12769,#12767,#379,.T.);
#16149=EDGE_CURVE('',#12770,#12768,#380,.T.);
#16150=EDGE_CURVE('',#12771,#12772,#7123,.T.);
#16151=EDGE_CURVE('',#12771,#12769,#381,.T.);
#16152=EDGE_CURVE('',#12772,#12770,#382,.T.);
#16153=EDGE_CURVE('',#12733,#12730,#383,.T.);
#16154=EDGE_CURVE('',#12773,#12730,#10645,.F.);
#16155=EDGE_CURVE('',#12773,#12734,#384,.T.);
#16156=EDGE_CURVE('',#12729,#12773,#385,.T.);
#16157=EDGE_CURVE('',#12774,#12689,#386,.T.);
#16158=EDGE_CURVE('',#12774,#12772,#387,.T.);
#16159=EDGE_CURVE('',#12689,#12775,#10646,.T.);
#16160=EDGE_CURVE('',#12775,#12688,#10647,.T.);
#16161=EDGE_CURVE('',#12688,#12776,#388,.T.);
#16162=EDGE_CURVE('',#12776,#12774,#10648,.T.);
#16163=EDGE_CURVE('',#12776,#12771,#389,.T.);
#16164=EDGE_CURVE('',#12777,#12778,#7124,.T.);
#16165=EDGE_CURVE('',#12777,#12779,#7125,.T.);
#16166=EDGE_CURVE('',#12780,#12779,#7126,.T.);
#16167=EDGE_CURVE('',#12778,#12780,#7127,.T.);
#16168=EDGE_CURVE('',#12778,#12781,#10649,.T.);
#16169=EDGE_CURVE('',#12780,#12781,#7128,.T.);
#16170=EDGE_CURVE('',#12781,#12782,#7129,.T.);
#16171=EDGE_CURVE('',#12779,#12782,#7130,.T.);
#16172=EDGE_CURVE('',#12782,#12777,#10650,.T.);
#16173=EDGE_CURVE('',#12783,#12784,#7131,.T.);
#16174=EDGE_CURVE('',#12783,#12785,#7132,.T.);
#16175=EDGE_CURVE('',#12786,#12785,#7133,.T.);
#16176=EDGE_CURVE('',#12784,#12786,#7134,.T.);
#16177=EDGE_CURVE('',#12784,#12787,#10651,.T.);
#16178=EDGE_CURVE('',#12786,#12787,#7135,.T.);
#16179=EDGE_CURVE('',#12787,#12788,#7136,.T.);
#16180=EDGE_CURVE('',#12785,#12788,#7137,.T.);
#16181=EDGE_CURVE('',#12788,#12783,#10652,.T.);
#16182=EDGE_CURVE('',#12789,#12790,#7138,.T.);
#16183=EDGE_CURVE('',#12789,#12791,#7139,.T.);
#16184=EDGE_CURVE('',#12792,#12791,#7140,.T.);
#16185=EDGE_CURVE('',#12790,#12792,#7141,.T.);
#16186=EDGE_CURVE('',#12790,#12793,#10653,.T.);
#16187=EDGE_CURVE('',#12792,#12793,#7142,.T.);
#16188=EDGE_CURVE('',#12793,#12794,#7143,.T.);
#16189=EDGE_CURVE('',#12791,#12794,#7144,.T.);
#16190=EDGE_CURVE('',#12794,#12789,#10654,.T.);
#16191=EDGE_CURVE('',#12795,#12796,#7145,.T.);
#16192=EDGE_CURVE('',#12795,#12797,#7146,.T.);
#16193=EDGE_CURVE('',#12798,#12797,#7147,.T.);
#16194=EDGE_CURVE('',#12796,#12798,#7148,.T.);
#16195=EDGE_CURVE('',#12796,#12799,#10655,.T.);
#16196=EDGE_CURVE('',#12798,#12799,#7149,.T.);
#16197=EDGE_CURVE('',#12799,#12800,#7150,.T.);
#16198=EDGE_CURVE('',#12797,#12800,#7151,.T.);
#16199=EDGE_CURVE('',#12800,#12795,#10656,.T.);
#16200=EDGE_CURVE('',#12801,#12802,#7152,.T.);
#16201=EDGE_CURVE('',#12801,#12803,#7153,.T.);
#16202=EDGE_CURVE('',#12804,#12803,#7154,.T.);
#16203=EDGE_CURVE('',#12802,#12804,#7155,.T.);
#16204=EDGE_CURVE('',#12802,#12805,#10657,.T.);
#16205=EDGE_CURVE('',#12804,#12805,#7156,.T.);
#16206=EDGE_CURVE('',#12805,#12806,#7157,.T.);
#16207=EDGE_CURVE('',#12803,#12806,#7158,.T.);
#16208=EDGE_CURVE('',#12806,#12801,#10658,.T.);
#16209=EDGE_CURVE('',#12807,#12808,#7159,.T.);
#16210=EDGE_CURVE('',#12807,#12809,#7160,.T.);
#16211=EDGE_CURVE('',#12810,#12809,#7161,.T.);
#16212=EDGE_CURVE('',#12808,#12810,#7162,.T.);
#16213=EDGE_CURVE('',#12808,#12811,#10659,.T.);
#16214=EDGE_CURVE('',#12810,#12811,#7163,.T.);
#16215=EDGE_CURVE('',#12811,#12812,#7164,.T.);
#16216=EDGE_CURVE('',#12809,#12812,#7165,.T.);
#16217=EDGE_CURVE('',#12812,#12807,#10660,.T.);
#16218=EDGE_CURVE('',#12813,#12814,#7166,.T.);
#16219=EDGE_CURVE('',#12813,#12815,#7167,.T.);
#16220=EDGE_CURVE('',#12816,#12815,#7168,.T.);
#16221=EDGE_CURVE('',#12814,#12816,#7169,.T.);
#16222=EDGE_CURVE('',#12814,#12817,#10661,.T.);
#16223=EDGE_CURVE('',#12816,#12817,#7170,.T.);
#16224=EDGE_CURVE('',#12817,#12818,#7171,.T.);
#16225=EDGE_CURVE('',#12815,#12818,#7172,.T.);
#16226=EDGE_CURVE('',#12818,#12813,#10662,.T.);
#16227=EDGE_CURVE('',#12819,#12820,#7173,.T.);
#16228=EDGE_CURVE('',#12819,#12821,#7174,.T.);
#16229=EDGE_CURVE('',#12822,#12821,#7175,.T.);
#16230=EDGE_CURVE('',#12820,#12822,#7176,.T.);
#16231=EDGE_CURVE('',#12820,#12823,#10663,.T.);
#16232=EDGE_CURVE('',#12822,#12823,#7177,.T.);
#16233=EDGE_CURVE('',#12823,#12824,#7178,.T.);
#16234=EDGE_CURVE('',#12821,#12824,#7179,.T.);
#16235=EDGE_CURVE('',#12824,#12819,#10664,.T.);
#16236=EDGE_CURVE('',#12825,#12826,#7180,.T.);
#16237=EDGE_CURVE('',#12825,#12827,#7181,.T.);
#16238=EDGE_CURVE('',#12828,#12827,#7182,.T.);
#16239=EDGE_CURVE('',#12826,#12828,#7183,.T.);
#16240=EDGE_CURVE('',#12826,#12829,#10665,.T.);
#16241=EDGE_CURVE('',#12828,#12829,#7184,.T.);
#16242=EDGE_CURVE('',#12829,#12830,#7185,.T.);
#16243=EDGE_CURVE('',#12827,#12830,#7186,.T.);
#16244=EDGE_CURVE('',#12830,#12825,#10666,.T.);
#16245=EDGE_CURVE('',#12831,#12832,#7187,.T.);
#16246=EDGE_CURVE('',#12831,#12833,#7188,.T.);
#16247=EDGE_CURVE('',#12834,#12833,#7189,.T.);
#16248=EDGE_CURVE('',#12832,#12834,#7190,.T.);
#16249=EDGE_CURVE('',#12832,#12835,#10667,.T.);
#16250=EDGE_CURVE('',#12834,#12835,#7191,.T.);
#16251=EDGE_CURVE('',#12835,#12836,#7192,.T.);
#16252=EDGE_CURVE('',#12833,#12836,#7193,.T.);
#16253=EDGE_CURVE('',#12836,#12831,#10668,.T.);
#16254=EDGE_CURVE('',#12837,#12838,#7194,.T.);
#16255=EDGE_CURVE('',#12837,#12839,#7195,.T.);
#16256=EDGE_CURVE('',#12840,#12839,#7196,.T.);
#16257=EDGE_CURVE('',#12838,#12840,#7197,.T.);
#16258=EDGE_CURVE('',#12838,#12841,#10669,.T.);
#16259=EDGE_CURVE('',#12840,#12841,#7198,.T.);
#16260=EDGE_CURVE('',#12841,#12842,#7199,.T.);
#16261=EDGE_CURVE('',#12839,#12842,#7200,.T.);
#16262=EDGE_CURVE('',#12842,#12837,#10670,.T.);
#16263=EDGE_CURVE('',#12843,#12844,#7201,.T.);
#16264=EDGE_CURVE('',#12843,#12845,#7202,.T.);
#16265=EDGE_CURVE('',#12846,#12845,#7203,.T.);
#16266=EDGE_CURVE('',#12844,#12846,#7204,.T.);
#16267=EDGE_CURVE('',#12844,#12847,#10671,.T.);
#16268=EDGE_CURVE('',#12846,#12847,#7205,.T.);
#16269=EDGE_CURVE('',#12847,#12848,#7206,.T.);
#16270=EDGE_CURVE('',#12845,#12848,#7207,.T.);
#16271=EDGE_CURVE('',#12848,#12843,#10672,.T.);
#16272=EDGE_CURVE('',#12849,#12850,#7208,.T.);
#16273=EDGE_CURVE('',#12849,#12851,#7209,.T.);
#16274=EDGE_CURVE('',#12852,#12851,#7210,.T.);
#16275=EDGE_CURVE('',#12850,#12852,#7211,.T.);
#16276=EDGE_CURVE('',#12850,#12853,#10673,.T.);
#16277=EDGE_CURVE('',#12852,#12853,#7212,.T.);
#16278=EDGE_CURVE('',#12853,#12854,#7213,.T.);
#16279=EDGE_CURVE('',#12851,#12854,#7214,.T.);
#16280=EDGE_CURVE('',#12854,#12849,#10674,.T.);
#16281=EDGE_CURVE('',#12855,#12856,#7215,.T.);
#16282=EDGE_CURVE('',#12855,#12857,#7216,.T.);
#16283=EDGE_CURVE('',#12858,#12857,#7217,.T.);
#16284=EDGE_CURVE('',#12856,#12858,#7218,.T.);
#16285=EDGE_CURVE('',#12856,#12859,#10675,.T.);
#16286=EDGE_CURVE('',#12858,#12859,#7219,.T.);
#16287=EDGE_CURVE('',#12859,#12860,#7220,.T.);
#16288=EDGE_CURVE('',#12857,#12860,#7221,.T.);
#16289=EDGE_CURVE('',#12860,#12855,#10676,.T.);
#16290=EDGE_CURVE('',#12861,#12862,#7222,.T.);
#16291=EDGE_CURVE('',#12861,#12863,#7223,.T.);
#16292=EDGE_CURVE('',#12864,#12863,#7224,.T.);
#16293=EDGE_CURVE('',#12862,#12864,#7225,.T.);
#16294=EDGE_CURVE('',#12862,#12865,#10677,.T.);
#16295=EDGE_CURVE('',#12864,#12865,#7226,.T.);
#16296=EDGE_CURVE('',#12865,#12866,#7227,.T.);
#16297=EDGE_CURVE('',#12863,#12866,#7228,.T.);
#16298=EDGE_CURVE('',#12866,#12861,#10678,.T.);
#16299=EDGE_CURVE('',#12867,#12868,#7229,.T.);
#16300=EDGE_CURVE('',#12867,#12869,#7230,.T.);
#16301=EDGE_CURVE('',#12870,#12869,#7231,.T.);
#16302=EDGE_CURVE('',#12868,#12870,#7232,.T.);
#16303=EDGE_CURVE('',#12868,#12871,#10679,.T.);
#16304=EDGE_CURVE('',#12870,#12871,#7233,.T.);
#16305=EDGE_CURVE('',#12871,#12872,#7234,.T.);
#16306=EDGE_CURVE('',#12869,#12872,#7235,.T.);
#16307=EDGE_CURVE('',#12872,#12867,#10680,.T.);
#16308=EDGE_CURVE('',#12873,#12874,#7236,.T.);
#16309=EDGE_CURVE('',#12873,#12875,#7237,.T.);
#16310=EDGE_CURVE('',#12876,#12875,#7238,.T.);
#16311=EDGE_CURVE('',#12874,#12876,#7239,.T.);
#16312=EDGE_CURVE('',#12874,#12877,#10681,.T.);
#16313=EDGE_CURVE('',#12876,#12877,#7240,.T.);
#16314=EDGE_CURVE('',#12877,#12878,#7241,.T.);
#16315=EDGE_CURVE('',#12875,#12878,#7242,.T.);
#16316=EDGE_CURVE('',#12878,#12873,#10682,.T.);
#16317=EDGE_CURVE('',#12879,#12880,#7243,.T.);
#16318=EDGE_CURVE('',#12879,#12881,#7244,.T.);
#16319=EDGE_CURVE('',#12882,#12881,#7245,.T.);
#16320=EDGE_CURVE('',#12880,#12882,#7246,.T.);
#16321=EDGE_CURVE('',#12880,#12883,#10683,.T.);
#16322=EDGE_CURVE('',#12882,#12884,#7247,.T.);
#16323=EDGE_CURVE('',#12883,#12884,#10684,.T.);
#16324=EDGE_CURVE('',#12884,#12885,#7248,.T.);
#16325=EDGE_CURVE('',#12881,#12885,#7249,.T.);
#16326=EDGE_CURVE('',#12885,#12886,#10685,.T.);
#16327=EDGE_CURVE('',#12886,#12879,#10686,.T.);
#16328=EDGE_CURVE('',#12887,#12888,#7250,.T.);
#16329=EDGE_CURVE('',#12887,#12889,#7251,.T.);
#16330=EDGE_CURVE('',#12890,#12889,#7252,.T.);
#16331=EDGE_CURVE('',#12888,#12890,#7253,.T.);
#16332=EDGE_CURVE('',#12888,#12891,#10687,.T.);
#16333=EDGE_CURVE('',#12890,#12891,#7254,.T.);
#16334=EDGE_CURVE('',#12891,#12892,#7255,.T.);
#16335=EDGE_CURVE('',#12889,#12892,#7256,.T.);
#16336=EDGE_CURVE('',#12892,#12887,#10688,.T.);
#16337=EDGE_CURVE('',#12893,#12894,#7257,.T.);
#16338=EDGE_CURVE('',#12893,#12895,#7258,.T.);
#16339=EDGE_CURVE('',#12896,#12895,#7259,.T.);
#16340=EDGE_CURVE('',#12894,#12896,#7260,.T.);
#16341=EDGE_CURVE('',#12894,#12897,#10689,.T.);
#16342=EDGE_CURVE('',#12896,#12897,#7261,.T.);
#16343=EDGE_CURVE('',#12897,#12898,#7262,.T.);
#16344=EDGE_CURVE('',#12895,#12898,#7263,.T.);
#16345=EDGE_CURVE('',#12898,#12893,#10690,.T.);
#16346=EDGE_CURVE('',#12899,#12900,#7264,.T.);
#16347=EDGE_CURVE('',#12899,#12901,#7265,.T.);
#16348=EDGE_CURVE('',#12902,#12901,#7266,.T.);
#16349=EDGE_CURVE('',#12900,#12902,#7267,.T.);
#16350=EDGE_CURVE('',#12900,#12903,#10691,.T.);
#16351=EDGE_CURVE('',#12902,#12903,#7268,.T.);
#16352=EDGE_CURVE('',#12903,#12904,#7269,.T.);
#16353=EDGE_CURVE('',#12901,#12904,#7270,.T.);
#16354=EDGE_CURVE('',#12904,#12899,#10692,.T.);
#16355=EDGE_CURVE('',#12905,#12906,#7271,.T.);
#16356=EDGE_CURVE('',#12905,#12907,#7272,.T.);
#16357=EDGE_CURVE('',#12908,#12907,#7273,.T.);
#16358=EDGE_CURVE('',#12906,#12908,#7274,.T.);
#16359=EDGE_CURVE('',#12906,#12909,#10693,.T.);
#16360=EDGE_CURVE('',#12908,#12909,#7275,.T.);
#16361=EDGE_CURVE('',#12909,#12910,#7276,.T.);
#16362=EDGE_CURVE('',#12907,#12910,#7277,.T.);
#16363=EDGE_CURVE('',#12910,#12905,#10694,.T.);
#16364=EDGE_CURVE('',#12911,#12912,#7278,.T.);
#16365=EDGE_CURVE('',#12911,#12913,#7279,.T.);
#16366=EDGE_CURVE('',#12914,#12913,#7280,.T.);
#16367=EDGE_CURVE('',#12912,#12914,#7281,.T.);
#16368=EDGE_CURVE('',#12912,#12915,#10695,.T.);
#16369=EDGE_CURVE('',#12914,#12915,#7282,.T.);
#16370=EDGE_CURVE('',#12915,#12916,#7283,.T.);
#16371=EDGE_CURVE('',#12913,#12916,#7284,.T.);
#16372=EDGE_CURVE('',#12916,#12911,#10696,.T.);
#16373=EDGE_CURVE('',#12917,#12918,#7285,.T.);
#16374=EDGE_CURVE('',#12917,#12919,#7286,.T.);
#16375=EDGE_CURVE('',#12920,#12919,#7287,.T.);
#16376=EDGE_CURVE('',#12918,#12920,#7288,.T.);
#16377=EDGE_CURVE('',#12918,#12921,#10697,.T.);
#16378=EDGE_CURVE('',#12920,#12921,#7289,.T.);
#16379=EDGE_CURVE('',#12921,#12922,#7290,.T.);
#16380=EDGE_CURVE('',#12919,#12922,#7291,.T.);
#16381=EDGE_CURVE('',#12922,#12917,#10698,.T.);
#16382=EDGE_CURVE('',#12923,#12924,#7292,.T.);
#16383=EDGE_CURVE('',#12923,#12925,#7293,.T.);
#16384=EDGE_CURVE('',#12926,#12925,#7294,.T.);
#16385=EDGE_CURVE('',#12924,#12926,#7295,.T.);
#16386=EDGE_CURVE('',#12924,#12927,#10699,.T.);
#16387=EDGE_CURVE('',#12926,#12927,#7296,.T.);
#16388=EDGE_CURVE('',#12927,#12928,#7297,.T.);
#16389=EDGE_CURVE('',#12925,#12928,#7298,.T.);
#16390=EDGE_CURVE('',#12928,#12923,#10700,.T.);
#16391=EDGE_CURVE('',#12929,#12930,#7299,.T.);
#16392=EDGE_CURVE('',#12929,#12931,#7300,.T.);
#16393=EDGE_CURVE('',#12932,#12931,#7301,.T.);
#16394=EDGE_CURVE('',#12930,#12932,#7302,.T.);
#16395=EDGE_CURVE('',#12930,#12933,#10701,.T.);
#16396=EDGE_CURVE('',#12932,#12933,#7303,.T.);
#16397=EDGE_CURVE('',#12933,#12934,#7304,.T.);
#16398=EDGE_CURVE('',#12931,#12934,#7305,.T.);
#16399=EDGE_CURVE('',#12934,#12929,#10702,.T.);
#16400=EDGE_CURVE('',#12935,#12936,#7306,.T.);
#16401=EDGE_CURVE('',#12935,#12937,#7307,.T.);
#16402=EDGE_CURVE('',#12938,#12937,#7308,.T.);
#16403=EDGE_CURVE('',#12936,#12938,#7309,.T.);
#16404=EDGE_CURVE('',#12936,#12939,#10703,.T.);
#16405=EDGE_CURVE('',#12938,#12939,#7310,.T.);
#16406=EDGE_CURVE('',#12939,#12940,#7311,.T.);
#16407=EDGE_CURVE('',#12937,#12940,#7312,.T.);
#16408=EDGE_CURVE('',#12940,#12935,#10704,.T.);
#16409=EDGE_CURVE('',#12941,#12942,#7313,.T.);
#16410=EDGE_CURVE('',#12941,#12943,#7314,.T.);
#16411=EDGE_CURVE('',#12944,#12943,#7315,.T.);
#16412=EDGE_CURVE('',#12942,#12944,#7316,.T.);
#16413=EDGE_CURVE('',#12942,#12945,#10705,.T.);
#16414=EDGE_CURVE('',#12944,#12945,#7317,.T.);
#16415=EDGE_CURVE('',#12945,#12946,#7318,.T.);
#16416=EDGE_CURVE('',#12943,#12946,#7319,.T.);
#16417=EDGE_CURVE('',#12946,#12941,#10706,.T.);
#16418=EDGE_CURVE('',#12947,#12948,#7320,.T.);
#16419=EDGE_CURVE('',#12947,#12949,#7321,.T.);
#16420=EDGE_CURVE('',#12950,#12949,#7322,.T.);
#16421=EDGE_CURVE('',#12948,#12950,#7323,.T.);
#16422=EDGE_CURVE('',#12948,#12951,#10707,.T.);
#16423=EDGE_CURVE('',#12950,#12951,#7324,.T.);
#16424=EDGE_CURVE('',#12951,#12952,#7325,.T.);
#16425=EDGE_CURVE('',#12949,#12952,#7326,.T.);
#16426=EDGE_CURVE('',#12952,#12947,#10708,.T.);
#16427=EDGE_CURVE('',#12953,#12954,#7327,.T.);
#16428=EDGE_CURVE('',#12953,#12955,#7328,.T.);
#16429=EDGE_CURVE('',#12956,#12955,#7329,.T.);
#16430=EDGE_CURVE('',#12954,#12956,#7330,.T.);
#16431=EDGE_CURVE('',#12954,#12957,#10709,.T.);
#16432=EDGE_CURVE('',#12956,#12957,#7331,.T.);
#16433=EDGE_CURVE('',#12957,#12958,#7332,.T.);
#16434=EDGE_CURVE('',#12955,#12958,#7333,.T.);
#16435=EDGE_CURVE('',#12958,#12953,#10710,.T.);
#16436=EDGE_CURVE('',#12959,#12960,#7334,.T.);
#16437=EDGE_CURVE('',#12959,#12961,#7335,.T.);
#16438=EDGE_CURVE('',#12962,#12961,#7336,.T.);
#16439=EDGE_CURVE('',#12960,#12962,#7337,.T.);
#16440=EDGE_CURVE('',#12960,#12963,#10711,.T.);
#16441=EDGE_CURVE('',#12962,#12963,#7338,.T.);
#16442=EDGE_CURVE('',#12963,#12964,#7339,.T.);
#16443=EDGE_CURVE('',#12961,#12964,#7340,.T.);
#16444=EDGE_CURVE('',#12964,#12959,#10712,.T.);
#16445=EDGE_CURVE('',#12965,#12966,#7341,.T.);
#16446=EDGE_CURVE('',#12965,#12967,#7342,.T.);
#16447=EDGE_CURVE('',#12968,#12967,#7343,.T.);
#16448=EDGE_CURVE('',#12966,#12968,#7344,.T.);
#16449=EDGE_CURVE('',#12966,#12969,#10713,.T.);
#16450=EDGE_CURVE('',#12968,#12969,#7345,.T.);
#16451=EDGE_CURVE('',#12969,#12970,#7346,.T.);
#16452=EDGE_CURVE('',#12967,#12970,#7347,.T.);
#16453=EDGE_CURVE('',#12970,#12965,#10714,.T.);
#16454=EDGE_CURVE('',#12971,#12972,#7348,.T.);
#16455=EDGE_CURVE('',#12971,#12973,#7349,.T.);
#16456=EDGE_CURVE('',#12974,#12973,#7350,.T.);
#16457=EDGE_CURVE('',#12972,#12974,#7351,.T.);
#16458=EDGE_CURVE('',#12972,#12975,#10715,.T.);
#16459=EDGE_CURVE('',#12974,#12975,#7352,.T.);
#16460=EDGE_CURVE('',#12975,#12976,#7353,.T.);
#16461=EDGE_CURVE('',#12973,#12976,#7354,.T.);
#16462=EDGE_CURVE('',#12976,#12971,#10716,.T.);
#16463=EDGE_CURVE('',#12977,#12978,#7355,.T.);
#16464=EDGE_CURVE('',#12977,#12979,#7356,.T.);
#16465=EDGE_CURVE('',#12980,#12979,#7357,.T.);
#16466=EDGE_CURVE('',#12978,#12980,#7358,.T.);
#16467=EDGE_CURVE('',#12978,#12981,#10717,.T.);
#16468=EDGE_CURVE('',#12980,#12981,#7359,.T.);
#16469=EDGE_CURVE('',#12981,#12982,#7360,.T.);
#16470=EDGE_CURVE('',#12979,#12982,#7361,.T.);
#16471=EDGE_CURVE('',#12982,#12977,#10718,.T.);
#16472=EDGE_CURVE('',#12983,#12984,#7362,.T.);
#16473=EDGE_CURVE('',#12983,#12985,#7363,.T.);
#16474=EDGE_CURVE('',#12986,#12985,#7364,.T.);
#16475=EDGE_CURVE('',#12984,#12986,#7365,.T.);
#16476=EDGE_CURVE('',#12984,#12987,#10719,.T.);
#16477=EDGE_CURVE('',#12986,#12987,#7366,.T.);
#16478=EDGE_CURVE('',#12987,#12988,#7367,.T.);
#16479=EDGE_CURVE('',#12985,#12988,#7368,.T.);
#16480=EDGE_CURVE('',#12988,#12983,#10720,.T.);
#16481=EDGE_CURVE('',#12989,#12990,#7369,.T.);
#16482=EDGE_CURVE('',#12989,#12991,#7370,.T.);
#16483=EDGE_CURVE('',#12992,#12991,#7371,.T.);
#16484=EDGE_CURVE('',#12990,#12992,#7372,.T.);
#16485=EDGE_CURVE('',#12990,#12993,#10721,.T.);
#16486=EDGE_CURVE('',#12992,#12993,#7373,.T.);
#16487=EDGE_CURVE('',#12993,#12994,#7374,.T.);
#16488=EDGE_CURVE('',#12991,#12994,#7375,.T.);
#16489=EDGE_CURVE('',#12994,#12989,#10722,.T.);
#16490=EDGE_CURVE('',#12995,#12996,#7376,.T.);
#16491=EDGE_CURVE('',#12995,#12997,#7377,.T.);
#16492=EDGE_CURVE('',#12997,#12998,#7378,.T.);
#16493=EDGE_CURVE('',#12996,#12998,#7379,.T.);
#16494=EDGE_CURVE('',#12999,#12995,#7380,.T.);
#16495=EDGE_CURVE('',#12999,#13000,#7381,.T.);
#16496=EDGE_CURVE('',#13000,#12997,#7382,.T.);
#16497=EDGE_CURVE('',#13001,#12999,#7383,.T.);
#16498=EDGE_CURVE('',#13001,#13002,#7384,.T.);
#16499=EDGE_CURVE('',#13002,#13000,#7385,.T.);
#16500=EDGE_CURVE('',#13003,#13001,#7386,.T.);
#16501=EDGE_CURVE('',#13003,#13004,#7387,.T.);
#16502=EDGE_CURVE('',#13004,#13002,#7388,.T.);
#16503=EDGE_CURVE('',#13005,#13003,#7389,.T.);
#16504=EDGE_CURVE('',#13005,#13006,#7390,.T.);
#16505=EDGE_CURVE('',#13006,#13004,#7391,.T.);
#16506=EDGE_CURVE('',#12996,#13005,#7392,.T.);
#16507=EDGE_CURVE('',#12998,#13006,#7393,.T.);
#16508=EDGE_CURVE('',#13007,#13007,#10723,.T.);
#16509=EDGE_CURVE('',#12775,#13007,#7394,.T.);
#16510=EDGE_CURVE('',#12728,#12773,#10724,.F.);
#16511=EDGE_CURVE('',#13008,#13008,#10725,.T.);
#16512=EDGE_CURVE('',#13008,#12728,#7395,.T.);
#16513=EDGE_CURVE('',#13009,#13009,#10726,.T.);
#16514=EDGE_CURVE('',#13009,#13008,#7396,.T.);
#16515=EDGE_CURVE('',#13010,#13010,#10727,.T.);
#16516=EDGE_CURVE('',#13011,#13011,#10728,.T.);
#16517=EDGE_CURVE('',#13011,#12886,#7397,.T.);
#16518=EDGE_CURVE('',#12883,#13010,#7398,.T.);
#16519=EDGE_CURVE('',#13012,#13012,#10729,.T.);
#16520=EDGE_CURVE('',#13012,#13011,#7399,.T.);
#22548=ORIENTED_EDGE('',*,*,#16027,.F.);
#22549=ORIENTED_EDGE('',*,*,#16028,.T.);
#22550=ORIENTED_EDGE('',*,*,#16029,.T.);
#22551=ORIENTED_EDGE('',*,*,#16030,.T.);
#22552=ORIENTED_EDGE('',*,*,#16031,.F.);
#22553=ORIENTED_EDGE('',*,*,#16032,.T.);
#22554=ORIENTED_EDGE('',*,*,#16027,.T.);
#22555=ORIENTED_EDGE('',*,*,#16033,.T.);
#22556=ORIENTED_EDGE('',*,*,#16034,.F.);
#22557=ORIENTED_EDGE('',*,*,#16035,.T.);
#22558=ORIENTED_EDGE('',*,*,#16031,.T.);
#22559=ORIENTED_EDGE('',*,*,#16036,.T.);
#22560=ORIENTED_EDGE('',*,*,#16037,.F.);
#22561=ORIENTED_EDGE('',*,*,#16038,.T.);
#22562=ORIENTED_EDGE('',*,*,#16034,.T.);
#22563=ORIENTED_EDGE('',*,*,#16039,.T.);
#22564=ORIENTED_EDGE('',*,*,#16040,.F.);
#22565=ORIENTED_EDGE('',*,*,#16041,.T.);
#22566=ORIENTED_EDGE('',*,*,#16037,.T.);
#22567=ORIENTED_EDGE('',*,*,#16042,.T.);
#22568=ORIENTED_EDGE('',*,*,#16043,.F.);
#22569=ORIENTED_EDGE('',*,*,#16044,.T.);
#22570=ORIENTED_EDGE('',*,*,#16040,.T.);
#22571=ORIENTED_EDGE('',*,*,#16045,.T.);
#22572=ORIENTED_EDGE('',*,*,#16046,.F.);
#22573=ORIENTED_EDGE('',*,*,#16047,.T.);
#22574=ORIENTED_EDGE('',*,*,#16043,.T.);
#22575=ORIENTED_EDGE('',*,*,#16048,.T.);
#22576=ORIENTED_EDGE('',*,*,#16049,.F.);
#22577=ORIENTED_EDGE('',*,*,#16050,.T.);
#22578=ORIENTED_EDGE('',*,*,#16046,.T.);
#22579=ORIENTED_EDGE('',*,*,#16051,.T.);
#22580=ORIENTED_EDGE('',*,*,#16052,.F.);
#22581=ORIENTED_EDGE('',*,*,#16053,.T.);
#22582=ORIENTED_EDGE('',*,*,#16049,.T.);
#22583=ORIENTED_EDGE('',*,*,#16054,.T.);
#22584=ORIENTED_EDGE('',*,*,#16055,.F.);
#22585=ORIENTED_EDGE('',*,*,#16056,.T.);
#22586=ORIENTED_EDGE('',*,*,#16052,.T.);
#22587=ORIENTED_EDGE('',*,*,#16057,.T.);
#22588=ORIENTED_EDGE('',*,*,#16058,.F.);
#22589=ORIENTED_EDGE('',*,*,#16059,.T.);
#22590=ORIENTED_EDGE('',*,*,#16055,.T.);
#22591=ORIENTED_EDGE('',*,*,#16060,.T.);
#22592=ORIENTED_EDGE('',*,*,#16061,.F.);
#22593=ORIENTED_EDGE('',*,*,#16062,.T.);
#22594=ORIENTED_EDGE('',*,*,#16058,.T.);
#22595=ORIENTED_EDGE('',*,*,#16063,.T.);
#22596=ORIENTED_EDGE('',*,*,#16064,.F.);
#22597=ORIENTED_EDGE('',*,*,#16065,.T.);
#22598=ORIENTED_EDGE('',*,*,#16061,.T.);
#22599=ORIENTED_EDGE('',*,*,#16066,.T.);
#22600=ORIENTED_EDGE('',*,*,#16067,.F.);
#22601=ORIENTED_EDGE('',*,*,#16068,.T.);
#22602=ORIENTED_EDGE('',*,*,#16064,.T.);
#22603=ORIENTED_EDGE('',*,*,#16069,.T.);
#22604=ORIENTED_EDGE('',*,*,#16070,.F.);
#22605=ORIENTED_EDGE('',*,*,#16071,.T.);
#22606=ORIENTED_EDGE('',*,*,#16067,.T.);
#22607=ORIENTED_EDGE('',*,*,#16072,.T.);
#22608=ORIENTED_EDGE('',*,*,#16073,.F.);
#22609=ORIENTED_EDGE('',*,*,#16074,.T.);
#22610=ORIENTED_EDGE('',*,*,#16070,.T.);
#22611=ORIENTED_EDGE('',*,*,#16075,.T.);
#22612=ORIENTED_EDGE('',*,*,#16076,.F.);
#22613=ORIENTED_EDGE('',*,*,#16077,.T.);
#22614=ORIENTED_EDGE('',*,*,#16073,.T.);
#22615=ORIENTED_EDGE('',*,*,#16078,.T.);
#22616=ORIENTED_EDGE('',*,*,#16079,.F.);
#22617=ORIENTED_EDGE('',*,*,#16080,.T.);
#22618=ORIENTED_EDGE('',*,*,#16076,.T.);
#22619=ORIENTED_EDGE('',*,*,#16081,.T.);
#22620=ORIENTED_EDGE('',*,*,#16082,.F.);
#22621=ORIENTED_EDGE('',*,*,#16083,.T.);
#22622=ORIENTED_EDGE('',*,*,#16079,.T.);
#22623=ORIENTED_EDGE('',*,*,#16084,.T.);
#22624=ORIENTED_EDGE('',*,*,#16085,.F.);
#22625=ORIENTED_EDGE('',*,*,#16086,.T.);
#22626=ORIENTED_EDGE('',*,*,#16082,.T.);
#22627=ORIENTED_EDGE('',*,*,#16087,.T.);
#22628=ORIENTED_EDGE('',*,*,#16088,.F.);
#22629=ORIENTED_EDGE('',*,*,#16089,.F.);
#22630=ORIENTED_EDGE('',*,*,#16090,.T.);
#22631=ORIENTED_EDGE('',*,*,#16085,.T.);
#22632=ORIENTED_EDGE('',*,*,#16091,.T.);
#22633=ORIENTED_EDGE('',*,*,#16092,.F.);
#22634=ORIENTED_EDGE('',*,*,#16093,.T.);
#22635=ORIENTED_EDGE('',*,*,#16094,.F.);
#22636=ORIENTED_EDGE('',*,*,#16095,.F.);
#22637=ORIENTED_EDGE('',*,*,#16096,.F.);
#22638=ORIENTED_EDGE('',*,*,#16097,.T.);
#22639=ORIENTED_EDGE('',*,*,#16092,.T.);
#22640=ORIENTED_EDGE('',*,*,#16098,.F.);
#22641=ORIENTED_EDGE('',*,*,#16099,.F.);
#22642=ORIENTED_EDGE('',*,*,#16100,.T.);
#22643=ORIENTED_EDGE('',*,*,#16096,.T.);
#22644=ORIENTED_EDGE('',*,*,#16101,.F.);
#22645=ORIENTED_EDGE('',*,*,#16102,.F.);
#22646=ORIENTED_EDGE('',*,*,#16103,.T.);
#22647=ORIENTED_EDGE('',*,*,#16099,.T.);
#22648=ORIENTED_EDGE('',*,*,#16104,.F.);
#22649=ORIENTED_EDGE('',*,*,#16105,.F.);
#22650=ORIENTED_EDGE('',*,*,#16106,.T.);
#22651=ORIENTED_EDGE('',*,*,#16102,.T.);
#22652=ORIENTED_EDGE('',*,*,#16107,.F.);
#22653=ORIENTED_EDGE('',*,*,#16108,.F.);
#22654=ORIENTED_EDGE('',*,*,#16109,.T.);
#22655=ORIENTED_EDGE('',*,*,#16105,.T.);
#22656=ORIENTED_EDGE('',*,*,#16110,.F.);
#22657=ORIENTED_EDGE('',*,*,#16111,.F.);
#22658=ORIENTED_EDGE('',*,*,#16112,.T.);
#22659=ORIENTED_EDGE('',*,*,#16108,.T.);
#22660=ORIENTED_EDGE('',*,*,#16113,.F.);
#22661=ORIENTED_EDGE('',*,*,#16114,.F.);
#22662=ORIENTED_EDGE('',*,*,#16115,.T.);
#22663=ORIENTED_EDGE('',*,*,#16111,.T.);
#22664=ORIENTED_EDGE('',*,*,#16116,.F.);
#22665=ORIENTED_EDGE('',*,*,#16117,.F.);
#22666=ORIENTED_EDGE('',*,*,#16118,.T.);
#22667=ORIENTED_EDGE('',*,*,#16114,.T.);
#22668=ORIENTED_EDGE('',*,*,#16119,.F.);
#22669=ORIENTED_EDGE('',*,*,#16120,.F.);
#22670=ORIENTED_EDGE('',*,*,#16121,.T.);
#22671=ORIENTED_EDGE('',*,*,#16117,.T.);
#22672=ORIENTED_EDGE('',*,*,#16122,.F.);
#22673=ORIENTED_EDGE('',*,*,#16123,.F.);
#22674=ORIENTED_EDGE('',*,*,#16124,.T.);
#22675=ORIENTED_EDGE('',*,*,#16120,.T.);
#22676=ORIENTED_EDGE('',*,*,#16125,.F.);
#22677=ORIENTED_EDGE('',*,*,#16126,.F.);
#22678=ORIENTED_EDGE('',*,*,#16127,.T.);
#22679=ORIENTED_EDGE('',*,*,#16123,.T.);
#22680=ORIENTED_EDGE('',*,*,#16128,.F.);
#22681=ORIENTED_EDGE('',*,*,#16129,.F.);
#22682=ORIENTED_EDGE('',*,*,#16130,.T.);
#22683=ORIENTED_EDGE('',*,*,#16126,.T.);
#22684=ORIENTED_EDGE('',*,*,#16131,.F.);
#22685=ORIENTED_EDGE('',*,*,#16132,.F.);
#22686=ORIENTED_EDGE('',*,*,#16133,.T.);
#22687=ORIENTED_EDGE('',*,*,#16129,.T.);
#22688=ORIENTED_EDGE('',*,*,#16134,.F.);
#22689=ORIENTED_EDGE('',*,*,#16135,.F.);
#22690=ORIENTED_EDGE('',*,*,#16136,.T.);
#22691=ORIENTED_EDGE('',*,*,#16132,.T.);
#22692=ORIENTED_EDGE('',*,*,#16137,.F.);
#22693=ORIENTED_EDGE('',*,*,#16138,.F.);
#22694=ORIENTED_EDGE('',*,*,#16139,.T.);
#22695=ORIENTED_EDGE('',*,*,#16135,.T.);
#22696=ORIENTED_EDGE('',*,*,#16140,.F.);
#22697=ORIENTED_EDGE('',*,*,#16141,.F.);
#22698=ORIENTED_EDGE('',*,*,#16142,.T.);
#22699=ORIENTED_EDGE('',*,*,#16138,.T.);
#22700=ORIENTED_EDGE('',*,*,#16143,.F.);
#22701=ORIENTED_EDGE('',*,*,#16144,.F.);
#22702=ORIENTED_EDGE('',*,*,#16145,.T.);
#22703=ORIENTED_EDGE('',*,*,#16141,.T.);
#22704=ORIENTED_EDGE('',*,*,#16146,.F.);
#22705=ORIENTED_EDGE('',*,*,#16147,.F.);
#22706=ORIENTED_EDGE('',*,*,#16148,.T.);
#22707=ORIENTED_EDGE('',*,*,#16144,.T.);
#22708=ORIENTED_EDGE('',*,*,#16149,.F.);
#22709=ORIENTED_EDGE('',*,*,#16150,.F.);
#22710=ORIENTED_EDGE('',*,*,#16151,.T.);
#22711=ORIENTED_EDGE('',*,*,#16147,.T.);
#22712=ORIENTED_EDGE('',*,*,#16152,.F.);
#22713=ORIENTED_EDGE('',*,*,#16094,.T.);
#22714=ORIENTED_EDGE('',*,*,#16153,.T.);
#22715=ORIENTED_EDGE('',*,*,#16154,.F.);
#22716=ORIENTED_EDGE('',*,*,#16155,.T.);
#22717=ORIENTED_EDGE('',*,*,#16155,.F.);
#22718=ORIENTED_EDGE('',*,*,#16156,.F.);
#22719=ORIENTED_EDGE('',*,*,#16091,.F.);
#22720=ORIENTED_EDGE('',*,*,#16087,.F.);
#22721=ORIENTED_EDGE('',*,*,#16084,.F.);
#22722=ORIENTED_EDGE('',*,*,#16081,.F.);
#22723=ORIENTED_EDGE('',*,*,#16078,.F.);
#22724=ORIENTED_EDGE('',*,*,#16075,.F.);
#22725=ORIENTED_EDGE('',*,*,#16072,.F.);
#22726=ORIENTED_EDGE('',*,*,#16069,.F.);
#22727=ORIENTED_EDGE('',*,*,#16066,.F.);
#22728=ORIENTED_EDGE('',*,*,#16063,.F.);
#22729=ORIENTED_EDGE('',*,*,#16060,.F.);
#22730=ORIENTED_EDGE('',*,*,#16057,.F.);
#22731=ORIENTED_EDGE('',*,*,#16054,.F.);
#22732=ORIENTED_EDGE('',*,*,#16051,.F.);
#22733=ORIENTED_EDGE('',*,*,#16048,.F.);
#22734=ORIENTED_EDGE('',*,*,#16045,.F.);
#22735=ORIENTED_EDGE('',*,*,#16042,.F.);
#22736=ORIENTED_EDGE('',*,*,#16039,.F.);
#22737=ORIENTED_EDGE('',*,*,#16036,.F.);
#22738=ORIENTED_EDGE('',*,*,#16033,.F.);
#22739=ORIENTED_EDGE('',*,*,#16030,.F.);
#22740=ORIENTED_EDGE('',*,*,#16157,.F.);
#22741=ORIENTED_EDGE('',*,*,#16158,.T.);
#22742=ORIENTED_EDGE('',*,*,#16152,.T.);
#22743=ORIENTED_EDGE('',*,*,#16149,.T.);
#22744=ORIENTED_EDGE('',*,*,#16146,.T.);
#22745=ORIENTED_EDGE('',*,*,#16143,.T.);
#22746=ORIENTED_EDGE('',*,*,#16140,.T.);
#22747=ORIENTED_EDGE('',*,*,#16137,.T.);
#22748=ORIENTED_EDGE('',*,*,#16134,.T.);
#22749=ORIENTED_EDGE('',*,*,#16131,.T.);
#22750=ORIENTED_EDGE('',*,*,#16128,.T.);
#22751=ORIENTED_EDGE('',*,*,#16125,.T.);
#22752=ORIENTED_EDGE('',*,*,#16122,.T.);
#22753=ORIENTED_EDGE('',*,*,#16119,.T.);
#22754=ORIENTED_EDGE('',*,*,#16116,.T.);
#22755=ORIENTED_EDGE('',*,*,#16113,.T.);
#22756=ORIENTED_EDGE('',*,*,#16110,.T.);
#22757=ORIENTED_EDGE('',*,*,#16107,.T.);
#22758=ORIENTED_EDGE('',*,*,#16104,.T.);
#22759=ORIENTED_EDGE('',*,*,#16101,.T.);
#22760=ORIENTED_EDGE('',*,*,#16098,.T.);
#22761=ORIENTED_EDGE('',*,*,#16095,.T.);
#22762=ORIENTED_EDGE('',*,*,#16159,.T.);
#22763=ORIENTED_EDGE('',*,*,#16160,.T.);
#22764=ORIENTED_EDGE('',*,*,#16161,.T.);
#22765=ORIENTED_EDGE('',*,*,#16162,.T.);
#22766=ORIENTED_EDGE('',*,*,#16157,.T.);
#22767=ORIENTED_EDGE('',*,*,#16150,.T.);
#22768=ORIENTED_EDGE('',*,*,#16158,.F.);
#22769=ORIENTED_EDGE('',*,*,#16162,.F.);
#22770=ORIENTED_EDGE('',*,*,#16163,.T.);
#22771=ORIENTED_EDGE('',*,*,#16153,.F.);
#22772=ORIENTED_EDGE('',*,*,#16093,.F.);
#22773=ORIENTED_EDGE('',*,*,#16097,.F.);
#22774=ORIENTED_EDGE('',*,*,#16100,.F.);
#22775=ORIENTED_EDGE('',*,*,#16103,.F.);
#22776=ORIENTED_EDGE('',*,*,#16106,.F.);
#22777=ORIENTED_EDGE('',*,*,#16109,.F.);
#22778=ORIENTED_EDGE('',*,*,#16112,.F.);
#22779=ORIENTED_EDGE('',*,*,#16115,.F.);
#22780=ORIENTED_EDGE('',*,*,#16118,.F.);
#22781=ORIENTED_EDGE('',*,*,#16121,.F.);
#22782=ORIENTED_EDGE('',*,*,#16124,.F.);
#22783=ORIENTED_EDGE('',*,*,#16127,.F.);
#22784=ORIENTED_EDGE('',*,*,#16130,.F.);
#22785=ORIENTED_EDGE('',*,*,#16133,.F.);
#22786=ORIENTED_EDGE('',*,*,#16136,.F.);
#22787=ORIENTED_EDGE('',*,*,#16139,.F.);
#22788=ORIENTED_EDGE('',*,*,#16142,.F.);
#22789=ORIENTED_EDGE('',*,*,#16145,.F.);
#22790=ORIENTED_EDGE('',*,*,#16148,.F.);
#22791=ORIENTED_EDGE('',*,*,#16151,.F.);
#22792=ORIENTED_EDGE('',*,*,#16163,.F.);
#22793=ORIENTED_EDGE('',*,*,#16161,.F.);
#22794=ORIENTED_EDGE('',*,*,#16028,.F.);
#22795=ORIENTED_EDGE('',*,*,#16032,.F.);
#22796=ORIENTED_EDGE('',*,*,#16035,.F.);
#22797=ORIENTED_EDGE('',*,*,#16038,.F.);
#22798=ORIENTED_EDGE('',*,*,#16041,.F.);
#22799=ORIENTED_EDGE('',*,*,#16044,.F.);
#22800=ORIENTED_EDGE('',*,*,#16047,.F.);
#22801=ORIENTED_EDGE('',*,*,#16050,.F.);
#22802=ORIENTED_EDGE('',*,*,#16053,.F.);
#22803=ORIENTED_EDGE('',*,*,#16056,.F.);
#22804=ORIENTED_EDGE('',*,*,#16059,.F.);
#22805=ORIENTED_EDGE('',*,*,#16062,.F.);
#22806=ORIENTED_EDGE('',*,*,#16065,.F.);
#22807=ORIENTED_EDGE('',*,*,#16068,.F.);
#22808=ORIENTED_EDGE('',*,*,#16071,.F.);
#22809=ORIENTED_EDGE('',*,*,#16074,.F.);
#22810=ORIENTED_EDGE('',*,*,#16077,.F.);
#22811=ORIENTED_EDGE('',*,*,#16080,.F.);
#22812=ORIENTED_EDGE('',*,*,#16083,.F.);
#22813=ORIENTED_EDGE('',*,*,#16086,.F.);
#22814=ORIENTED_EDGE('',*,*,#16090,.F.);
#22815=ORIENTED_EDGE('',*,*,#16164,.F.);
#22816=ORIENTED_EDGE('',*,*,#16165,.T.);
#22817=ORIENTED_EDGE('',*,*,#16166,.F.);
#22818=ORIENTED_EDGE('',*,*,#16167,.F.);
#22819=ORIENTED_EDGE('',*,*,#16168,.F.);
#22820=ORIENTED_EDGE('',*,*,#16167,.T.);
#22821=ORIENTED_EDGE('',*,*,#16169,.T.);
#22822=ORIENTED_EDGE('',*,*,#16170,.F.);
#22823=ORIENTED_EDGE('',*,*,#16169,.F.);
#22824=ORIENTED_EDGE('',*,*,#16166,.T.);
#22825=ORIENTED_EDGE('',*,*,#16171,.T.);
#22826=ORIENTED_EDGE('',*,*,#16172,.F.);
#22827=ORIENTED_EDGE('',*,*,#16171,.F.);
#22828=ORIENTED_EDGE('',*,*,#16165,.F.);
#22829=ORIENTED_EDGE('',*,*,#16173,.F.);
#22830=ORIENTED_EDGE('',*,*,#16174,.T.);
#22831=ORIENTED_EDGE('',*,*,#16175,.F.);
#22832=ORIENTED_EDGE('',*,*,#16176,.F.);
#22833=ORIENTED_EDGE('',*,*,#16177,.F.);
#22834=ORIENTED_EDGE('',*,*,#16176,.T.);
#22835=ORIENTED_EDGE('',*,*,#16178,.T.);
#22836=ORIENTED_EDGE('',*,*,#16179,.F.);
#22837=ORIENTED_EDGE('',*,*,#16178,.F.);
#22838=ORIENTED_EDGE('',*,*,#16175,.T.);
#22839=ORIENTED_EDGE('',*,*,#16180,.T.);
#22840=ORIENTED_EDGE('',*,*,#16181,.F.);
#22841=ORIENTED_EDGE('',*,*,#16180,.F.);
#22842=ORIENTED_EDGE('',*,*,#16174,.F.);
#22843=ORIENTED_EDGE('',*,*,#16182,.F.);
#22844=ORIENTED_EDGE('',*,*,#16183,.T.);
#22845=ORIENTED_EDGE('',*,*,#16184,.F.);
#22846=ORIENTED_EDGE('',*,*,#16185,.F.);
#22847=ORIENTED_EDGE('',*,*,#16186,.F.);
#22848=ORIENTED_EDGE('',*,*,#16185,.T.);
#22849=ORIENTED_EDGE('',*,*,#16187,.T.);
#22850=ORIENTED_EDGE('',*,*,#16188,.F.);
#22851=ORIENTED_EDGE('',*,*,#16187,.F.);
#22852=ORIENTED_EDGE('',*,*,#16184,.T.);
#22853=ORIENTED_EDGE('',*,*,#16189,.T.);
#22854=ORIENTED_EDGE('',*,*,#16190,.F.);
#22855=ORIENTED_EDGE('',*,*,#16189,.F.);
#22856=ORIENTED_EDGE('',*,*,#16183,.F.);
#22857=ORIENTED_EDGE('',*,*,#16191,.F.);
#22858=ORIENTED_EDGE('',*,*,#16192,.T.);
#22859=ORIENTED_EDGE('',*,*,#16193,.F.);
#22860=ORIENTED_EDGE('',*,*,#16194,.F.);
#22861=ORIENTED_EDGE('',*,*,#16195,.F.);
#22862=ORIENTED_EDGE('',*,*,#16194,.T.);
#22863=ORIENTED_EDGE('',*,*,#16196,.T.);
#22864=ORIENTED_EDGE('',*,*,#16197,.F.);
#22865=ORIENTED_EDGE('',*,*,#16196,.F.);
#22866=ORIENTED_EDGE('',*,*,#16193,.T.);
#22867=ORIENTED_EDGE('',*,*,#16198,.T.);
#22868=ORIENTED_EDGE('',*,*,#16199,.F.);
#22869=ORIENTED_EDGE('',*,*,#16198,.F.);
#22870=ORIENTED_EDGE('',*,*,#16192,.F.);
#22871=ORIENTED_EDGE('',*,*,#16200,.F.);
#22872=ORIENTED_EDGE('',*,*,#16201,.T.);
#22873=ORIENTED_EDGE('',*,*,#16202,.F.);
#22874=ORIENTED_EDGE('',*,*,#16203,.F.);
#22875=ORIENTED_EDGE('',*,*,#16204,.F.);
#22876=ORIENTED_EDGE('',*,*,#16203,.T.);
#22877=ORIENTED_EDGE('',*,*,#16205,.T.);
#22878=ORIENTED_EDGE('',*,*,#16206,.F.);
#22879=ORIENTED_EDGE('',*,*,#16205,.F.);
#22880=ORIENTED_EDGE('',*,*,#16202,.T.);
#22881=ORIENTED_EDGE('',*,*,#16207,.T.);
#22882=ORIENTED_EDGE('',*,*,#16208,.F.);
#22883=ORIENTED_EDGE('',*,*,#16207,.F.);
#22884=ORIENTED_EDGE('',*,*,#16201,.F.);
#22885=ORIENTED_EDGE('',*,*,#16209,.F.);
#22886=ORIENTED_EDGE('',*,*,#16210,.T.);
#22887=ORIENTED_EDGE('',*,*,#16211,.F.);
#22888=ORIENTED_EDGE('',*,*,#16212,.F.);
#22889=ORIENTED_EDGE('',*,*,#16213,.F.);
#22890=ORIENTED_EDGE('',*,*,#16212,.T.);
#22891=ORIENTED_EDGE('',*,*,#16214,.T.);
#22892=ORIENTED_EDGE('',*,*,#16215,.F.);
#22893=ORIENTED_EDGE('',*,*,#16214,.F.);
#22894=ORIENTED_EDGE('',*,*,#16211,.T.);
#22895=ORIENTED_EDGE('',*,*,#16216,.T.);
#22896=ORIENTED_EDGE('',*,*,#16217,.F.);
#22897=ORIENTED_EDGE('',*,*,#16216,.F.);
#22898=ORIENTED_EDGE('',*,*,#16210,.F.);
#22899=ORIENTED_EDGE('',*,*,#16218,.F.);
#22900=ORIENTED_EDGE('',*,*,#16219,.T.);
#22901=ORIENTED_EDGE('',*,*,#16220,.F.);
#22902=ORIENTED_EDGE('',*,*,#16221,.F.);
#22903=ORIENTED_EDGE('',*,*,#16222,.F.);
#22904=ORIENTED_EDGE('',*,*,#16221,.T.);
#22905=ORIENTED_EDGE('',*,*,#16223,.T.);
#22906=ORIENTED_EDGE('',*,*,#16224,.F.);
#22907=ORIENTED_EDGE('',*,*,#16223,.F.);
#22908=ORIENTED_EDGE('',*,*,#16220,.T.);
#22909=ORIENTED_EDGE('',*,*,#16225,.T.);
#22910=ORIENTED_EDGE('',*,*,#16226,.F.);
#22911=ORIENTED_EDGE('',*,*,#16225,.F.);
#22912=ORIENTED_EDGE('',*,*,#16219,.F.);
#22913=ORIENTED_EDGE('',*,*,#16227,.F.);
#22914=ORIENTED_EDGE('',*,*,#16228,.T.);
#22915=ORIENTED_EDGE('',*,*,#16229,.F.);
#22916=ORIENTED_EDGE('',*,*,#16230,.F.);
#22917=ORIENTED_EDGE('',*,*,#16231,.F.);
#22918=ORIENTED_EDGE('',*,*,#16230,.T.);
#22919=ORIENTED_EDGE('',*,*,#16232,.T.);
#22920=ORIENTED_EDGE('',*,*,#16233,.F.);
#22921=ORIENTED_EDGE('',*,*,#16232,.F.);
#22922=ORIENTED_EDGE('',*,*,#16229,.T.);
#22923=ORIENTED_EDGE('',*,*,#16234,.T.);
#22924=ORIENTED_EDGE('',*,*,#16235,.F.);
#22925=ORIENTED_EDGE('',*,*,#16234,.F.);
#22926=ORIENTED_EDGE('',*,*,#16228,.F.);
#22927=ORIENTED_EDGE('',*,*,#16236,.F.);
#22928=ORIENTED_EDGE('',*,*,#16237,.T.);
#22929=ORIENTED_EDGE('',*,*,#16238,.F.);
#22930=ORIENTED_EDGE('',*,*,#16239,.F.);
#22931=ORIENTED_EDGE('',*,*,#16240,.F.);
#22932=ORIENTED_EDGE('',*,*,#16239,.T.);
#22933=ORIENTED_EDGE('',*,*,#16241,.T.);
#22934=ORIENTED_EDGE('',*,*,#16242,.F.);
#22935=ORIENTED_EDGE('',*,*,#16241,.F.);
#22936=ORIENTED_EDGE('',*,*,#16238,.T.);
#22937=ORIENTED_EDGE('',*,*,#16243,.T.);
#22938=ORIENTED_EDGE('',*,*,#16244,.F.);
#22939=ORIENTED_EDGE('',*,*,#16243,.F.);
#22940=ORIENTED_EDGE('',*,*,#16237,.F.);
#22941=ORIENTED_EDGE('',*,*,#16245,.F.);
#22942=ORIENTED_EDGE('',*,*,#16246,.T.);
#22943=ORIENTED_EDGE('',*,*,#16247,.F.);
#22944=ORIENTED_EDGE('',*,*,#16248,.F.);
#22945=ORIENTED_EDGE('',*,*,#16249,.F.);
#22946=ORIENTED_EDGE('',*,*,#16248,.T.);
#22947=ORIENTED_EDGE('',*,*,#16250,.T.);
#22948=ORIENTED_EDGE('',*,*,#16251,.F.);
#22949=ORIENTED_EDGE('',*,*,#16250,.F.);
#22950=ORIENTED_EDGE('',*,*,#16247,.T.);
#22951=ORIENTED_EDGE('',*,*,#16252,.T.);
#22952=ORIENTED_EDGE('',*,*,#16253,.F.);
#22953=ORIENTED_EDGE('',*,*,#16252,.F.);
#22954=ORIENTED_EDGE('',*,*,#16246,.F.);
#22955=ORIENTED_EDGE('',*,*,#16254,.F.);
#22956=ORIENTED_EDGE('',*,*,#16255,.T.);
#22957=ORIENTED_EDGE('',*,*,#16256,.F.);
#22958=ORIENTED_EDGE('',*,*,#16257,.F.);
#22959=ORIENTED_EDGE('',*,*,#16258,.F.);
#22960=ORIENTED_EDGE('',*,*,#16257,.T.);
#22961=ORIENTED_EDGE('',*,*,#16259,.T.);
#22962=ORIENTED_EDGE('',*,*,#16260,.F.);
#22963=ORIENTED_EDGE('',*,*,#16259,.F.);
#22964=ORIENTED_EDGE('',*,*,#16256,.T.);
#22965=ORIENTED_EDGE('',*,*,#16261,.T.);
#22966=ORIENTED_EDGE('',*,*,#16262,.F.);
#22967=ORIENTED_EDGE('',*,*,#16261,.F.);
#22968=ORIENTED_EDGE('',*,*,#16255,.F.);
#22969=ORIENTED_EDGE('',*,*,#16263,.F.);
#22970=ORIENTED_EDGE('',*,*,#16264,.T.);
#22971=ORIENTED_EDGE('',*,*,#16265,.F.);
#22972=ORIENTED_EDGE('',*,*,#16266,.F.);
#22973=ORIENTED_EDGE('',*,*,#16267,.F.);
#22974=ORIENTED_EDGE('',*,*,#16266,.T.);
#22975=ORIENTED_EDGE('',*,*,#16268,.T.);
#22976=ORIENTED_EDGE('',*,*,#16269,.F.);
#22977=ORIENTED_EDGE('',*,*,#16268,.F.);
#22978=ORIENTED_EDGE('',*,*,#16265,.T.);
#22979=ORIENTED_EDGE('',*,*,#16270,.T.);
#22980=ORIENTED_EDGE('',*,*,#16271,.F.);
#22981=ORIENTED_EDGE('',*,*,#16270,.F.);
#22982=ORIENTED_EDGE('',*,*,#16264,.F.);
#22983=ORIENTED_EDGE('',*,*,#16272,.F.);
#22984=ORIENTED_EDGE('',*,*,#16273,.T.);
#22985=ORIENTED_EDGE('',*,*,#16274,.F.);
#22986=ORIENTED_EDGE('',*,*,#16275,.F.);
#22987=ORIENTED_EDGE('',*,*,#16276,.F.);
#22988=ORIENTED_EDGE('',*,*,#16275,.T.);
#22989=ORIENTED_EDGE('',*,*,#16277,.T.);
#22990=ORIENTED_EDGE('',*,*,#16278,.F.);
#22991=ORIENTED_EDGE('',*,*,#16277,.F.);
#22992=ORIENTED_EDGE('',*,*,#16274,.T.);
#22993=ORIENTED_EDGE('',*,*,#16279,.T.);
#22994=ORIENTED_EDGE('',*,*,#16280,.F.);
#22995=ORIENTED_EDGE('',*,*,#16279,.F.);
#22996=ORIENTED_EDGE('',*,*,#16273,.F.);
#22997=ORIENTED_EDGE('',*,*,#16281,.F.);
#22998=ORIENTED_EDGE('',*,*,#16282,.T.);
#22999=ORIENTED_EDGE('',*,*,#16283,.F.);
#23000=ORIENTED_EDGE('',*,*,#16284,.F.);
#23001=ORIENTED_EDGE('',*,*,#16285,.F.);
#23002=ORIENTED_EDGE('',*,*,#16284,.T.);
#23003=ORIENTED_EDGE('',*,*,#16286,.T.);
#23004=ORIENTED_EDGE('',*,*,#16287,.F.);
#23005=ORIENTED_EDGE('',*,*,#16286,.F.);
#23006=ORIENTED_EDGE('',*,*,#16283,.T.);
#23007=ORIENTED_EDGE('',*,*,#16288,.T.);
#23008=ORIENTED_EDGE('',*,*,#16289,.F.);
#23009=ORIENTED_EDGE('',*,*,#16288,.F.);
#23010=ORIENTED_EDGE('',*,*,#16282,.F.);
#23011=ORIENTED_EDGE('',*,*,#16290,.F.);
#23012=ORIENTED_EDGE('',*,*,#16291,.T.);
#23013=ORIENTED_EDGE('',*,*,#16292,.F.);
#23014=ORIENTED_EDGE('',*,*,#16293,.F.);
#23015=ORIENTED_EDGE('',*,*,#16294,.F.);
#23016=ORIENTED_EDGE('',*,*,#16293,.T.);
#23017=ORIENTED_EDGE('',*,*,#16295,.T.);
#23018=ORIENTED_EDGE('',*,*,#16296,.F.);
#23019=ORIENTED_EDGE('',*,*,#16295,.F.);
#23020=ORIENTED_EDGE('',*,*,#16292,.T.);
#23021=ORIENTED_EDGE('',*,*,#16297,.T.);
#23022=ORIENTED_EDGE('',*,*,#16298,.F.);
#23023=ORIENTED_EDGE('',*,*,#16297,.F.);
#23024=ORIENTED_EDGE('',*,*,#16291,.F.);
#23025=ORIENTED_EDGE('',*,*,#16299,.F.);
#23026=ORIENTED_EDGE('',*,*,#16300,.T.);
#23027=ORIENTED_EDGE('',*,*,#16301,.F.);
#23028=ORIENTED_EDGE('',*,*,#16302,.F.);
#23029=ORIENTED_EDGE('',*,*,#16303,.F.);
#23030=ORIENTED_EDGE('',*,*,#16302,.T.);
#23031=ORIENTED_EDGE('',*,*,#16304,.T.);
#23032=ORIENTED_EDGE('',*,*,#16305,.F.);
#23033=ORIENTED_EDGE('',*,*,#16304,.F.);
#23034=ORIENTED_EDGE('',*,*,#16301,.T.);
#23035=ORIENTED_EDGE('',*,*,#16306,.T.);
#23036=ORIENTED_EDGE('',*,*,#16307,.F.);
#23037=ORIENTED_EDGE('',*,*,#16306,.F.);
#23038=ORIENTED_EDGE('',*,*,#16300,.F.);
#23039=ORIENTED_EDGE('',*,*,#16308,.F.);
#23040=ORIENTED_EDGE('',*,*,#16309,.T.);
#23041=ORIENTED_EDGE('',*,*,#16310,.F.);
#23042=ORIENTED_EDGE('',*,*,#16311,.F.);
#23043=ORIENTED_EDGE('',*,*,#16312,.F.);
#23044=ORIENTED_EDGE('',*,*,#16311,.T.);
#23045=ORIENTED_EDGE('',*,*,#16313,.T.);
#23046=ORIENTED_EDGE('',*,*,#16314,.F.);
#23047=ORIENTED_EDGE('',*,*,#16313,.F.);
#23048=ORIENTED_EDGE('',*,*,#16310,.T.);
#23049=ORIENTED_EDGE('',*,*,#16315,.T.);
#23050=ORIENTED_EDGE('',*,*,#16316,.F.);
#23051=ORIENTED_EDGE('',*,*,#16315,.F.);
#23052=ORIENTED_EDGE('',*,*,#16309,.F.);
#23053=ORIENTED_EDGE('',*,*,#16317,.F.);
#23054=ORIENTED_EDGE('',*,*,#16318,.T.);
#23055=ORIENTED_EDGE('',*,*,#16319,.F.);
#23056=ORIENTED_EDGE('',*,*,#16320,.F.);
#23057=ORIENTED_EDGE('',*,*,#16321,.F.);
#23058=ORIENTED_EDGE('',*,*,#16320,.T.);
#23059=ORIENTED_EDGE('',*,*,#16322,.T.);
#23060=ORIENTED_EDGE('',*,*,#16323,.F.);
#23061=ORIENTED_EDGE('',*,*,#16324,.F.);
#23062=ORIENTED_EDGE('',*,*,#16322,.F.);
#23063=ORIENTED_EDGE('',*,*,#16319,.T.);
#23064=ORIENTED_EDGE('',*,*,#16325,.T.);
#23065=ORIENTED_EDGE('',*,*,#16326,.F.);
#23066=ORIENTED_EDGE('',*,*,#16325,.F.);
#23067=ORIENTED_EDGE('',*,*,#16318,.F.);
#23068=ORIENTED_EDGE('',*,*,#16327,.F.);
#23069=ORIENTED_EDGE('',*,*,#16328,.F.);
#23070=ORIENTED_EDGE('',*,*,#16329,.T.);
#23071=ORIENTED_EDGE('',*,*,#16330,.F.);
#23072=ORIENTED_EDGE('',*,*,#16331,.F.);
#23073=ORIENTED_EDGE('',*,*,#16332,.F.);
#23074=ORIENTED_EDGE('',*,*,#16331,.T.);
#23075=ORIENTED_EDGE('',*,*,#16333,.T.);
#23076=ORIENTED_EDGE('',*,*,#16334,.F.);
#23077=ORIENTED_EDGE('',*,*,#16333,.F.);
#23078=ORIENTED_EDGE('',*,*,#16330,.T.);
#23079=ORIENTED_EDGE('',*,*,#16335,.T.);
#23080=ORIENTED_EDGE('',*,*,#16336,.F.);
#23081=ORIENTED_EDGE('',*,*,#16335,.F.);
#23082=ORIENTED_EDGE('',*,*,#16329,.F.);
#23083=ORIENTED_EDGE('',*,*,#16337,.F.);
#23084=ORIENTED_EDGE('',*,*,#16338,.T.);
#23085=ORIENTED_EDGE('',*,*,#16339,.F.);
#23086=ORIENTED_EDGE('',*,*,#16340,.F.);
#23087=ORIENTED_EDGE('',*,*,#16341,.F.);
#23088=ORIENTED_EDGE('',*,*,#16340,.T.);
#23089=ORIENTED_EDGE('',*,*,#16342,.T.);
#23090=ORIENTED_EDGE('',*,*,#16343,.F.);
#23091=ORIENTED_EDGE('',*,*,#16342,.F.);
#23092=ORIENTED_EDGE('',*,*,#16339,.T.);
#23093=ORIENTED_EDGE('',*,*,#16344,.T.);
#23094=ORIENTED_EDGE('',*,*,#16345,.F.);
#23095=ORIENTED_EDGE('',*,*,#16344,.F.);
#23096=ORIENTED_EDGE('',*,*,#16338,.F.);
#23097=ORIENTED_EDGE('',*,*,#16346,.F.);
#23098=ORIENTED_EDGE('',*,*,#16347,.T.);
#23099=ORIENTED_EDGE('',*,*,#16348,.F.);
#23100=ORIENTED_EDGE('',*,*,#16349,.F.);
#23101=ORIENTED_EDGE('',*,*,#16350,.F.);
#23102=ORIENTED_EDGE('',*,*,#16349,.T.);
#23103=ORIENTED_EDGE('',*,*,#16351,.T.);
#23104=ORIENTED_EDGE('',*,*,#16352,.F.);
#23105=ORIENTED_EDGE('',*,*,#16351,.F.);
#23106=ORIENTED_EDGE('',*,*,#16348,.T.);
#23107=ORIENTED_EDGE('',*,*,#16353,.T.);
#23108=ORIENTED_EDGE('',*,*,#16354,.F.);
#23109=ORIENTED_EDGE('',*,*,#16353,.F.);
#23110=ORIENTED_EDGE('',*,*,#16347,.F.);
#23111=ORIENTED_EDGE('',*,*,#16355,.F.);
#23112=ORIENTED_EDGE('',*,*,#16356,.T.);
#23113=ORIENTED_EDGE('',*,*,#16357,.F.);
#23114=ORIENTED_EDGE('',*,*,#16358,.F.);
#23115=ORIENTED_EDGE('',*,*,#16359,.F.);
#23116=ORIENTED_EDGE('',*,*,#16358,.T.);
#23117=ORIENTED_EDGE('',*,*,#16360,.T.);
#23118=ORIENTED_EDGE('',*,*,#16361,.F.);
#23119=ORIENTED_EDGE('',*,*,#16360,.F.);
#23120=ORIENTED_EDGE('',*,*,#16357,.T.);
#23121=ORIENTED_EDGE('',*,*,#16362,.T.);
#23122=ORIENTED_EDGE('',*,*,#16363,.F.);
#23123=ORIENTED_EDGE('',*,*,#16362,.F.);
#23124=ORIENTED_EDGE('',*,*,#16356,.F.);
#23125=ORIENTED_EDGE('',*,*,#16364,.F.);
#23126=ORIENTED_EDGE('',*,*,#16365,.T.);
#23127=ORIENTED_EDGE('',*,*,#16366,.F.);
#23128=ORIENTED_EDGE('',*,*,#16367,.F.);
#23129=ORIENTED_EDGE('',*,*,#16368,.F.);
#23130=ORIENTED_EDGE('',*,*,#16367,.T.);
#23131=ORIENTED_EDGE('',*,*,#16369,.T.);
#23132=ORIENTED_EDGE('',*,*,#16370,.F.);
#23133=ORIENTED_EDGE('',*,*,#16369,.F.);
#23134=ORIENTED_EDGE('',*,*,#16366,.T.);
#23135=ORIENTED_EDGE('',*,*,#16371,.T.);
#23136=ORIENTED_EDGE('',*,*,#16372,.F.);
#23137=ORIENTED_EDGE('',*,*,#16371,.F.);
#23138=ORIENTED_EDGE('',*,*,#16365,.F.);
#23139=ORIENTED_EDGE('',*,*,#16373,.F.);
#23140=ORIENTED_EDGE('',*,*,#16374,.T.);
#23141=ORIENTED_EDGE('',*,*,#16375,.F.);
#23142=ORIENTED_EDGE('',*,*,#16376,.F.);
#23143=ORIENTED_EDGE('',*,*,#16377,.F.);
#23144=ORIENTED_EDGE('',*,*,#16376,.T.);
#23145=ORIENTED_EDGE('',*,*,#16378,.T.);
#23146=ORIENTED_EDGE('',*,*,#16379,.F.);
#23147=ORIENTED_EDGE('',*,*,#16378,.F.);
#23148=ORIENTED_EDGE('',*,*,#16375,.T.);
#23149=ORIENTED_EDGE('',*,*,#16380,.T.);
#23150=ORIENTED_EDGE('',*,*,#16381,.F.);
#23151=ORIENTED_EDGE('',*,*,#16380,.F.);
#23152=ORIENTED_EDGE('',*,*,#16374,.F.);
#23153=ORIENTED_EDGE('',*,*,#16382,.F.);
#23154=ORIENTED_EDGE('',*,*,#16383,.T.);
#23155=ORIENTED_EDGE('',*,*,#16384,.F.);
#23156=ORIENTED_EDGE('',*,*,#16385,.F.);
#23157=ORIENTED_EDGE('',*,*,#16386,.F.);
#23158=ORIENTED_EDGE('',*,*,#16385,.T.);
#23159=ORIENTED_EDGE('',*,*,#16387,.T.);
#23160=ORIENTED_EDGE('',*,*,#16388,.F.);
#23161=ORIENTED_EDGE('',*,*,#16387,.F.);
#23162=ORIENTED_EDGE('',*,*,#16384,.T.);
#23163=ORIENTED_EDGE('',*,*,#16389,.T.);
#23164=ORIENTED_EDGE('',*,*,#16390,.F.);
#23165=ORIENTED_EDGE('',*,*,#16389,.F.);
#23166=ORIENTED_EDGE('',*,*,#16383,.F.);
#23167=ORIENTED_EDGE('',*,*,#16391,.F.);
#23168=ORIENTED_EDGE('',*,*,#16392,.T.);
#23169=ORIENTED_EDGE('',*,*,#16393,.F.);
#23170=ORIENTED_EDGE('',*,*,#16394,.F.);
#23171=ORIENTED_EDGE('',*,*,#16395,.F.);
#23172=ORIENTED_EDGE('',*,*,#16394,.T.);
#23173=ORIENTED_EDGE('',*,*,#16396,.T.);
#23174=ORIENTED_EDGE('',*,*,#16397,.F.);
#23175=ORIENTED_EDGE('',*,*,#16396,.F.);
#23176=ORIENTED_EDGE('',*,*,#16393,.T.);
#23177=ORIENTED_EDGE('',*,*,#16398,.T.);
#23178=ORIENTED_EDGE('',*,*,#16399,.F.);
#23179=ORIENTED_EDGE('',*,*,#16398,.F.);
#23180=ORIENTED_EDGE('',*,*,#16392,.F.);
#23181=ORIENTED_EDGE('',*,*,#16400,.F.);
#23182=ORIENTED_EDGE('',*,*,#16401,.T.);
#23183=ORIENTED_EDGE('',*,*,#16402,.F.);
#23184=ORIENTED_EDGE('',*,*,#16403,.F.);
#23185=ORIENTED_EDGE('',*,*,#16404,.F.);
#23186=ORIENTED_EDGE('',*,*,#16403,.T.);
#23187=ORIENTED_EDGE('',*,*,#16405,.T.);
#23188=ORIENTED_EDGE('',*,*,#16406,.F.);
#23189=ORIENTED_EDGE('',*,*,#16405,.F.);
#23190=ORIENTED_EDGE('',*,*,#16402,.T.);
#23191=ORIENTED_EDGE('',*,*,#16407,.T.);
#23192=ORIENTED_EDGE('',*,*,#16408,.F.);
#23193=ORIENTED_EDGE('',*,*,#16407,.F.);
#23194=ORIENTED_EDGE('',*,*,#16401,.F.);
#23195=ORIENTED_EDGE('',*,*,#16409,.F.);
#23196=ORIENTED_EDGE('',*,*,#16410,.T.);
#23197=ORIENTED_EDGE('',*,*,#16411,.F.);
#23198=ORIENTED_EDGE('',*,*,#16412,.F.);
#23199=ORIENTED_EDGE('',*,*,#16413,.F.);
#23200=ORIENTED_EDGE('',*,*,#16412,.T.);
#23201=ORIENTED_EDGE('',*,*,#16414,.T.);
#23202=ORIENTED_EDGE('',*,*,#16415,.F.);
#23203=ORIENTED_EDGE('',*,*,#16414,.F.);
#23204=ORIENTED_EDGE('',*,*,#16411,.T.);
#23205=ORIENTED_EDGE('',*,*,#16416,.T.);
#23206=ORIENTED_EDGE('',*,*,#16417,.F.);
#23207=ORIENTED_EDGE('',*,*,#16416,.F.);
#23208=ORIENTED_EDGE('',*,*,#16410,.F.);
#23209=ORIENTED_EDGE('',*,*,#16418,.F.);
#23210=ORIENTED_EDGE('',*,*,#16419,.T.);
#23211=ORIENTED_EDGE('',*,*,#16420,.F.);
#23212=ORIENTED_EDGE('',*,*,#16421,.F.);
#23213=ORIENTED_EDGE('',*,*,#16422,.F.);
#23214=ORIENTED_EDGE('',*,*,#16421,.T.);
#23215=ORIENTED_EDGE('',*,*,#16423,.T.);
#23216=ORIENTED_EDGE('',*,*,#16424,.F.);
#23217=ORIENTED_EDGE('',*,*,#16423,.F.);
#23218=ORIENTED_EDGE('',*,*,#16420,.T.);
#23219=ORIENTED_EDGE('',*,*,#16425,.T.);
#23220=ORIENTED_EDGE('',*,*,#16426,.F.);
#23221=ORIENTED_EDGE('',*,*,#16425,.F.);
#23222=ORIENTED_EDGE('',*,*,#16419,.F.);
#23223=ORIENTED_EDGE('',*,*,#16427,.F.);
#23224=ORIENTED_EDGE('',*,*,#16428,.T.);
#23225=ORIENTED_EDGE('',*,*,#16429,.F.);
#23226=ORIENTED_EDGE('',*,*,#16430,.F.);
#23227=ORIENTED_EDGE('',*,*,#16431,.F.);
#23228=ORIENTED_EDGE('',*,*,#16430,.T.);
#23229=ORIENTED_EDGE('',*,*,#16432,.T.);
#23230=ORIENTED_EDGE('',*,*,#16433,.F.);
#23231=ORIENTED_EDGE('',*,*,#16432,.F.);
#23232=ORIENTED_EDGE('',*,*,#16429,.T.);
#23233=ORIENTED_EDGE('',*,*,#16434,.T.);
#23234=ORIENTED_EDGE('',*,*,#16435,.F.);
#23235=ORIENTED_EDGE('',*,*,#16434,.F.);
#23236=ORIENTED_EDGE('',*,*,#16428,.F.);
#23237=ORIENTED_EDGE('',*,*,#16436,.F.);
#23238=ORIENTED_EDGE('',*,*,#16437,.T.);
#23239=ORIENTED_EDGE('',*,*,#16438,.F.);
#23240=ORIENTED_EDGE('',*,*,#16439,.F.);
#23241=ORIENTED_EDGE('',*,*,#16440,.F.);
#23242=ORIENTED_EDGE('',*,*,#16439,.T.);
#23243=ORIENTED_EDGE('',*,*,#16441,.T.);
#23244=ORIENTED_EDGE('',*,*,#16442,.F.);
#23245=ORIENTED_EDGE('',*,*,#16441,.F.);
#23246=ORIENTED_EDGE('',*,*,#16438,.T.);
#23247=ORIENTED_EDGE('',*,*,#16443,.T.);
#23248=ORIENTED_EDGE('',*,*,#16444,.F.);
#23249=ORIENTED_EDGE('',*,*,#16443,.F.);
#23250=ORIENTED_EDGE('',*,*,#16437,.F.);
#23251=ORIENTED_EDGE('',*,*,#16445,.F.);
#23252=ORIENTED_EDGE('',*,*,#16446,.T.);
#23253=ORIENTED_EDGE('',*,*,#16447,.F.);
#23254=ORIENTED_EDGE('',*,*,#16448,.F.);
#23255=ORIENTED_EDGE('',*,*,#16449,.F.);
#23256=ORIENTED_EDGE('',*,*,#16448,.T.);
#23257=ORIENTED_EDGE('',*,*,#16450,.T.);
#23258=ORIENTED_EDGE('',*,*,#16451,.F.);
#23259=ORIENTED_EDGE('',*,*,#16450,.F.);
#23260=ORIENTED_EDGE('',*,*,#16447,.T.);
#23261=ORIENTED_EDGE('',*,*,#16452,.T.);
#23262=ORIENTED_EDGE('',*,*,#16453,.F.);
#23263=ORIENTED_EDGE('',*,*,#16452,.F.);
#23264=ORIENTED_EDGE('',*,*,#16446,.F.);
#23265=ORIENTED_EDGE('',*,*,#16454,.F.);
#23266=ORIENTED_EDGE('',*,*,#16455,.T.);
#23267=ORIENTED_EDGE('',*,*,#16456,.F.);
#23268=ORIENTED_EDGE('',*,*,#16457,.F.);
#23269=ORIENTED_EDGE('',*,*,#16458,.F.);
#23270=ORIENTED_EDGE('',*,*,#16457,.T.);
#23271=ORIENTED_EDGE('',*,*,#16459,.T.);
#23272=ORIENTED_EDGE('',*,*,#16460,.F.);
#23273=ORIENTED_EDGE('',*,*,#16459,.F.);
#23274=ORIENTED_EDGE('',*,*,#16456,.T.);
#23275=ORIENTED_EDGE('',*,*,#16461,.T.);
#23276=ORIENTED_EDGE('',*,*,#16462,.F.);
#23277=ORIENTED_EDGE('',*,*,#16461,.F.);
#23278=ORIENTED_EDGE('',*,*,#16455,.F.);
#23279=ORIENTED_EDGE('',*,*,#16463,.F.);
#23280=ORIENTED_EDGE('',*,*,#16464,.T.);
#23281=ORIENTED_EDGE('',*,*,#16465,.F.);
#23282=ORIENTED_EDGE('',*,*,#16466,.F.);
#23283=ORIENTED_EDGE('',*,*,#16467,.F.);
#23284=ORIENTED_EDGE('',*,*,#16466,.T.);
#23285=ORIENTED_EDGE('',*,*,#16468,.T.);
#23286=ORIENTED_EDGE('',*,*,#16469,.F.);
#23287=ORIENTED_EDGE('',*,*,#16468,.F.);
#23288=ORIENTED_EDGE('',*,*,#16465,.T.);
#23289=ORIENTED_EDGE('',*,*,#16470,.T.);
#23290=ORIENTED_EDGE('',*,*,#16471,.F.);
#23291=ORIENTED_EDGE('',*,*,#16470,.F.);
#23292=ORIENTED_EDGE('',*,*,#16464,.F.);
#23293=ORIENTED_EDGE('',*,*,#16472,.F.);
#23294=ORIENTED_EDGE('',*,*,#16473,.T.);
#23295=ORIENTED_EDGE('',*,*,#16474,.F.);
#23296=ORIENTED_EDGE('',*,*,#16475,.F.);
#23297=ORIENTED_EDGE('',*,*,#16476,.F.);
#23298=ORIENTED_EDGE('',*,*,#16475,.T.);
#23299=ORIENTED_EDGE('',*,*,#16477,.T.);
#23300=ORIENTED_EDGE('',*,*,#16478,.F.);
#23301=ORIENTED_EDGE('',*,*,#16477,.F.);
#23302=ORIENTED_EDGE('',*,*,#16474,.T.);
#23303=ORIENTED_EDGE('',*,*,#16479,.T.);
#23304=ORIENTED_EDGE('',*,*,#16480,.F.);
#23305=ORIENTED_EDGE('',*,*,#16479,.F.);
#23306=ORIENTED_EDGE('',*,*,#16473,.F.);
#23307=ORIENTED_EDGE('',*,*,#16481,.F.);
#23308=ORIENTED_EDGE('',*,*,#16482,.T.);
#23309=ORIENTED_EDGE('',*,*,#16483,.F.);
#23310=ORIENTED_EDGE('',*,*,#16484,.F.);
#23311=ORIENTED_EDGE('',*,*,#16485,.F.);
#23312=ORIENTED_EDGE('',*,*,#16484,.T.);
#23313=ORIENTED_EDGE('',*,*,#16486,.T.);
#23314=ORIENTED_EDGE('',*,*,#16487,.F.);
#23315=ORIENTED_EDGE('',*,*,#16486,.F.);
#23316=ORIENTED_EDGE('',*,*,#16483,.T.);
#23317=ORIENTED_EDGE('',*,*,#16488,.T.);
#23318=ORIENTED_EDGE('',*,*,#16489,.F.);
#23319=ORIENTED_EDGE('',*,*,#16488,.F.);
#23320=ORIENTED_EDGE('',*,*,#16482,.F.);
#23321=ORIENTED_EDGE('',*,*,#16490,.F.);
#23322=ORIENTED_EDGE('',*,*,#16491,.T.);
#23323=ORIENTED_EDGE('',*,*,#16492,.T.);
#23324=ORIENTED_EDGE('',*,*,#16493,.F.);
#23325=ORIENTED_EDGE('',*,*,#16494,.F.);
#23326=ORIENTED_EDGE('',*,*,#16495,.T.);
#23327=ORIENTED_EDGE('',*,*,#16496,.T.);
#23328=ORIENTED_EDGE('',*,*,#16491,.F.);
#23329=ORIENTED_EDGE('',*,*,#16497,.F.);
#23330=ORIENTED_EDGE('',*,*,#16498,.T.);
#23331=ORIENTED_EDGE('',*,*,#16499,.T.);
#23332=ORIENTED_EDGE('',*,*,#16495,.F.);
#23333=ORIENTED_EDGE('',*,*,#16500,.F.);
#23334=ORIENTED_EDGE('',*,*,#16501,.T.);
#23335=ORIENTED_EDGE('',*,*,#16502,.T.);
#23336=ORIENTED_EDGE('',*,*,#16498,.F.);
#23337=ORIENTED_EDGE('',*,*,#16503,.F.);
#23338=ORIENTED_EDGE('',*,*,#16504,.T.);
#23339=ORIENTED_EDGE('',*,*,#16505,.T.);
#23340=ORIENTED_EDGE('',*,*,#16501,.F.);
#23341=ORIENTED_EDGE('',*,*,#16506,.F.);
#23342=ORIENTED_EDGE('',*,*,#16493,.T.);
#23343=ORIENTED_EDGE('',*,*,#16507,.T.);
#23344=ORIENTED_EDGE('',*,*,#16504,.F.);
#23345=ORIENTED_EDGE('',*,*,#16507,.F.);
#23346=ORIENTED_EDGE('',*,*,#16492,.F.);
#23347=ORIENTED_EDGE('',*,*,#16496,.F.);
#23348=ORIENTED_EDGE('',*,*,#16499,.F.);
#23349=ORIENTED_EDGE('',*,*,#16502,.F.);
#23350=ORIENTED_EDGE('',*,*,#16505,.F.);
#23351=ORIENTED_EDGE('',*,*,#16508,.F.);
#23352=ORIENTED_EDGE('',*,*,#16159,.F.);
#23353=ORIENTED_EDGE('',*,*,#16029,.F.);
#23354=ORIENTED_EDGE('',*,*,#16160,.F.);
#23355=ORIENTED_EDGE('',*,*,#16509,.T.);
#23356=ORIENTED_EDGE('',*,*,#16508,.T.);
#23357=ORIENTED_EDGE('',*,*,#16509,.F.);
#23358=ORIENTED_EDGE('',*,*,#16088,.T.);
#23359=ORIENTED_EDGE('',*,*,#16156,.T.);
#23360=ORIENTED_EDGE('',*,*,#16510,.F.);
#23361=ORIENTED_EDGE('',*,*,#16511,.F.);
#23362=ORIENTED_EDGE('',*,*,#16512,.T.);
#23363=ORIENTED_EDGE('',*,*,#16510,.T.);
#23364=ORIENTED_EDGE('',*,*,#16154,.T.);
#23365=ORIENTED_EDGE('',*,*,#16089,.T.);
#23366=ORIENTED_EDGE('',*,*,#16512,.F.);
#23367=ORIENTED_EDGE('',*,*,#16513,.F.);
#23368=ORIENTED_EDGE('',*,*,#16514,.T.);
#23369=ORIENTED_EDGE('',*,*,#16511,.T.);
#23370=ORIENTED_EDGE('',*,*,#16514,.F.);
#23371=ORIENTED_EDGE('',*,*,#16515,.F.);
#23372=ORIENTED_EDGE('',*,*,#16513,.T.);
#23373=ORIENTED_EDGE('',*,*,#16516,.F.);
#23374=ORIENTED_EDGE('',*,*,#16517,.T.);
#23375=ORIENTED_EDGE('',*,*,#16327,.T.);
#23376=ORIENTED_EDGE('',*,*,#16317,.T.);
#23377=ORIENTED_EDGE('',*,*,#16321,.T.);
#23378=ORIENTED_EDGE('',*,*,#16518,.T.);
#23379=ORIENTED_EDGE('',*,*,#16515,.T.);
#23380=ORIENTED_EDGE('',*,*,#16518,.F.);
#23381=ORIENTED_EDGE('',*,*,#16323,.T.);
#23382=ORIENTED_EDGE('',*,*,#16324,.T.);
#23383=ORIENTED_EDGE('',*,*,#16326,.T.);
#23384=ORIENTED_EDGE('',*,*,#16517,.F.);
#23385=ORIENTED_EDGE('',*,*,#16170,.T.);
#23386=ORIENTED_EDGE('',*,*,#16172,.T.);
#23387=ORIENTED_EDGE('',*,*,#16164,.T.);
#23388=ORIENTED_EDGE('',*,*,#16168,.T.);
#23389=ORIENTED_EDGE('',*,*,#16179,.T.);
#23390=ORIENTED_EDGE('',*,*,#16181,.T.);
#23391=ORIENTED_EDGE('',*,*,#16173,.T.);
#23392=ORIENTED_EDGE('',*,*,#16177,.T.);
#23393=ORIENTED_EDGE('',*,*,#16188,.T.);
#23394=ORIENTED_EDGE('',*,*,#16190,.T.);
#23395=ORIENTED_EDGE('',*,*,#16182,.T.);
#23396=ORIENTED_EDGE('',*,*,#16186,.T.);
#23397=ORIENTED_EDGE('',*,*,#16197,.T.);
#23398=ORIENTED_EDGE('',*,*,#16199,.T.);
#23399=ORIENTED_EDGE('',*,*,#16191,.T.);
#23400=ORIENTED_EDGE('',*,*,#16195,.T.);
#23401=ORIENTED_EDGE('',*,*,#16206,.T.);
#23402=ORIENTED_EDGE('',*,*,#16208,.T.);
#23403=ORIENTED_EDGE('',*,*,#16200,.T.);
#23404=ORIENTED_EDGE('',*,*,#16204,.T.);
#23405=ORIENTED_EDGE('',*,*,#16215,.T.);
#23406=ORIENTED_EDGE('',*,*,#16217,.T.);
#23407=ORIENTED_EDGE('',*,*,#16209,.T.);
#23408=ORIENTED_EDGE('',*,*,#16213,.T.);
#23409=ORIENTED_EDGE('',*,*,#16224,.T.);
#23410=ORIENTED_EDGE('',*,*,#16226,.T.);
#23411=ORIENTED_EDGE('',*,*,#16218,.T.);
#23412=ORIENTED_EDGE('',*,*,#16222,.T.);
#23413=ORIENTED_EDGE('',*,*,#16233,.T.);
#23414=ORIENTED_EDGE('',*,*,#16235,.T.);
#23415=ORIENTED_EDGE('',*,*,#16227,.T.);
#23416=ORIENTED_EDGE('',*,*,#16231,.T.);
#23417=ORIENTED_EDGE('',*,*,#16242,.T.);
#23418=ORIENTED_EDGE('',*,*,#16244,.T.);
#23419=ORIENTED_EDGE('',*,*,#16236,.T.);
#23420=ORIENTED_EDGE('',*,*,#16240,.T.);
#23421=ORIENTED_EDGE('',*,*,#16251,.T.);
#23422=ORIENTED_EDGE('',*,*,#16253,.T.);
#23423=ORIENTED_EDGE('',*,*,#16245,.T.);
#23424=ORIENTED_EDGE('',*,*,#16249,.T.);
#23425=ORIENTED_EDGE('',*,*,#16260,.T.);
#23426=ORIENTED_EDGE('',*,*,#16262,.T.);
#23427=ORIENTED_EDGE('',*,*,#16254,.T.);
#23428=ORIENTED_EDGE('',*,*,#16258,.T.);
#23429=ORIENTED_EDGE('',*,*,#16269,.T.);
#23430=ORIENTED_EDGE('',*,*,#16271,.T.);
#23431=ORIENTED_EDGE('',*,*,#16263,.T.);
#23432=ORIENTED_EDGE('',*,*,#16267,.T.);
#23433=ORIENTED_EDGE('',*,*,#16278,.T.);
#23434=ORIENTED_EDGE('',*,*,#16280,.T.);
#23435=ORIENTED_EDGE('',*,*,#16272,.T.);
#23436=ORIENTED_EDGE('',*,*,#16276,.T.);
#23437=ORIENTED_EDGE('',*,*,#16287,.T.);
#23438=ORIENTED_EDGE('',*,*,#16289,.T.);
#23439=ORIENTED_EDGE('',*,*,#16281,.T.);
#23440=ORIENTED_EDGE('',*,*,#16285,.T.);
#23441=ORIENTED_EDGE('',*,*,#16296,.T.);
#23442=ORIENTED_EDGE('',*,*,#16298,.T.);
#23443=ORIENTED_EDGE('',*,*,#16290,.T.);
#23444=ORIENTED_EDGE('',*,*,#16294,.T.);
#23445=ORIENTED_EDGE('',*,*,#16305,.T.);
#23446=ORIENTED_EDGE('',*,*,#16307,.T.);
#23447=ORIENTED_EDGE('',*,*,#16299,.T.);
#23448=ORIENTED_EDGE('',*,*,#16303,.T.);
#23449=ORIENTED_EDGE('',*,*,#16314,.T.);
#23450=ORIENTED_EDGE('',*,*,#16316,.T.);
#23451=ORIENTED_EDGE('',*,*,#16308,.T.);
#23452=ORIENTED_EDGE('',*,*,#16312,.T.);
#23453=ORIENTED_EDGE('',*,*,#16334,.T.);
#23454=ORIENTED_EDGE('',*,*,#16336,.T.);
#23455=ORIENTED_EDGE('',*,*,#16328,.T.);
#23456=ORIENTED_EDGE('',*,*,#16332,.T.);
#23457=ORIENTED_EDGE('',*,*,#16343,.T.);
#23458=ORIENTED_EDGE('',*,*,#16345,.T.);
#23459=ORIENTED_EDGE('',*,*,#16337,.T.);
#23460=ORIENTED_EDGE('',*,*,#16341,.T.);
#23461=ORIENTED_EDGE('',*,*,#16352,.T.);
#23462=ORIENTED_EDGE('',*,*,#16354,.T.);
#23463=ORIENTED_EDGE('',*,*,#16346,.T.);
#23464=ORIENTED_EDGE('',*,*,#16350,.T.);
#23465=ORIENTED_EDGE('',*,*,#16361,.T.);
#23466=ORIENTED_EDGE('',*,*,#16363,.T.);
#23467=ORIENTED_EDGE('',*,*,#16355,.T.);
#23468=ORIENTED_EDGE('',*,*,#16359,.T.);
#23469=ORIENTED_EDGE('',*,*,#16370,.T.);
#23470=ORIENTED_EDGE('',*,*,#16372,.T.);
#23471=ORIENTED_EDGE('',*,*,#16364,.T.);
#23472=ORIENTED_EDGE('',*,*,#16368,.T.);
#23473=ORIENTED_EDGE('',*,*,#16379,.T.);
#23474=ORIENTED_EDGE('',*,*,#16381,.T.);
#23475=ORIENTED_EDGE('',*,*,#16373,.T.);
#23476=ORIENTED_EDGE('',*,*,#16377,.T.);
#23477=ORIENTED_EDGE('',*,*,#16388,.T.);
#23478=ORIENTED_EDGE('',*,*,#16390,.T.);
#23479=ORIENTED_EDGE('',*,*,#16382,.T.);
#23480=ORIENTED_EDGE('',*,*,#16386,.T.);
#23481=ORIENTED_EDGE('',*,*,#16397,.T.);
#23482=ORIENTED_EDGE('',*,*,#16399,.T.);
#23483=ORIENTED_EDGE('',*,*,#16391,.T.);
#23484=ORIENTED_EDGE('',*,*,#16395,.T.);
#23485=ORIENTED_EDGE('',*,*,#16406,.T.);
#23486=ORIENTED_EDGE('',*,*,#16408,.T.);
#23487=ORIENTED_EDGE('',*,*,#16400,.T.);
#23488=ORIENTED_EDGE('',*,*,#16404,.T.);
#23489=ORIENTED_EDGE('',*,*,#16415,.T.);
#23490=ORIENTED_EDGE('',*,*,#16417,.T.);
#23491=ORIENTED_EDGE('',*,*,#16409,.T.);
#23492=ORIENTED_EDGE('',*,*,#16413,.T.);
#23493=ORIENTED_EDGE('',*,*,#16424,.T.);
#23494=ORIENTED_EDGE('',*,*,#16426,.T.);
#23495=ORIENTED_EDGE('',*,*,#16418,.T.);
#23496=ORIENTED_EDGE('',*,*,#16422,.T.);
#23497=ORIENTED_EDGE('',*,*,#16433,.T.);
#23498=ORIENTED_EDGE('',*,*,#16435,.T.);
#23499=ORIENTED_EDGE('',*,*,#16427,.T.);
#23500=ORIENTED_EDGE('',*,*,#16431,.T.);
#23501=ORIENTED_EDGE('',*,*,#16442,.T.);
#23502=ORIENTED_EDGE('',*,*,#16444,.T.);
#23503=ORIENTED_EDGE('',*,*,#16436,.T.);
#23504=ORIENTED_EDGE('',*,*,#16440,.T.);
#23505=ORIENTED_EDGE('',*,*,#16451,.T.);
#23506=ORIENTED_EDGE('',*,*,#16453,.T.);
#23507=ORIENTED_EDGE('',*,*,#16445,.T.);
#23508=ORIENTED_EDGE('',*,*,#16449,.T.);
#23509=ORIENTED_EDGE('',*,*,#16460,.T.);
#23510=ORIENTED_EDGE('',*,*,#16462,.T.);
#23511=ORIENTED_EDGE('',*,*,#16454,.T.);
#23512=ORIENTED_EDGE('',*,*,#16458,.T.);
#23513=ORIENTED_EDGE('',*,*,#16469,.T.);
#23514=ORIENTED_EDGE('',*,*,#16471,.T.);
#23515=ORIENTED_EDGE('',*,*,#16463,.T.);
#23516=ORIENTED_EDGE('',*,*,#16467,.T.);
#23517=ORIENTED_EDGE('',*,*,#16478,.T.);
#23518=ORIENTED_EDGE('',*,*,#16480,.T.);
#23519=ORIENTED_EDGE('',*,*,#16472,.T.);
#23520=ORIENTED_EDGE('',*,*,#16476,.T.);
#23521=ORIENTED_EDGE('',*,*,#16487,.T.);
#23522=ORIENTED_EDGE('',*,*,#16489,.T.);
#23523=ORIENTED_EDGE('',*,*,#16481,.T.);
#23524=ORIENTED_EDGE('',*,*,#16485,.T.);
#23525=ORIENTED_EDGE('',*,*,#16519,.F.);
#23526=ORIENTED_EDGE('',*,*,#16520,.T.);
#23527=ORIENTED_EDGE('',*,*,#16516,.T.);
#23528=ORIENTED_EDGE('',*,*,#16520,.F.);
#23529=ORIENTED_EDGE('',*,*,#16519,.T.);
#23530=ORIENTED_EDGE('',*,*,#16490,.T.);
#23531=ORIENTED_EDGE('',*,*,#16506,.T.);
#23532=ORIENTED_EDGE('',*,*,#16503,.T.);
#23533=ORIENTED_EDGE('',*,*,#16500,.T.);
#23534=ORIENTED_EDGE('',*,*,#16497,.T.);
#23535=ORIENTED_EDGE('',*,*,#16494,.T.);
#23601=CONICAL_SURFACE('',#26884,4.75,0.785398163397441);
#23602=CONICAL_SURFACE('',#26887,4.975,0.0996686524911625);
#23603=CONICAL_SURFACE('',#26895,7.75,0.785398163397448);
#24726=ADVANCED_FACE('',(#2867),#540,.T.);
#24727=ADVANCED_FACE('',(#2868),#541,.T.);
#24728=ADVANCED_FACE('',(#2869),#542,.T.);
#24729=ADVANCED_FACE('',(#2870),#543,.T.);
#24730=ADVANCED_FACE('',(#2871),#544,.T.);
#24731=ADVANCED_FACE('',(#2872),#545,.T.);
#24732=ADVANCED_FACE('',(#2873),#546,.T.);
#24733=ADVANCED_FACE('',(#2874),#547,.T.);
#24734=ADVANCED_FACE('',(#2875),#548,.T.);
#24735=ADVANCED_FACE('',(#2876),#549,.T.);
#24736=ADVANCED_FACE('',(#2877),#550,.T.);
#24737=ADVANCED_FACE('',(#2878),#551,.T.);
#24738=ADVANCED_FACE('',(#2879),#552,.T.);
#24739=ADVANCED_FACE('',(#2880),#553,.T.);
#24740=ADVANCED_FACE('',(#2881),#554,.T.);
#24741=ADVANCED_FACE('',(#2882),#555,.T.);
#24742=ADVANCED_FACE('',(#2883),#556,.T.);
#24743=ADVANCED_FACE('',(#2884),#557,.T.);
#24744=ADVANCED_FACE('',(#2885),#558,.T.);
#24745=ADVANCED_FACE('',(#2886),#559,.T.);
#24746=ADVANCED_FACE('',(#2887),#560,.T.);
#24747=ADVANCED_FACE('',(#2888),#561,.T.);
#24748=ADVANCED_FACE('',(#2889),#562,.T.);
#24749=ADVANCED_FACE('',(#2890),#563,.T.);
#24750=ADVANCED_FACE('',(#2891),#564,.T.);
#24751=ADVANCED_FACE('',(#2892),#565,.T.);
#24752=ADVANCED_FACE('',(#2893),#566,.T.);
#24753=ADVANCED_FACE('',(#2894),#567,.T.);
#24754=ADVANCED_FACE('',(#2895),#568,.T.);
#24755=ADVANCED_FACE('',(#2896),#569,.T.);
#24756=ADVANCED_FACE('',(#2897),#570,.T.);
#24757=ADVANCED_FACE('',(#2898),#571,.T.);
#24758=ADVANCED_FACE('',(#2899),#572,.T.);
#24759=ADVANCED_FACE('',(#2900),#573,.T.);
#24760=ADVANCED_FACE('',(#2901),#574,.T.);
#24761=ADVANCED_FACE('',(#2902),#575,.T.);
#24762=ADVANCED_FACE('',(#2903),#576,.T.);
#24763=ADVANCED_FACE('',(#2904),#577,.T.);
#24764=ADVANCED_FACE('',(#2905),#578,.T.);
#24765=ADVANCED_FACE('',(#2906),#579,.T.);
#24766=ADVANCED_FACE('',(#2907),#580,.T.);
#24767=ADVANCED_FACE('',(#2908),#1589,.F.);
#24768=ADVANCED_FACE('',(#2909),#398,.F.);
#24769=ADVANCED_FACE('',(#2910),#1590,.T.);
#24770=ADVANCED_FACE('',(#2911),#581,.T.);
#24771=ADVANCED_FACE('',(#2912),#399,.F.);
#24772=ADVANCED_FACE('',(#2913),#1591,.F.);
#24773=ADVANCED_FACE('',(#2914),#1592,.T.);
#24774=ADVANCED_FACE('',(#2915),#1593,.F.);
#24775=ADVANCED_FACE('',(#2916),#1594,.F.);
#24776=ADVANCED_FACE('',(#2917),#1595,.F.);
#24777=ADVANCED_FACE('',(#2918),#1596,.T.);
#24778=ADVANCED_FACE('',(#2919),#1597,.F.);
#24779=ADVANCED_FACE('',(#2920),#1598,.F.);
#24780=ADVANCED_FACE('',(#2921),#1599,.F.);
#24781=ADVANCED_FACE('',(#2922),#1600,.T.);
#24782=ADVANCED_FACE('',(#2923),#1601,.F.);
#24783=ADVANCED_FACE('',(#2924),#1602,.F.);
#24784=ADVANCED_FACE('',(#2925),#1603,.F.);
#24785=ADVANCED_FACE('',(#2926),#1604,.T.);
#24786=ADVANCED_FACE('',(#2927),#1605,.F.);
#24787=ADVANCED_FACE('',(#2928),#1606,.F.);
#24788=ADVANCED_FACE('',(#2929),#1607,.F.);
#24789=ADVANCED_FACE('',(#2930),#1608,.T.);
#24790=ADVANCED_FACE('',(#2931),#1609,.F.);
#24791=ADVANCED_FACE('',(#2932),#1610,.F.);
#24792=ADVANCED_FACE('',(#2933),#1611,.F.);
#24793=ADVANCED_FACE('',(#2934),#1612,.T.);
#24794=ADVANCED_FACE('',(#2935),#1613,.F.);
#24795=ADVANCED_FACE('',(#2936),#1614,.F.);
#24796=ADVANCED_FACE('',(#2937),#1615,.F.);
#24797=ADVANCED_FACE('',(#2938),#1616,.T.);
#24798=ADVANCED_FACE('',(#2939),#1617,.F.);
#24799=ADVANCED_FACE('',(#2940),#1618,.F.);
#24800=ADVANCED_FACE('',(#2941),#1619,.F.);
#24801=ADVANCED_FACE('',(#2942),#1620,.T.);
#24802=ADVANCED_FACE('',(#2943),#1621,.F.);
#24803=ADVANCED_FACE('',(#2944),#1622,.F.);
#24804=ADVANCED_FACE('',(#2945),#1623,.F.);
#24805=ADVANCED_FACE('',(#2946),#1624,.T.);
#24806=ADVANCED_FACE('',(#2947),#1625,.F.);
#24807=ADVANCED_FACE('',(#2948),#1626,.F.);
#24808=ADVANCED_FACE('',(#2949),#1627,.F.);
#24809=ADVANCED_FACE('',(#2950),#1628,.T.);
#24810=ADVANCED_FACE('',(#2951),#1629,.F.);
#24811=ADVANCED_FACE('',(#2952),#1630,.F.);
#24812=ADVANCED_FACE('',(#2953),#1631,.F.);
#24813=ADVANCED_FACE('',(#2954),#1632,.T.);
#24814=ADVANCED_FACE('',(#2955),#1633,.F.);
#24815=ADVANCED_FACE('',(#2956),#1634,.F.);
#24816=ADVANCED_FACE('',(#2957),#1635,.F.);
#24817=ADVANCED_FACE('',(#2958),#1636,.T.);
#24818=ADVANCED_FACE('',(#2959),#1637,.F.);
#24819=ADVANCED_FACE('',(#2960),#1638,.F.);
#24820=ADVANCED_FACE('',(#2961),#1639,.F.);
#24821=ADVANCED_FACE('',(#2962),#1640,.T.);
#24822=ADVANCED_FACE('',(#2963),#1641,.F.);
#24823=ADVANCED_FACE('',(#2964),#1642,.F.);
#24824=ADVANCED_FACE('',(#2965),#1643,.F.);
#24825=ADVANCED_FACE('',(#2966),#1644,.T.);
#24826=ADVANCED_FACE('',(#2967),#1645,.F.);
#24827=ADVANCED_FACE('',(#2968),#1646,.F.);
#24828=ADVANCED_FACE('',(#2969),#1647,.F.);
#24829=ADVANCED_FACE('',(#2970),#1648,.T.);
#24830=ADVANCED_FACE('',(#2971),#1649,.F.);
#24831=ADVANCED_FACE('',(#2972),#1650,.F.);
#24832=ADVANCED_FACE('',(#2973),#1651,.F.);
#24833=ADVANCED_FACE('',(#2974),#1652,.T.);
#24834=ADVANCED_FACE('',(#2975),#1653,.F.);
#24835=ADVANCED_FACE('',(#2976),#1654,.F.);
#24836=ADVANCED_FACE('',(#2977),#1655,.F.);
#24837=ADVANCED_FACE('',(#2978),#1656,.T.);
#24838=ADVANCED_FACE('',(#2979),#1657,.F.);
#24839=ADVANCED_FACE('',(#2980),#1658,.F.);
#24840=ADVANCED_FACE('',(#2981),#1659,.F.);
#24841=ADVANCED_FACE('',(#2982),#1660,.T.);
#24842=ADVANCED_FACE('',(#2983),#1661,.F.);
#24843=ADVANCED_FACE('',(#2984),#1662,.F.);
#24844=ADVANCED_FACE('',(#2985),#1663,.F.);
#24845=ADVANCED_FACE('',(#2986),#1664,.T.);
#24846=ADVANCED_FACE('',(#2987),#1665,.F.);
#24847=ADVANCED_FACE('',(#2988),#1666,.F.);
#24848=ADVANCED_FACE('',(#2989),#1667,.F.);
#24849=ADVANCED_FACE('',(#2990),#1668,.T.);
#24850=ADVANCED_FACE('',(#2991),#1669,.F.);
#24851=ADVANCED_FACE('',(#2992),#1670,.F.);
#24852=ADVANCED_FACE('',(#2993),#1671,.F.);
#24853=ADVANCED_FACE('',(#2994),#1672,.T.);
#24854=ADVANCED_FACE('',(#2995),#1673,.F.);
#24855=ADVANCED_FACE('',(#2996),#1674,.F.);
#24856=ADVANCED_FACE('',(#2997),#1675,.F.);
#24857=ADVANCED_FACE('',(#2998),#1676,.T.);
#24858=ADVANCED_FACE('',(#2999),#1677,.F.);
#24859=ADVANCED_FACE('',(#3000),#1678,.F.);
#24860=ADVANCED_FACE('',(#3001),#1679,.F.);
#24861=ADVANCED_FACE('',(#3002),#1680,.T.);
#24862=ADVANCED_FACE('',(#3003),#1681,.F.);
#24863=ADVANCED_FACE('',(#3004),#1682,.F.);
#24864=ADVANCED_FACE('',(#3005),#1683,.F.);
#24865=ADVANCED_FACE('',(#3006),#1684,.T.);
#24866=ADVANCED_FACE('',(#3007),#1685,.F.);
#24867=ADVANCED_FACE('',(#3008),#1686,.F.);
#24868=ADVANCED_FACE('',(#3009),#1687,.F.);
#24869=ADVANCED_FACE('',(#3010),#1688,.T.);
#24870=ADVANCED_FACE('',(#3011),#1689,.F.);
#24871=ADVANCED_FACE('',(#3012),#1690,.F.);
#24872=ADVANCED_FACE('',(#3013),#1691,.F.);
#24873=ADVANCED_FACE('',(#3014),#1692,.T.);
#24874=ADVANCED_FACE('',(#3015),#1693,.F.);
#24875=ADVANCED_FACE('',(#3016),#1694,.F.);
#24876=ADVANCED_FACE('',(#3017),#1695,.F.);
#24877=ADVANCED_FACE('',(#3018),#1696,.T.);
#24878=ADVANCED_FACE('',(#3019),#1697,.F.);
#24879=ADVANCED_FACE('',(#3020),#1698,.F.);
#24880=ADVANCED_FACE('',(#3021),#1699,.F.);
#24881=ADVANCED_FACE('',(#3022),#1700,.T.);
#24882=ADVANCED_FACE('',(#3023),#1701,.F.);
#24883=ADVANCED_FACE('',(#3024),#1702,.F.);
#24884=ADVANCED_FACE('',(#3025),#1703,.F.);
#24885=ADVANCED_FACE('',(#3026),#1704,.T.);
#24886=ADVANCED_FACE('',(#3027),#1705,.F.);
#24887=ADVANCED_FACE('',(#3028),#1706,.F.);
#24888=ADVANCED_FACE('',(#3029),#1707,.F.);
#24889=ADVANCED_FACE('',(#3030),#1708,.T.);
#24890=ADVANCED_FACE('',(#3031),#1709,.F.);
#24891=ADVANCED_FACE('',(#3032),#1710,.F.);
#24892=ADVANCED_FACE('',(#3033),#1711,.F.);
#24893=ADVANCED_FACE('',(#3034),#1712,.T.);
#24894=ADVANCED_FACE('',(#3035),#1713,.F.);
#24895=ADVANCED_FACE('',(#3036),#1714,.F.);
#24896=ADVANCED_FACE('',(#3037),#1715,.F.);
#24897=ADVANCED_FACE('',(#3038),#1716,.T.);
#24898=ADVANCED_FACE('',(#3039),#1717,.F.);
#24899=ADVANCED_FACE('',(#3040),#1718,.F.);
#24900=ADVANCED_FACE('',(#3041),#1719,.F.);
#24901=ADVANCED_FACE('',(#3042),#1720,.T.);
#24902=ADVANCED_FACE('',(#3043),#1721,.F.);
#24903=ADVANCED_FACE('',(#3044),#1722,.F.);
#24904=ADVANCED_FACE('',(#3045),#1723,.F.);
#24905=ADVANCED_FACE('',(#3046),#1724,.T.);
#24906=ADVANCED_FACE('',(#3047),#1725,.F.);
#24907=ADVANCED_FACE('',(#3048),#1726,.F.);
#24908=ADVANCED_FACE('',(#3049),#1727,.F.);
#24909=ADVANCED_FACE('',(#3050),#1728,.T.);
#24910=ADVANCED_FACE('',(#3051),#1729,.F.);
#24911=ADVANCED_FACE('',(#3052),#1730,.F.);
#24912=ADVANCED_FACE('',(#3053),#1731,.F.);
#24913=ADVANCED_FACE('',(#3054),#1732,.T.);
#24914=ADVANCED_FACE('',(#3055),#1733,.F.);
#24915=ADVANCED_FACE('',(#3056),#1734,.F.);
#24916=ADVANCED_FACE('',(#3057),#1735,.F.);
#24917=ADVANCED_FACE('',(#3058),#1736,.F.);
#24918=ADVANCED_FACE('',(#3059),#1737,.F.);
#24919=ADVANCED_FACE('',(#3060),#1738,.F.);
#24920=ADVANCED_FACE('',(#3061),#1739,.F.);
#24921=ADVANCED_FACE('',(#3062),#1740,.F.);
#24922=ADVANCED_FACE('',(#3063),#1741,.F.);
#24923=ADVANCED_FACE('',(#3064),#1742,.T.);
#24924=ADVANCED_FACE('',(#3065),#23601,.T.);
#24925=ADVANCED_FACE('',(#3066),#582,.T.);
#24926=ADVANCED_FACE('',(#3067),#23602,.F.);
#24927=ADVANCED_FACE('',(#3068),#583,.T.);
#24928=ADVANCED_FACE('',(#3069,#674),#1743,.T.);
#24929=ADVANCED_FACE('',(#3070,#675,#676,#677,#678,#679,#680,#681,#682,
#683,#684,#685,#686,#687,#688,#689,#690,#691,#692,#693,#694,#695,#696,#697,
#698,#699,#700,#701,#702,#703,#704,#705,#706,#707,#708,#709),#584,.T.);
#24930=ADVANCED_FACE('',(#3071),#23603,.T.);
#24931=ADVANCED_FACE('',(#3072,#710),#1744,.T.);
#24949=CLOSED_SHELL('',(#24726,#24727,#24728,#24729,#24730,#24731,#24732,
#24733,#24734,#24735,#24736,#24737,#24738,#24739,#24740,#24741,#24742,#24743,
#24744,#24745,#24746,#24747,#24748,#24749,#24750,#24751,#24752,#24753,#24754,
#24755,#24756,#24757,#24758,#24759,#24760,#24761,#24762,#24763,#24764,#24765,
#24766,#24767,#24768,#24769,#24770,#24771,#24772,#24773,#24774,#24775,#24776,
#24777,#24778,#24779,#24780,#24781,#24782,#24783,#24784,#24785,#24786,#24787,
#24788,#24789,#24790,#24791,#24792,#24793,#24794,#24795,#24796,#24797,#24798,
#24799,#24800,#24801,#24802,#24803,#24804,#24805,#24806,#24807,#24808,#24809,
#24810,#24811,#24812,#24813,#24814,#24815,#24816,#24817,#24818,#24819,#24820,
#24821,#24822,#24823,#24824,#24825,#24826,#24827,#24828,#24829,#24830,#24831,
#24832,#24833,#24834,#24835,#24836,#24837,#24838,#24839,#24840,#24841,#24842,
#24843,#24844,#24845,#24846,#24847,#24848,#24849,#24850,#24851,#24852,#24853,
#24854,#24855,#24856,#24857,#24858,#24859,#24860,#24861,#24862,#24863,#24864,
#24865,#24866,#24867,#24868,#24869,#24870,#24871,#24872,#24873,#24874,#24875,
#24876,#24877,#24878,#24879,#24880,#24881,#24882,#24883,#24884,#24885,#24886,
#24887,#24888,#24889,#24890,#24891,#24892,#24893,#24894,#24895,#24896,#24897,
#24898,#24899,#24900,#24901,#24902,#24903,#24904,#24905,#24906,#24907,#24908,
#24909,#24910,#24911,#24912,#24913,#24914,#24915,#24916,#24917,#24918,#24919,
#24920,#24921,#24922,#24923,#24924,#24925,#24926,#24927,#24928,#24929,#24930,
#24931));
#26605=AXIS2_PLACEMENT_3D('',#40729,#32480,#32481);
#26606=AXIS2_PLACEMENT_3D('',#40730,#32482,#32483);
#26607=AXIS2_PLACEMENT_3D('',#40752,#32485,#32486);
#26608=AXIS2_PLACEMENT_3D('',#40763,#32487,#32488);
#26609=AXIS2_PLACEMENT_3D('',#40847,#32490,#32491);
#26610=AXIS2_PLACEMENT_3D('',#40937,#32493,#32494);
#26611=AXIS2_PLACEMENT_3D('',#41027,#32496,#32497);
#26612=AXIS2_PLACEMENT_3D('',#41111,#32499,#32500);
#26613=AXIS2_PLACEMENT_3D('',#41201,#32502,#32503);
#26614=AXIS2_PLACEMENT_3D('',#41291,#32505,#32506);
#26615=AXIS2_PLACEMENT_3D('',#41375,#32508,#32509);
#26616=AXIS2_PLACEMENT_3D('',#41465,#32511,#32512);
#26617=AXIS2_PLACEMENT_3D('',#41543,#32514,#32515);
#26618=AXIS2_PLACEMENT_3D('',#41591,#32517,#32518);
#26619=AXIS2_PLACEMENT_3D('',#41645,#32520,#32521);
#26620=AXIS2_PLACEMENT_3D('',#41729,#32523,#32524);
#26621=AXIS2_PLACEMENT_3D('',#41813,#32526,#32527);
#26622=AXIS2_PLACEMENT_3D('',#41903,#32529,#32530);
#26623=AXIS2_PLACEMENT_3D('',#41993,#32532,#32533);
#26624=AXIS2_PLACEMENT_3D('',#42077,#32535,#32536);
#26625=AXIS2_PLACEMENT_3D('',#42167,#32538,#32539);
#26626=AXIS2_PLACEMENT_3D('',#42257,#32541,#32542);
#26627=AXIS2_PLACEMENT_3D('',#42341,#32544,#32545);
#26628=AXIS2_PLACEMENT_3D('',#42346,#32547,#32548);
#26629=AXIS2_PLACEMENT_3D('',#42427,#32549,#32550);
#26630=AXIS2_PLACEMENT_3D('',#42444,#32552,#32553);
#26631=AXIS2_PLACEMENT_3D('',#42453,#32554,#32555);
#26632=AXIS2_PLACEMENT_3D('',#42490,#32557,#32558);
#26633=AXIS2_PLACEMENT_3D('',#42527,#32560,#32561);
#26634=AXIS2_PLACEMENT_3D('',#42565,#32563,#32564);
#26635=AXIS2_PLACEMENT_3D('',#42602,#32566,#32567);
#26636=AXIS2_PLACEMENT_3D('',#42639,#32569,#32570);
#26637=AXIS2_PLACEMENT_3D('',#42677,#32572,#32573);
#26638=AXIS2_PLACEMENT_3D('',#42714,#32575,#32576);
#26639=AXIS2_PLACEMENT_3D('',#42751,#32578,#32579);
#26640=AXIS2_PLACEMENT_3D('',#42782,#32581,#32582);
#26641=AXIS2_PLACEMENT_3D('',#42806,#32584,#32585);
#26642=AXIS2_PLACEMENT_3D('',#42834,#32587,#32588);
#26643=AXIS2_PLACEMENT_3D('',#42871,#32590,#32591);
#26644=AXIS2_PLACEMENT_3D('',#42908,#32593,#32594);
#26645=AXIS2_PLACEMENT_3D('',#42945,#32596,#32597);
#26646=AXIS2_PLACEMENT_3D('',#42983,#32599,#32600);
#26647=AXIS2_PLACEMENT_3D('',#43020,#32602,#32603);
#26648=AXIS2_PLACEMENT_3D('',#43057,#32605,#32606);
#26649=AXIS2_PLACEMENT_3D('',#43095,#32608,#32609);
#26650=AXIS2_PLACEMENT_3D('',#43132,#32611,#32612);
#26651=AXIS2_PLACEMENT_3D('',#43237,#32613,#32614);
#26652=AXIS2_PLACEMENT_3D('',#44451,#32615,#32616);
#26653=AXIS2_PLACEMENT_3D('',#44453,#32617,#32618);
#26654=AXIS2_PLACEMENT_3D('',#44454,#32619,#32620);
#26655=AXIS2_PLACEMENT_3D('',#44559,#32621,#32622);
#26656=AXIS2_PLACEMENT_3D('',#44560,#32623,#32624);
#26657=AXIS2_PLACEMENT_3D('',#45569,#32625,#32626);
#26658=AXIS2_PLACEMENT_3D('',#45578,#32631,#32632);
#26659=AXIS2_PLACEMENT_3D('',#45580,#32633,#32634);
#26660=AXIS2_PLACEMENT_3D('',#45582,#32636,#32637);
#26661=AXIS2_PLACEMENT_3D('',#45586,#32640,#32641);
#26662=AXIS2_PLACEMENT_3D('',#45587,#32642,#32643);
#26663=AXIS2_PLACEMENT_3D('',#45588,#32644,#32645);
#26664=AXIS2_PLACEMENT_3D('',#45597,#32650,#32651);
#26665=AXIS2_PLACEMENT_3D('',#45599,#32652,#32653);
#26666=AXIS2_PLACEMENT_3D('',#45601,#32655,#32656);
#26667=AXIS2_PLACEMENT_3D('',#45605,#32659,#32660);
#26668=AXIS2_PLACEMENT_3D('',#45606,#32661,#32662);
#26669=AXIS2_PLACEMENT_3D('',#45607,#32663,#32664);
#26670=AXIS2_PLACEMENT_3D('',#45616,#32669,#32670);
#26671=AXIS2_PLACEMENT_3D('',#45618,#32671,#32672);
#26672=AXIS2_PLACEMENT_3D('',#45620,#32674,#32675);
#26673=AXIS2_PLACEMENT_3D('',#45624,#32678,#32679);
#26674=AXIS2_PLACEMENT_3D('',#45625,#32680,#32681);
#26675=AXIS2_PLACEMENT_3D('',#45626,#32682,#32683);
#26676=AXIS2_PLACEMENT_3D('',#45635,#32688,#32689);
#26677=AXIS2_PLACEMENT_3D('',#45637,#32690,#32691);
#26678=AXIS2_PLACEMENT_3D('',#45639,#32693,#32694);
#26679=AXIS2_PLACEMENT_3D('',#45643,#32697,#32698);
#26680=AXIS2_PLACEMENT_3D('',#45644,#32699,#32700);
#26681=AXIS2_PLACEMENT_3D('',#45645,#32701,#32702);
#26682=AXIS2_PLACEMENT_3D('',#45654,#32707,#32708);
#26683=AXIS2_PLACEMENT_3D('',#45656,#32709,#32710);
#26684=AXIS2_PLACEMENT_3D('',#45658,#32712,#32713);
#26685=AXIS2_PLACEMENT_3D('',#45662,#32716,#32717);
#26686=AXIS2_PLACEMENT_3D('',#45663,#32718,#32719);
#26687=AXIS2_PLACEMENT_3D('',#45664,#32720,#32721);
#26688=AXIS2_PLACEMENT_3D('',#45673,#32726,#32727);
#26689=AXIS2_PLACEMENT_3D('',#45675,#32728,#32729);
#26690=AXIS2_PLACEMENT_3D('',#45677,#32731,#32732);
#26691=AXIS2_PLACEMENT_3D('',#45681,#32735,#32736);
#26692=AXIS2_PLACEMENT_3D('',#45682,#32737,#32738);
#26693=AXIS2_PLACEMENT_3D('',#45683,#32739,#32740);
#26694=AXIS2_PLACEMENT_3D('',#45692,#32745,#32746);
#26695=AXIS2_PLACEMENT_3D('',#45694,#32747,#32748);
#26696=AXIS2_PLACEMENT_3D('',#45696,#32750,#32751);
#26697=AXIS2_PLACEMENT_3D('',#45700,#32754,#32755);
#26698=AXIS2_PLACEMENT_3D('',#45701,#32756,#32757);
#26699=AXIS2_PLACEMENT_3D('',#45702,#32758,#32759);
#26700=AXIS2_PLACEMENT_3D('',#45711,#32764,#32765);
#26701=AXIS2_PLACEMENT_3D('',#45713,#32766,#32767);
#26702=AXIS2_PLACEMENT_3D('',#45715,#32769,#32770);
#26703=AXIS2_PLACEMENT_3D('',#45719,#32773,#32774);
#26704=AXIS2_PLACEMENT_3D('',#45720,#32775,#32776);
#26705=AXIS2_PLACEMENT_3D('',#45721,#32777,#32778);
#26706=AXIS2_PLACEMENT_3D('',#45730,#32783,#32784);
#26707=AXIS2_PLACEMENT_3D('',#45732,#32785,#32786);
#26708=AXIS2_PLACEMENT_3D('',#45734,#32788,#32789);
#26709=AXIS2_PLACEMENT_3D('',#45738,#32792,#32793);
#26710=AXIS2_PLACEMENT_3D('',#45739,#32794,#32795);
#26711=AXIS2_PLACEMENT_3D('',#45740,#32796,#32797);
#26712=AXIS2_PLACEMENT_3D('',#45749,#32802,#32803);
#26713=AXIS2_PLACEMENT_3D('',#45751,#32804,#32805);
#26714=AXIS2_PLACEMENT_3D('',#45753,#32807,#32808);
#26715=AXIS2_PLACEMENT_3D('',#45757,#32811,#32812);
#26716=AXIS2_PLACEMENT_3D('',#45758,#32813,#32814);
#26717=AXIS2_PLACEMENT_3D('',#45759,#32815,#32816);
#26718=AXIS2_PLACEMENT_3D('',#45768,#32821,#32822);
#26719=AXIS2_PLACEMENT_3D('',#45770,#32823,#32824);
#26720=AXIS2_PLACEMENT_3D('',#45772,#32826,#32827);
#26721=AXIS2_PLACEMENT_3D('',#45776,#32830,#32831);
#26722=AXIS2_PLACEMENT_3D('',#45777,#32832,#32833);
#26723=AXIS2_PLACEMENT_3D('',#45778,#32834,#32835);
#26724=AXIS2_PLACEMENT_3D('',#45787,#32840,#32841);
#26725=AXIS2_PLACEMENT_3D('',#45789,#32842,#32843);
#26726=AXIS2_PLACEMENT_3D('',#45791,#32845,#32846);
#26727=AXIS2_PLACEMENT_3D('',#45795,#32849,#32850);
#26728=AXIS2_PLACEMENT_3D('',#45796,#32851,#32852);
#26729=AXIS2_PLACEMENT_3D('',#45797,#32853,#32854);
#26730=AXIS2_PLACEMENT_3D('',#45806,#32859,#32860);
#26731=AXIS2_PLACEMENT_3D('',#45808,#32861,#32862);
#26732=AXIS2_PLACEMENT_3D('',#45810,#32864,#32865);
#26733=AXIS2_PLACEMENT_3D('',#45814,#32868,#32869);
#26734=AXIS2_PLACEMENT_3D('',#45815,#32870,#32871);
#26735=AXIS2_PLACEMENT_3D('',#45816,#32872,#32873);
#26736=AXIS2_PLACEMENT_3D('',#45825,#32878,#32879);
#26737=AXIS2_PLACEMENT_3D('',#45827,#32880,#32881);
#26738=AXIS2_PLACEMENT_3D('',#45829,#32883,#32884);
#26739=AXIS2_PLACEMENT_3D('',#45833,#32887,#32888);
#26740=AXIS2_PLACEMENT_3D('',#45834,#32889,#32890);
#26741=AXIS2_PLACEMENT_3D('',#45835,#32891,#32892);
#26742=AXIS2_PLACEMENT_3D('',#45844,#32897,#32898);
#26743=AXIS2_PLACEMENT_3D('',#45846,#32899,#32900);
#26744=AXIS2_PLACEMENT_3D('',#45848,#32902,#32903);
#26745=AXIS2_PLACEMENT_3D('',#45852,#32906,#32907);
#26746=AXIS2_PLACEMENT_3D('',#45853,#32908,#32909);
#26747=AXIS2_PLACEMENT_3D('',#45854,#32910,#32911);
#26748=AXIS2_PLACEMENT_3D('',#45863,#32916,#32917);
#26749=AXIS2_PLACEMENT_3D('',#45865,#32918,#32919);
#26750=AXIS2_PLACEMENT_3D('',#45867,#32921,#32922);
#26751=AXIS2_PLACEMENT_3D('',#45871,#32925,#32926);
#26752=AXIS2_PLACEMENT_3D('',#45872,#32927,#32928);
#26753=AXIS2_PLACEMENT_3D('',#45873,#32929,#32930);
#26754=AXIS2_PLACEMENT_3D('',#45882,#32935,#32936);
#26755=AXIS2_PLACEMENT_3D('',#45884,#32937,#32938);
#26756=AXIS2_PLACEMENT_3D('',#45886,#32940,#32941);
#26757=AXIS2_PLACEMENT_3D('',#45890,#32944,#32945);
#26758=AXIS2_PLACEMENT_3D('',#45891,#32946,#32947);
#26759=AXIS2_PLACEMENT_3D('',#45892,#32948,#32949);
#26760=AXIS2_PLACEMENT_3D('',#45901,#32954,#32955);
#26761=AXIS2_PLACEMENT_3D('',#45903,#32956,#32957);
#26762=AXIS2_PLACEMENT_3D('',#45906,#32959,#32960);
#26763=AXIS2_PLACEMENT_3D('',#45907,#32961,#32962);
#26764=AXIS2_PLACEMENT_3D('',#45911,#32965,#32966);
#26765=AXIS2_PLACEMENT_3D('',#45913,#32967,#32968);
#26766=AXIS2_PLACEMENT_3D('',#45914,#32969,#32970);
#26767=AXIS2_PLACEMENT_3D('',#45915,#32971,#32972);
#26768=AXIS2_PLACEMENT_3D('',#45924,#32977,#32978);
#26769=AXIS2_PLACEMENT_3D('',#45926,#32979,#32980);
#26770=AXIS2_PLACEMENT_3D('',#45928,#32982,#32983);
#26771=AXIS2_PLACEMENT_3D('',#45932,#32986,#32987);
#26772=AXIS2_PLACEMENT_3D('',#45933,#32988,#32989);
#26773=AXIS2_PLACEMENT_3D('',#45934,#32990,#32991);
#26774=AXIS2_PLACEMENT_3D('',#45943,#32996,#32997);
#26775=AXIS2_PLACEMENT_3D('',#45945,#32998,#32999);
#26776=AXIS2_PLACEMENT_3D('',#45947,#33001,#33002);
#26777=AXIS2_PLACEMENT_3D('',#45951,#33005,#33006);
#26778=AXIS2_PLACEMENT_3D('',#45952,#33007,#33008);
#26779=AXIS2_PLACEMENT_3D('',#45953,#33009,#33010);
#26780=AXIS2_PLACEMENT_3D('',#45962,#33015,#33016);
#26781=AXIS2_PLACEMENT_3D('',#45964,#33017,#33018);
#26782=AXIS2_PLACEMENT_3D('',#45966,#33020,#33021);
#26783=AXIS2_PLACEMENT_3D('',#45970,#33024,#33025);
#26784=AXIS2_PLACEMENT_3D('',#45971,#33026,#33027);
#26785=AXIS2_PLACEMENT_3D('',#45972,#33028,#33029);
#26786=AXIS2_PLACEMENT_3D('',#45981,#33034,#33035);
#26787=AXIS2_PLACEMENT_3D('',#45983,#33036,#33037);
#26788=AXIS2_PLACEMENT_3D('',#45985,#33039,#33040);
#26789=AXIS2_PLACEMENT_3D('',#45989,#33043,#33044);
#26790=AXIS2_PLACEMENT_3D('',#45990,#33045,#33046);
#26791=AXIS2_PLACEMENT_3D('',#45991,#33047,#33048);
#26792=AXIS2_PLACEMENT_3D('',#46000,#33053,#33054);
#26793=AXIS2_PLACEMENT_3D('',#46002,#33055,#33056);
#26794=AXIS2_PLACEMENT_3D('',#46004,#33058,#33059);
#26795=AXIS2_PLACEMENT_3D('',#46008,#33062,#33063);
#26796=AXIS2_PLACEMENT_3D('',#46009,#33064,#33065);
#26797=AXIS2_PLACEMENT_3D('',#46010,#33066,#33067);
#26798=AXIS2_PLACEMENT_3D('',#46019,#33072,#33073);
#26799=AXIS2_PLACEMENT_3D('',#46021,#33074,#33075);
#26800=AXIS2_PLACEMENT_3D('',#46023,#33077,#33078);
#26801=AXIS2_PLACEMENT_3D('',#46027,#33081,#33082);
#26802=AXIS2_PLACEMENT_3D('',#46028,#33083,#33084);
#26803=AXIS2_PLACEMENT_3D('',#46029,#33085,#33086);
#26804=AXIS2_PLACEMENT_3D('',#46038,#33091,#33092);
#26805=AXIS2_PLACEMENT_3D('',#46040,#33093,#33094);
#26806=AXIS2_PLACEMENT_3D('',#46042,#33096,#33097);
#26807=AXIS2_PLACEMENT_3D('',#46046,#33100,#33101);
#26808=AXIS2_PLACEMENT_3D('',#46047,#33102,#33103);
#26809=AXIS2_PLACEMENT_3D('',#46048,#33104,#33105);
#26810=AXIS2_PLACEMENT_3D('',#46057,#33110,#33111);
#26811=AXIS2_PLACEMENT_3D('',#46059,#33112,#33113);
#26812=AXIS2_PLACEMENT_3D('',#46061,#33115,#33116);
#26813=AXIS2_PLACEMENT_3D('',#46065,#33119,#33120);
#26814=AXIS2_PLACEMENT_3D('',#46066,#33121,#33122);
#26815=AXIS2_PLACEMENT_3D('',#46067,#33123,#33124);
#26816=AXIS2_PLACEMENT_3D('',#46076,#33129,#33130);
#26817=AXIS2_PLACEMENT_3D('',#46078,#33131,#33132);
#26818=AXIS2_PLACEMENT_3D('',#46080,#33134,#33135);
#26819=AXIS2_PLACEMENT_3D('',#46084,#33138,#33139);
#26820=AXIS2_PLACEMENT_3D('',#46085,#33140,#33141);
#26821=AXIS2_PLACEMENT_3D('',#46086,#33142,#33143);
#26822=AXIS2_PLACEMENT_3D('',#46095,#33148,#33149);
#26823=AXIS2_PLACEMENT_3D('',#46097,#33150,#33151);
#26824=AXIS2_PLACEMENT_3D('',#46099,#33153,#33154);
#26825=AXIS2_PLACEMENT_3D('',#46103,#33157,#33158);
#26826=AXIS2_PLACEMENT_3D('',#46104,#33159,#33160);
#26827=AXIS2_PLACEMENT_3D('',#46105,#33161,#33162);
#26828=AXIS2_PLACEMENT_3D('',#46114,#33167,#33168);
#26829=AXIS2_PLACEMENT_3D('',#46116,#33169,#33170);
#26830=AXIS2_PLACEMENT_3D('',#46118,#33172,#33173);
#26831=AXIS2_PLACEMENT_3D('',#46122,#33176,#33177);
#26832=AXIS2_PLACEMENT_3D('',#46123,#33178,#33179);
#26833=AXIS2_PLACEMENT_3D('',#46124,#33180,#33181);
#26834=AXIS2_PLACEMENT_3D('',#46133,#33186,#33187);
#26835=AXIS2_PLACEMENT_3D('',#46135,#33188,#33189);
#26836=AXIS2_PLACEMENT_3D('',#46137,#33191,#33192);
#26837=AXIS2_PLACEMENT_3D('',#46141,#33195,#33196);
#26838=AXIS2_PLACEMENT_3D('',#46142,#33197,#33198);
#26839=AXIS2_PLACEMENT_3D('',#46143,#33199,#33200);
#26840=AXIS2_PLACEMENT_3D('',#46152,#33205,#33206);
#26841=AXIS2_PLACEMENT_3D('',#46154,#33207,#33208);
#26842=AXIS2_PLACEMENT_3D('',#46156,#33210,#33211);
#26843=AXIS2_PLACEMENT_3D('',#46160,#33214,#33215);
#26844=AXIS2_PLACEMENT_3D('',#46161,#33216,#33217);
#26845=AXIS2_PLACEMENT_3D('',#46162,#33218,#33219);
#26846=AXIS2_PLACEMENT_3D('',#46171,#33224,#33225);
#26847=AXIS2_PLACEMENT_3D('',#46173,#33226,#33227);
#26848=AXIS2_PLACEMENT_3D('',#46175,#33229,#33230);
#26849=AXIS2_PLACEMENT_3D('',#46179,#33233,#33234);
#26850=AXIS2_PLACEMENT_3D('',#46180,#33235,#33236);
#26851=AXIS2_PLACEMENT_3D('',#46181,#33237,#33238);
#26852=AXIS2_PLACEMENT_3D('',#46190,#33243,#33244);
#26853=AXIS2_PLACEMENT_3D('',#46192,#33245,#33246);
#26854=AXIS2_PLACEMENT_3D('',#46194,#33248,#33249);
#26855=AXIS2_PLACEMENT_3D('',#46198,#33252,#33253);
#26856=AXIS2_PLACEMENT_3D('',#46199,#33254,#33255);
#26857=AXIS2_PLACEMENT_3D('',#46200,#33256,#33257);
#26858=AXIS2_PLACEMENT_3D('',#46209,#33262,#33263);
#26859=AXIS2_PLACEMENT_3D('',#46211,#33264,#33265);
#26860=AXIS2_PLACEMENT_3D('',#46213,#33267,#33268);
#26861=AXIS2_PLACEMENT_3D('',#46217,#33271,#33272);
#26862=AXIS2_PLACEMENT_3D('',#46218,#33273,#33274);
#26863=AXIS2_PLACEMENT_3D('',#46219,#33275,#33276);
#26864=AXIS2_PLACEMENT_3D('',#46228,#33281,#33282);
#26865=AXIS2_PLACEMENT_3D('',#46230,#33283,#33284);
#26866=AXIS2_PLACEMENT_3D('',#46232,#33286,#33287);
#26867=AXIS2_PLACEMENT_3D('',#46236,#33290,#33291);
#26868=AXIS2_PLACEMENT_3D('',#46237,#33292,#33293);
#26869=AXIS2_PLACEMENT_3D('',#46238,#33294,#33295);
#26870=AXIS2_PLACEMENT_3D('',#46247,#33300,#33301);
#26871=AXIS2_PLACEMENT_3D('',#46249,#33302,#33303);
#26872=AXIS2_PLACEMENT_3D('',#46251,#33305,#33306);
#26873=AXIS2_PLACEMENT_3D('',#46255,#33309,#33310);
#26874=AXIS2_PLACEMENT_3D('',#46256,#33311,#33312);
#26875=AXIS2_PLACEMENT_3D('',#46257,#33313,#33314);
#26876=AXIS2_PLACEMENT_3D('',#46266,#33319,#33320);
#26877=AXIS2_PLACEMENT_3D('',#46272,#33324,#33325);
#26878=AXIS2_PLACEMENT_3D('',#46278,#33329,#33330);
#26879=AXIS2_PLACEMENT_3D('',#46284,#33334,#33335);
#26880=AXIS2_PLACEMENT_3D('',#46290,#33339,#33340);
#26881=AXIS2_PLACEMENT_3D('',#46293,#33343,#33344);
#26882=AXIS2_PLACEMENT_3D('',#46294,#33345,#33346);
#26883=AXIS2_PLACEMENT_3D('',#46296,#33347,#33348);
#26884=AXIS2_PLACEMENT_3D('',#46297,#33349,#33350);
#26885=AXIS2_PLACEMENT_3D('',#46299,#33352,#33353);
#26886=AXIS2_PLACEMENT_3D('',#46300,#33354,#33355);
#26887=AXIS2_PLACEMENT_3D('',#46301,#33356,#33357);
#26888=AXIS2_PLACEMENT_3D('',#46303,#33358,#33359);
#26889=AXIS2_PLACEMENT_3D('',#46305,#33361,#33362);
#26890=AXIS2_PLACEMENT_3D('',#46307,#33363,#33364);
#26891=AXIS2_PLACEMENT_3D('',#46309,#33366,#33367);
#26892=AXIS2_PLACEMENT_3D('',#46311,#33368,#33369);
#26893=AXIS2_PLACEMENT_3D('',#46312,#33370,#33371);
#26894=AXIS2_PLACEMENT_3D('',#46314,#33372,#33373);
#26895=AXIS2_PLACEMENT_3D('',#46317,#33376,#33377);
#26896=AXIS2_PLACEMENT_3D('',#46319,#33378,#33379);
#26897=AXIS2_PLACEMENT_3D('',#46321,#33381,#33382);
#32480=DIRECTION('axis',(0.,0.,1.));
#32481=DIRECTION('refdir',(1.,0.,0.));
#32482=DIRECTION('center_axis',(1.,0.,0.));
#32483=DIRECTION('ref_axis',(0.,1.,0.));
#32484=DIRECTION('',(-1.,0.,0.));
#32485=DIRECTION('center_axis',(1.,0.,0.));
#32486=DIRECTION('ref_axis',(0.,1.,0.));
#32487=DIRECTION('center_axis',(1.,0.,0.));
#32488=DIRECTION('ref_axis',(0.,1.,0.));
#32489=DIRECTION('',(-1.,0.,0.));
#32490=DIRECTION('center_axis',(1.,0.,0.));
#32491=DIRECTION('ref_axis',(0.,1.,0.));
#32492=DIRECTION('',(-1.,0.,0.));
#32493=DIRECTION('center_axis',(1.,0.,0.));
#32494=DIRECTION('ref_axis',(0.,1.,0.));
#32495=DIRECTION('',(-1.,0.,0.));
#32496=DIRECTION('center_axis',(1.,0.,0.));
#32497=DIRECTION('ref_axis',(0.,1.,0.));
#32498=DIRECTION('',(-1.,0.,0.));
#32499=DIRECTION('center_axis',(1.,0.,0.));
#32500=DIRECTION('ref_axis',(0.,1.,0.));
#32501=DIRECTION('',(-1.,0.,0.));
#32502=DIRECTION('center_axis',(1.,0.,0.));
#32503=DIRECTION('ref_axis',(0.,1.,0.));
#32504=DIRECTION('',(-1.,0.,0.));
#32505=DIRECTION('center_axis',(1.,0.,0.));
#32506=DIRECTION('ref_axis',(0.,1.,0.));
#32507=DIRECTION('',(-1.,0.,0.));
#32508=DIRECTION('center_axis',(1.,0.,0.));
#32509=DIRECTION('ref_axis',(0.,1.,0.));
#32510=DIRECTION('',(-1.,0.,0.));
#32511=DIRECTION('center_axis',(1.,0.,0.));
#32512=DIRECTION('ref_axis',(0.,1.,0.));
#32513=DIRECTION('',(-1.,0.,0.));
#32514=DIRECTION('center_axis',(1.,0.,0.));
#32515=DIRECTION('ref_axis',(0.,1.,0.));
#32516=DIRECTION('',(-1.,0.,0.));
#32517=DIRECTION('center_axis',(1.,0.,0.));
#32518=DIRECTION('ref_axis',(0.,1.,0.));
#32519=DIRECTION('',(-1.,0.,0.));
#32520=DIRECTION('center_axis',(1.,0.,0.));
#32521=DIRECTION('ref_axis',(0.,1.,0.));
#32522=DIRECTION('',(-1.,0.,0.));
#32523=DIRECTION('center_axis',(1.,0.,0.));
#32524=DIRECTION('ref_axis',(0.,1.,0.));
#32525=DIRECTION('',(-1.,0.,0.));
#32526=DIRECTION('center_axis',(1.,0.,0.));
#32527=DIRECTION('ref_axis',(0.,1.,0.));
#32528=DIRECTION('',(-1.,0.,0.));
#32529=DIRECTION('center_axis',(1.,0.,0.));
#32530=DIRECTION('ref_axis',(0.,1.,0.));
#32531=DIRECTION('',(-1.,0.,0.));
#32532=DIRECTION('center_axis',(1.,0.,0.));
#32533=DIRECTION('ref_axis',(0.,1.,0.));
#32534=DIRECTION('',(-1.,0.,0.));
#32535=DIRECTION('center_axis',(1.,0.,0.));
#32536=DIRECTION('ref_axis',(0.,1.,0.));
#32537=DIRECTION('',(-1.,0.,0.));
#32538=DIRECTION('center_axis',(1.,0.,0.));
#32539=DIRECTION('ref_axis',(0.,1.,0.));
#32540=DIRECTION('',(-1.,0.,0.));
#32541=DIRECTION('center_axis',(1.,0.,0.));
#32542=DIRECTION('ref_axis',(0.,1.,0.));
#32543=DIRECTION('',(-1.,0.,0.));
#32544=DIRECTION('center_axis',(1.,0.,0.));
#32545=DIRECTION('ref_axis',(0.,1.,0.));
#32546=DIRECTION('',(-1.,0.,0.));
#32547=DIRECTION('center_axis',(-1.,0.,0.));
#32548=DIRECTION('ref_axis',(0.,1.,0.));
#32549=DIRECTION('center_axis',(1.,0.,0.));
#32550=DIRECTION('ref_axis',(0.,0.203428885041595,-0.97908972455579));
#32551=DIRECTION('',(1.,0.,0.));
#32552=DIRECTION('center_axis',(1.,0.,0.));
#32553=DIRECTION('ref_axis',(0.,1.,1.07759279891775E-13));
#32554=DIRECTION('center_axis',(1.,0.,0.));
#32555=DIRECTION('ref_axis',(0.,1.,1.07759279891775E-13));
#32556=DIRECTION('',(1.,0.,0.));
#32557=DIRECTION('center_axis',(1.,0.,0.));
#32558=DIRECTION('ref_axis',(0.,1.,1.07759279891775E-13));
#32559=DIRECTION('',(1.,0.,0.));
#32560=DIRECTION('center_axis',(1.,0.,0.));
#32561=DIRECTION('ref_axis',(0.,1.,1.07759279891775E-13));
#32562=DIRECTION('',(1.,0.,0.));
#32563=DIRECTION('center_axis',(1.,0.,0.));
#32564=DIRECTION('ref_axis',(0.,1.,1.07759279891775E-13));
#32565=DIRECTION('',(1.,0.,0.));
#32566=DIRECTION('center_axis',(1.,0.,0.));
#32567=DIRECTION('ref_axis',(0.,1.,1.07759279891775E-13));
#32568=DIRECTION('',(1.,0.,0.));
#32569=DIRECTION('center_axis',(1.,0.,0.));
#32570=DIRECTION('ref_axis',(0.,1.,1.07759279891775E-13));
#32571=DIRECTION('',(1.,0.,0.));
#32572=DIRECTION('center_axis',(1.,0.,0.));
#32573=DIRECTION('ref_axis',(0.,1.,1.07759279891775E-13));
#32574=DIRECTION('',(1.,0.,0.));
#32575=DIRECTION('center_axis',(1.,0.,0.));
#32576=DIRECTION('ref_axis',(0.,1.,1.07759279891775E-13));
#32577=DIRECTION('',(1.,0.,0.));
#32578=DIRECTION('center_axis',(1.,0.,0.));
#32579=DIRECTION('ref_axis',(0.,1.,1.07759279891775E-13));
#32580=DIRECTION('',(1.,0.,0.));
#32581=DIRECTION('center_axis',(1.,0.,0.));
#32582=DIRECTION('ref_axis',(0.,1.,1.07759279891775E-13));
#32583=DIRECTION('',(1.,0.,0.));
#32584=DIRECTION('center_axis',(1.,0.,0.));
#32585=DIRECTION('ref_axis',(0.,1.,1.07759279891775E-13));
#32586=DIRECTION('',(1.,0.,0.));
#32587=DIRECTION('center_axis',(1.,0.,0.));
#32588=DIRECTION('ref_axis',(0.,1.,1.07759279891775E-13));
#32589=DIRECTION('',(1.,0.,0.));
#32590=DIRECTION('center_axis',(1.,0.,0.));
#32591=DIRECTION('ref_axis',(0.,1.,1.07759279891775E-13));
#32592=DIRECTION('',(1.,0.,0.));
#32593=DIRECTION('center_axis',(1.,0.,0.));
#32594=DIRECTION('ref_axis',(0.,1.,1.07759279891775E-13));
#32595=DIRECTION('',(1.,0.,0.));
#32596=DIRECTION('center_axis',(1.,0.,0.));
#32597=DIRECTION('ref_axis',(0.,1.,1.07759279891775E-13));
#32598=DIRECTION('',(1.,0.,0.));
#32599=DIRECTION('center_axis',(1.,0.,0.));
#32600=DIRECTION('ref_axis',(0.,1.,1.07759279891775E-13));
#32601=DIRECTION('',(1.,0.,0.));
#32602=DIRECTION('center_axis',(1.,0.,0.));
#32603=DIRECTION('ref_axis',(0.,1.,1.07759279891775E-13));
#32604=DIRECTION('',(1.,0.,0.));
#32605=DIRECTION('center_axis',(1.,0.,0.));
#32606=DIRECTION('ref_axis',(0.,1.,1.07759279891775E-13));
#32607=DIRECTION('',(1.,0.,0.));
#32608=DIRECTION('center_axis',(1.,0.,0.));
#32609=DIRECTION('ref_axis',(0.,1.,1.07759279891775E-13));
#32610=DIRECTION('',(1.,0.,0.));
#32611=DIRECTION('center_axis',(1.,0.,0.));
#32612=DIRECTION('ref_axis',(0.,0.,-1.));
#32613=DIRECTION('center_axis',(-1.,0.,0.));
#32614=DIRECTION('ref_axis',(0.,1.,0.));
#32615=DIRECTION('center_axis',(1.,0.,0.));
#32616=DIRECTION('ref_axis',(0.,0.,-1.));
#32617=DIRECTION('center_axis',(1.,0.,0.));
#32618=DIRECTION('ref_axis',(0.,1.,0.));
#32619=DIRECTION('center_axis',(1.,0.,0.));
#32620=DIRECTION('ref_axis',(0.,1.,0.));
#32621=DIRECTION('center_axis',(-1.,0.,0.));
#32622=DIRECTION('ref_axis',(0.,1.,1.07759279891775E-13));
#32623=DIRECTION('center_axis',(1.,0.,0.));
#32624=DIRECTION('ref_axis',(0.,0.88891871603891,0.458064969492032));
#32625=DIRECTION('center_axis',(0.,-0.451966109673778,0.892035109009926));
#32626=DIRECTION('ref_axis',(0.,-0.892035109009926,-0.451966109673778));
#32627=DIRECTION('',(-1.,0.,0.));
#32628=DIRECTION('',(0.,-0.892035109009926,-0.451966109673778));
#32629=DIRECTION('',(1.,0.,0.));
#32630=DIRECTION('',(0.,-0.892035109009926,-0.451966109673778));
#32631=DIRECTION('center_axis',(1.,0.,0.));
#32632=DIRECTION('ref_axis',(0.,-0.17364817766693,-0.984807753012208));
#32633=DIRECTION('center_axis',(-1.,0.,0.));
#32634=DIRECTION('ref_axis',(0.,1.,0.));
#32635=DIRECTION('',(0.,0.68365729580961,-0.729803193940867));
#32636=DIRECTION('center_axis',(0.,-0.729803193940867,-0.683657295809611));
#32637=DIRECTION('ref_axis',(0.,0.68365729580961,-0.729803193940867));
#32638=DIRECTION('',(1.,0.,0.));
#32639=DIRECTION('',(0.,0.68365729580961,-0.729803193940867));
#32640=DIRECTION('center_axis',(1.,0.,0.));
#32641=DIRECTION('ref_axis',(0.,-0.17364817766693,-0.984807753012208));
#32642=DIRECTION('center_axis',(1.,0.,0.));
#32643=DIRECTION('ref_axis',(0.,1.,0.));
#32644=DIRECTION('center_axis',(0.,-0.290199457811006,0.956966182624129));
#32645=DIRECTION('ref_axis',(0.,-0.956966182624129,-0.290199457811006));
#32646=DIRECTION('',(-1.,0.,0.));
#32647=DIRECTION('',(0.,-0.956966182624129,-0.290199457811006));
#32648=DIRECTION('',(1.,0.,0.));
#32649=DIRECTION('',(0.,-0.956966182624129,-0.290199457811006));
#32650=DIRECTION('center_axis',(1.,0.,0.));
#32651=DIRECTION('ref_axis',(0.,-0.342020143325669,-0.939692620785908));
#32652=DIRECTION('center_axis',(-1.,0.,0.));
#32653=DIRECTION('ref_axis',(0.,1.,0.));
#32654=DIRECTION('',(0.,0.546542010633327,-0.837431687132079));
#32655=DIRECTION('center_axis',(0.,-0.837431687132079,-0.546542010633327));
#32656=DIRECTION('ref_axis',(0.,0.546542010633327,-0.837431687132079));
#32657=DIRECTION('',(1.,0.,0.));
#32658=DIRECTION('',(0.,0.546542010633327,-0.837431687132079));
#32659=DIRECTION('center_axis',(1.,0.,0.));
#32660=DIRECTION('ref_axis',(0.,-0.342020143325669,-0.939692620785908));
#32661=DIRECTION('center_axis',(1.,0.,0.));
#32662=DIRECTION('ref_axis',(0.,1.,0.));
#32663=DIRECTION('center_axis',(0.,-0.11961524227066,0.992820323027551));
#32664=DIRECTION('ref_axis',(0.,-0.992820323027551,-0.11961524227066));
#32665=DIRECTION('',(-1.,0.,0.));
#32666=DIRECTION('',(0.,-0.992820323027551,-0.11961524227066));
#32667=DIRECTION('',(1.,0.,0.));
#32668=DIRECTION('',(0.,-0.992820323027551,-0.11961524227066));
#32669=DIRECTION('center_axis',(1.,0.,0.));
#32670=DIRECTION('ref_axis',(0.,-0.5,-0.866025403784438));
#32671=DIRECTION('center_axis',(-1.,0.,0.));
#32672=DIRECTION('ref_axis',(0.,1.,0.));
#32673=DIRECTION('',(0.,0.392820323027553,-0.919615242270662));
#32674=DIRECTION('center_axis',(0.,-0.919615242270662,-0.392820323027553));
#32675=DIRECTION('ref_axis',(0.,0.392820323027553,-0.919615242270662));
#32676=DIRECTION('',(1.,0.,0.));
#32677=DIRECTION('',(0.,0.392820323027553,-0.919615242270662));
#32678=DIRECTION('center_axis',(1.,0.,0.));
#32679=DIRECTION('ref_axis',(0.,-0.5,-0.866025403784438));
#32680=DIRECTION('center_axis',(1.,0.,0.));
#32681=DIRECTION('ref_axis',(0.,1.,0.));
#32682=DIRECTION('center_axis',(0.,0.0546034218778482,0.998508120307106));
#32683=DIRECTION('ref_axis',(0.,-0.998508120307106,0.0546034218778482));
#32684=DIRECTION('',(-1.,0.,0.));
#32685=DIRECTION('',(0.,-0.998508120307106,0.0546034218778482));
#32686=DIRECTION('',(1.,0.,0.));
#32687=DIRECTION('',(0.,-0.998508120307106,0.0546034218778482));
#32688=DIRECTION('center_axis',(1.,0.,0.));
#32689=DIRECTION('ref_axis',(0.,-0.64278760968654,-0.766044443118978));
#32690=DIRECTION('center_axis',(-1.,0.,0.));
#32691=DIRECTION('ref_axis',(0.,1.,0.));
#32692=DIRECTION('',(0.,0.227162988683261,-0.973856753620618));
#32693=DIRECTION('center_axis',(0.,-0.973856753620618,-0.227162988683262));
#32694=DIRECTION('ref_axis',(0.,0.227162988683261,-0.973856753620618));
#32695=DIRECTION('',(1.,0.,0.));
#32696=DIRECTION('',(0.,0.227162988683261,-0.973856753620618));
#32697=DIRECTION('center_axis',(1.,0.,0.));
#32698=DIRECTION('ref_axis',(0.,-0.64278760968654,-0.766044443118978));
#32699=DIRECTION('center_axis',(1.,0.,0.));
#32700=DIRECTION('ref_axis',(0.,1.,0.));
#32701=DIRECTION('center_axis',(0.,0.227162988683262,0.973856753620618));
#32702=DIRECTION('ref_axis',(0.,-0.973856753620618,0.227162988683262));
#32703=DIRECTION('',(-1.,0.,0.));
#32704=DIRECTION('',(0.,-0.973856753620618,0.227162988683262));
#32705=DIRECTION('',(1.,0.,0.));
#32706=DIRECTION('',(0.,-0.973856753620618,0.227162988683262));
#32707=DIRECTION('center_axis',(1.,0.,0.));
#32708=DIRECTION('ref_axis',(0.,-0.766044443118978,-0.642787609686539));
#32709=DIRECTION('center_axis',(-1.,0.,0.));
#32710=DIRECTION('ref_axis',(0.,1.,0.));
#32711=DIRECTION('',(0.,0.0546034218778476,-0.998508120307106));
#32712=DIRECTION('center_axis',(0.,-0.998508120307106,-0.0546034218778476));
#32713=DIRECTION('ref_axis',(0.,0.0546034218778476,-0.998508120307106));
#32714=DIRECTION('',(1.,0.,0.));
#32715=DIRECTION('',(0.,0.0546034218778476,-0.998508120307106));
#32716=DIRECTION('center_axis',(1.,0.,0.));
#32717=DIRECTION('ref_axis',(0.,-0.766044443118978,-0.642787609686539));
#32718=DIRECTION('center_axis',(1.,0.,0.));
#32719=DIRECTION('ref_axis',(0.,1.,0.));
#32720=DIRECTION('center_axis',(0.,0.392820323027554,0.919615242270662));
#32721=DIRECTION('ref_axis',(0.,-0.919615242270662,0.392820323027554));
#32722=DIRECTION('',(-1.,0.,0.));
#32723=DIRECTION('',(0.,-0.919615242270662,0.392820323027554));
#32724=DIRECTION('',(1.,0.,0.));
#32725=DIRECTION('',(0.,-0.919615242270662,0.392820323027554));
#32726=DIRECTION('center_axis',(1.,0.,0.));
#32727=DIRECTION('ref_axis',(0.,-0.866025403784439,-0.5));
#32728=DIRECTION('center_axis',(-1.,0.,0.));
#32729=DIRECTION('ref_axis',(0.,1.,0.));
#32730=DIRECTION('',(0.,-0.11961524227066,-0.992820323027551));
#32731=DIRECTION('center_axis',(0.,-0.992820323027551,0.11961524227066));
#32732=DIRECTION('ref_axis',(0.,-0.11961524227066,-0.992820323027551));
#32733=DIRECTION('',(1.,0.,0.));
#32734=DIRECTION('',(0.,-0.11961524227066,-0.992820323027551));
#32735=DIRECTION('center_axis',(1.,0.,0.));
#32736=DIRECTION('ref_axis',(0.,-0.866025403784439,-0.5));
#32737=DIRECTION('center_axis',(1.,0.,0.));
#32738=DIRECTION('ref_axis',(0.,1.,0.));
#32739=DIRECTION('center_axis',(0.,0.546542010633329,0.837431687132078));
#32740=DIRECTION('ref_axis',(0.,-0.837431687132078,0.546542010633329));
#32741=DIRECTION('',(-1.,0.,0.));
#32742=DIRECTION('',(0.,-0.837431687132078,0.546542010633329));
#32743=DIRECTION('',(1.,0.,0.));
#32744=DIRECTION('',(0.,-0.837431687132078,0.546542010633329));
#32745=DIRECTION('center_axis',(1.,0.,0.));
#32746=DIRECTION('ref_axis',(0.,-0.939692620785909,-0.342020143325668));
#32747=DIRECTION('center_axis',(-1.,0.,0.));
#32748=DIRECTION('ref_axis',(0.,1.,0.));
#32749=DIRECTION('',(0.,-0.290199457811008,-0.956966182624129));
#32750=DIRECTION('center_axis',(0.,-0.956966182624129,0.290199457811008));
#32751=DIRECTION('ref_axis',(0.,-0.290199457811008,-0.956966182624129));
#32752=DIRECTION('',(1.,0.,0.));
#32753=DIRECTION('',(0.,-0.290199457811008,-0.956966182624129));
#32754=DIRECTION('center_axis',(1.,0.,0.));
#32755=DIRECTION('ref_axis',(0.,-0.939692620785909,-0.342020143325668));
#32756=DIRECTION('center_axis',(1.,0.,0.));
#32757=DIRECTION('ref_axis',(0.,1.,0.));
#32758=DIRECTION('center_axis',(0.,0.683657295809611,0.729803193940867));
#32759=DIRECTION('ref_axis',(0.,-0.729803193940867,0.683657295809611));
#32760=DIRECTION('',(-1.,0.,0.));
#32761=DIRECTION('',(0.,-0.729803193940867,0.683657295809611));
#32762=DIRECTION('',(1.,0.,0.));
#32763=DIRECTION('',(0.,-0.729803193940867,0.683657295809611));
#32764=DIRECTION('center_axis',(1.,0.,0.));
#32765=DIRECTION('ref_axis',(0.,-0.984807753012208,-0.17364817766693));
#32766=DIRECTION('center_axis',(-1.,0.,0.));
#32767=DIRECTION('ref_axis',(0.,1.,0.));
#32768=DIRECTION('',(0.,-0.451966109673778,-0.892035109009926));
#32769=DIRECTION('center_axis',(0.,-0.892035109009926,0.451966109673778));
#32770=DIRECTION('ref_axis',(0.,-0.451966109673778,-0.892035109009926));
#32771=DIRECTION('',(1.,0.,0.));
#32772=DIRECTION('',(0.,-0.451966109673778,-0.892035109009926));
#32773=DIRECTION('center_axis',(1.,0.,0.));
#32774=DIRECTION('ref_axis',(0.,-0.984807753012208,-0.17364817766693));
#32775=DIRECTION('center_axis',(1.,0.,0.));
#32776=DIRECTION('ref_axis',(0.,1.,0.));
#32777=DIRECTION('center_axis',(0.,0.800000000000002,0.599999999999997));
#32778=DIRECTION('ref_axis',(0.,-0.599999999999997,0.800000000000002));
#32779=DIRECTION('',(-1.,0.,0.));
#32780=DIRECTION('',(0.,-0.599999999999997,0.800000000000002));
#32781=DIRECTION('',(1.,0.,0.));
#32782=DIRECTION('',(0.,-0.599999999999997,0.800000000000002));
#32783=DIRECTION('center_axis',(1.,0.,0.));
#32784=DIRECTION('ref_axis',(0.,-1.,1.83697019872103E-16));
#32785=DIRECTION('center_axis',(-1.,0.,0.));
#32786=DIRECTION('ref_axis',(0.,1.,0.));
#32787=DIRECTION('',(0.,-0.599999999999998,-0.800000000000002));
#32788=DIRECTION('center_axis',(0.,-0.800000000000002,0.599999999999998));
#32789=DIRECTION('ref_axis',(0.,-0.599999999999998,-0.800000000000002));
#32790=DIRECTION('',(1.,0.,0.));
#32791=DIRECTION('',(0.,-0.599999999999998,-0.800000000000002));
#32792=DIRECTION('center_axis',(1.,0.,0.));
#32793=DIRECTION('ref_axis',(0.,-1.,1.83697019872103E-16));
#32794=DIRECTION('center_axis',(1.,0.,0.));
#32795=DIRECTION('ref_axis',(0.,1.,0.));
#32796=DIRECTION('center_axis',(0.,0.892035109009926,0.451966109673778));
#32797=DIRECTION('ref_axis',(0.,-0.451966109673778,0.892035109009926));
#32798=DIRECTION('',(-1.,0.,0.));
#32799=DIRECTION('',(0.,-0.451966109673778,0.892035109009926));
#32800=DIRECTION('',(1.,0.,0.));
#32801=DIRECTION('',(0.,-0.451966109673778,0.892035109009926));
#32802=DIRECTION('center_axis',(1.,0.,0.));
#32803=DIRECTION('ref_axis',(0.,-0.984807753012208,0.17364817766693));
#32804=DIRECTION('center_axis',(-1.,0.,0.));
#32805=DIRECTION('ref_axis',(0.,1.,0.));
#32806=DIRECTION('',(0.,-0.729803193940867,-0.683657295809611));
#32807=DIRECTION('center_axis',(0.,-0.683657295809611,0.729803193940867));
#32808=DIRECTION('ref_axis',(0.,-0.729803193940867,-0.683657295809611));
#32809=DIRECTION('',(1.,0.,0.));
#32810=DIRECTION('',(0.,-0.729803193940867,-0.683657295809611));
#32811=DIRECTION('center_axis',(1.,0.,0.));
#32812=DIRECTION('ref_axis',(0.,-0.984807753012208,0.17364817766693));
#32813=DIRECTION('center_axis',(1.,0.,0.));
#32814=DIRECTION('ref_axis',(0.,1.,0.));
#32815=DIRECTION('center_axis',(0.,0.956966182624129,0.290199457811006));
#32816=DIRECTION('ref_axis',(0.,-0.290199457811006,0.956966182624129));
#32817=DIRECTION('',(-1.,0.,0.));
#32818=DIRECTION('',(0.,-0.290199457811006,0.956966182624129));
#32819=DIRECTION('',(1.,0.,0.));
#32820=DIRECTION('',(0.,-0.290199457811006,0.956966182624129));
#32821=DIRECTION('center_axis',(1.,0.,0.));
#32822=DIRECTION('ref_axis',(0.,-0.939692620785908,0.342020143325669));
#32823=DIRECTION('center_axis',(-1.,0.,0.));
#32824=DIRECTION('ref_axis',(0.,1.,0.));
#32825=DIRECTION('',(0.,-0.837431687132079,-0.546542010633328));
#32826=DIRECTION('center_axis',(0.,-0.546542010633328,0.837431687132079));
#32827=DIRECTION('ref_axis',(0.,-0.837431687132079,-0.546542010633328));
#32828=DIRECTION('',(1.,0.,0.));
#32829=DIRECTION('',(0.,-0.837431687132079,-0.546542010633328));
#32830=DIRECTION('center_axis',(1.,0.,0.));
#32831=DIRECTION('ref_axis',(0.,-0.939692620785908,0.342020143325669));
#32832=DIRECTION('center_axis',(1.,0.,0.));
#32833=DIRECTION('ref_axis',(0.,1.,0.));
#32834=DIRECTION('center_axis',(0.,0.992820323027551,0.11961524227066));
#32835=DIRECTION('ref_axis',(0.,-0.11961524227066,0.992820323027551));
#32836=DIRECTION('',(-1.,0.,0.));
#32837=DIRECTION('',(0.,-0.11961524227066,0.992820323027551));
#32838=DIRECTION('',(1.,0.,0.));
#32839=DIRECTION('',(0.,-0.11961524227066,0.992820323027551));
#32840=DIRECTION('center_axis',(1.,0.,0.));
#32841=DIRECTION('ref_axis',(0.,-0.866025403784438,0.5));
#32842=DIRECTION('center_axis',(-1.,0.,0.));
#32843=DIRECTION('ref_axis',(0.,1.,0.));
#32844=DIRECTION('',(0.,-0.919615242270662,-0.392820323027553));
#32845=DIRECTION('center_axis',(0.,-0.392820323027553,0.919615242270662));
#32846=DIRECTION('ref_axis',(0.,-0.919615242270662,-0.392820323027553));
#32847=DIRECTION('',(1.,0.,0.));
#32848=DIRECTION('',(0.,-0.919615242270662,-0.392820323027553));
#32849=DIRECTION('center_axis',(1.,0.,0.));
#32850=DIRECTION('ref_axis',(0.,-0.866025403784438,0.5));
#32851=DIRECTION('center_axis',(1.,0.,0.));
#32852=DIRECTION('ref_axis',(0.,1.,0.));
#32853=DIRECTION('center_axis',(0.,0.998508120307106,-0.054603421877848));
#32854=DIRECTION('ref_axis',(0.,0.054603421877848,0.998508120307106));
#32855=DIRECTION('',(-1.,0.,0.));
#32856=DIRECTION('',(0.,0.054603421877848,0.998508120307106));
#32857=DIRECTION('',(1.,0.,0.));
#32858=DIRECTION('',(0.,0.054603421877848,0.998508120307106));
#32859=DIRECTION('center_axis',(1.,0.,0.));
#32860=DIRECTION('ref_axis',(0.,-0.766044443118978,0.642787609686539));
#32861=DIRECTION('center_axis',(-1.,0.,0.));
#32862=DIRECTION('ref_axis',(0.,1.,0.));
#32863=DIRECTION('',(0.,-0.973856753620618,-0.227162988683262));
#32864=DIRECTION('center_axis',(0.,-0.227162988683262,0.973856753620618));
#32865=DIRECTION('ref_axis',(0.,-0.973856753620618,-0.227162988683262));
#32866=DIRECTION('',(1.,0.,0.));
#32867=DIRECTION('',(0.,-0.973856753620618,-0.227162988683262));
#32868=DIRECTION('center_axis',(1.,0.,0.));
#32869=DIRECTION('ref_axis',(0.,-0.766044443118978,0.642787609686539));
#32870=DIRECTION('center_axis',(1.,0.,0.));
#32871=DIRECTION('ref_axis',(0.,1.,0.));
#32872=DIRECTION('center_axis',(0.,0.973856753620618,-0.227162988683262));
#32873=DIRECTION('ref_axis',(0.,0.227162988683262,0.973856753620618));
#32874=DIRECTION('',(-1.,0.,0.));
#32875=DIRECTION('',(0.,0.227162988683262,0.973856753620618));
#32876=DIRECTION('',(1.,0.,0.));
#32877=DIRECTION('',(0.,0.227162988683262,0.973856753620618));
#32878=DIRECTION('center_axis',(1.,0.,0.));
#32879=DIRECTION('ref_axis',(0.,-0.642787609686539,0.766044443118978));
#32880=DIRECTION('center_axis',(-1.,0.,0.));
#32881=DIRECTION('ref_axis',(0.,1.,0.));
#32882=DIRECTION('',(0.,-0.998508120307106,-0.0546034218778477));
#32883=DIRECTION('center_axis',(0.,-0.0546034218778477,0.998508120307106));
#32884=DIRECTION('ref_axis',(0.,-0.998508120307106,-0.0546034218778477));
#32885=DIRECTION('',(1.,0.,0.));
#32886=DIRECTION('',(0.,-0.998508120307106,-0.0546034218778477));
#32887=DIRECTION('center_axis',(1.,0.,0.));
#32888=DIRECTION('ref_axis',(0.,-0.642787609686539,0.766044443118978));
#32889=DIRECTION('center_axis',(1.,0.,0.));
#32890=DIRECTION('ref_axis',(0.,1.,0.));
#32891=DIRECTION('center_axis',(0.,0.919615242270662,-0.392820323027554));
#32892=DIRECTION('ref_axis',(0.,0.392820323027554,0.919615242270662));
#32893=DIRECTION('',(-1.,0.,0.));
#32894=DIRECTION('',(0.,0.392820323027554,0.919615242270662));
#32895=DIRECTION('',(1.,0.,0.));
#32896=DIRECTION('',(0.,0.392820323027554,0.919615242270662));
#32897=DIRECTION('center_axis',(1.,0.,0.));
#32898=DIRECTION('ref_axis',(0.,-0.5,0.866025403784439));
#32899=DIRECTION('center_axis',(-1.,0.,0.));
#32900=DIRECTION('ref_axis',(0.,1.,0.));
#32901=DIRECTION('',(0.,-0.992820323027551,0.11961524227066));
#32902=DIRECTION('center_axis',(0.,0.11961524227066,0.992820323027551));
#32903=DIRECTION('ref_axis',(0.,-0.992820323027551,0.11961524227066));
#32904=DIRECTION('',(1.,0.,0.));
#32905=DIRECTION('',(0.,-0.992820323027551,0.11961524227066));
#32906=DIRECTION('center_axis',(1.,0.,0.));
#32907=DIRECTION('ref_axis',(0.,-0.5,0.866025403784439));
#32908=DIRECTION('center_axis',(1.,0.,0.));
#32909=DIRECTION('ref_axis',(0.,1.,0.));
#32910=DIRECTION('center_axis',(0.,0.837431687132078,-0.546542010633328));
#32911=DIRECTION('ref_axis',(0.,0.546542010633328,0.837431687132078));
#32912=DIRECTION('',(-1.,0.,0.));
#32913=DIRECTION('',(0.,0.546542010633328,0.837431687132078));
#32914=DIRECTION('',(1.,0.,0.));
#32915=DIRECTION('',(0.,0.546542010633328,0.837431687132078));
#32916=DIRECTION('center_axis',(1.,0.,0.));
#32917=DIRECTION('ref_axis',(0.,-0.342020143325669,0.939692620785909));
#32918=DIRECTION('center_axis',(-1.,0.,0.));
#32919=DIRECTION('ref_axis',(0.,1.,0.));
#32920=DIRECTION('',(0.,-0.956966182624129,0.290199457811007));
#32921=DIRECTION('center_axis',(0.,0.290199457811007,0.956966182624129));
#32922=DIRECTION('ref_axis',(0.,-0.956966182624129,0.290199457811007));
#32923=DIRECTION('',(1.,0.,0.));
#32924=DIRECTION('',(0.,-0.956966182624129,0.290199457811007));
#32925=DIRECTION('center_axis',(1.,0.,0.));
#32926=DIRECTION('ref_axis',(0.,-0.342020143325669,0.939692620785909));
#32927=DIRECTION('center_axis',(1.,0.,0.));
#32928=DIRECTION('ref_axis',(0.,1.,0.));
#32929=DIRECTION('center_axis',(0.,0.729803193940867,-0.683657295809611));
#32930=DIRECTION('ref_axis',(0.,0.683657295809611,0.729803193940867));
#32931=DIRECTION('',(-1.,0.,0.));
#32932=DIRECTION('',(0.,0.683657295809611,0.729803193940867));
#32933=DIRECTION('',(1.,0.,0.));
#32934=DIRECTION('',(0.,0.683657295809611,0.729803193940867));
#32935=DIRECTION('center_axis',(1.,0.,0.));
#32936=DIRECTION('ref_axis',(0.,-0.17364817766693,0.984807753012208));
#32937=DIRECTION('center_axis',(-1.,0.,0.));
#32938=DIRECTION('ref_axis',(0.,1.,0.));
#32939=DIRECTION('',(0.,-0.892035109009926,0.451966109673778));
#32940=DIRECTION('center_axis',(0.,0.451966109673778,0.892035109009926));
#32941=DIRECTION('ref_axis',(0.,-0.892035109009926,0.451966109673778));
#32942=DIRECTION('',(1.,0.,0.));
#32943=DIRECTION('',(0.,-0.892035109009926,0.451966109673778));
#32944=DIRECTION('center_axis',(1.,0.,0.));
#32945=DIRECTION('ref_axis',(0.,-0.17364817766693,0.984807753012208));
#32946=DIRECTION('center_axis',(1.,0.,0.));
#32947=DIRECTION('ref_axis',(0.,1.,0.));
#32948=DIRECTION('center_axis',(0.,0.599999999999997,-0.800000000000002));
#32949=DIRECTION('ref_axis',(0.,0.800000000000002,0.599999999999997));
#32950=DIRECTION('',(-1.,0.,0.));
#32951=DIRECTION('',(0.,0.800000000000002,0.599999999999997));
#32952=DIRECTION('',(1.,0.,0.));
#32953=DIRECTION('',(0.,0.800000000000002,0.599999999999997));
#32954=DIRECTION('center_axis',(1.,0.,0.));
#32955=DIRECTION('ref_axis',(0.,1.22464679914735E-16,1.));
#32956=DIRECTION('center_axis',(-1.,0.,0.));
#32957=DIRECTION('ref_axis',(0.,1.,0.));
#32958=DIRECTION('',(0.,-0.800000000000002,0.599999999999998));
#32959=DIRECTION('center_axis',(-1.,0.,0.));
#32960=DIRECTION('ref_axis',(0.,1.,0.));
#32961=DIRECTION('center_axis',(0.,0.599999999999998,0.800000000000002));
#32962=DIRECTION('ref_axis',(0.,-0.800000000000002,0.599999999999998));
#32963=DIRECTION('',(1.,0.,0.));
#32964=DIRECTION('',(0.,-0.800000000000002,0.599999999999998));
#32965=DIRECTION('center_axis',(1.,0.,0.));
#32966=DIRECTION('ref_axis',(0.,1.22464679914735E-16,1.));
#32967=DIRECTION('center_axis',(1.,0.,0.));
#32968=DIRECTION('ref_axis',(0.,1.,0.));
#32969=DIRECTION('center_axis',(1.,0.,0.));
#32970=DIRECTION('ref_axis',(0.,1.,0.));
#32971=DIRECTION('center_axis',(0.,0.451966109673778,-0.892035109009926));
#32972=DIRECTION('ref_axis',(0.,0.892035109009926,0.451966109673777));
#32973=DIRECTION('',(-1.,0.,0.));
#32974=DIRECTION('',(0.,0.892035109009926,0.451966109673777));
#32975=DIRECTION('',(1.,0.,0.));
#32976=DIRECTION('',(0.,0.892035109009926,0.451966109673777));
#32977=DIRECTION('center_axis',(1.,0.,0.));
#32978=DIRECTION('ref_axis',(0.,0.173648177666931,0.984807753012208));
#32979=DIRECTION('center_axis',(-1.,0.,0.));
#32980=DIRECTION('ref_axis',(0.,1.,0.));
#32981=DIRECTION('',(0.,-0.68365729580961,0.729803193940867));
#32982=DIRECTION('center_axis',(0.,0.729803193940867,0.68365729580961));
#32983=DIRECTION('ref_axis',(0.,-0.68365729580961,0.729803193940867));
#32984=DIRECTION('',(1.,0.,0.));
#32985=DIRECTION('',(0.,-0.68365729580961,0.729803193940867));
#32986=DIRECTION('center_axis',(1.,0.,0.));
#32987=DIRECTION('ref_axis',(0.,0.173648177666931,0.984807753012208));
#32988=DIRECTION('center_axis',(1.,0.,0.));
#32989=DIRECTION('ref_axis',(0.,1.,0.));
#32990=DIRECTION('center_axis',(0.,0.290199457811007,-0.956966182624129));
#32991=DIRECTION('ref_axis',(0.,0.956966182624129,0.290199457811007));
#32992=DIRECTION('',(-1.,0.,0.));
#32993=DIRECTION('',(0.,0.956966182624129,0.290199457811007));
#32994=DIRECTION('',(1.,0.,0.));
#32995=DIRECTION('',(0.,0.956966182624129,0.290199457811007));
#32996=DIRECTION('center_axis',(1.,0.,0.));
#32997=DIRECTION('ref_axis',(0.,0.342020143325669,0.939692620785908));
#32998=DIRECTION('center_axis',(-1.,0.,0.));
#32999=DIRECTION('ref_axis',(0.,1.,0.));
#33000=DIRECTION('',(0.,-0.546542010633328,0.837431687132078));
#33001=DIRECTION('center_axis',(0.,0.837431687132078,0.546542010633328));
#33002=DIRECTION('ref_axis',(0.,-0.546542010633328,0.837431687132078));
#33003=DIRECTION('',(1.,0.,0.));
#33004=DIRECTION('',(0.,-0.546542010633328,0.837431687132078));
#33005=DIRECTION('center_axis',(1.,0.,0.));
#33006=DIRECTION('ref_axis',(0.,0.342020143325669,0.939692620785908));
#33007=DIRECTION('center_axis',(1.,0.,0.));
#33008=DIRECTION('ref_axis',(0.,1.,0.));
#33009=DIRECTION('center_axis',(0.,0.11961524227066,-0.992820323027551));
#33010=DIRECTION('ref_axis',(0.,0.992820323027551,0.11961524227066));
#33011=DIRECTION('',(-1.,0.,0.));
#33012=DIRECTION('',(0.,0.992820323027551,0.11961524227066));
#33013=DIRECTION('',(1.,0.,0.));
#33014=DIRECTION('',(0.,0.992820323027551,0.11961524227066));
#33015=DIRECTION('center_axis',(1.,0.,0.));
#33016=DIRECTION('ref_axis',(0.,0.5,0.866025403784439));
#33017=DIRECTION('center_axis',(-1.,0.,0.));
#33018=DIRECTION('ref_axis',(0.,1.,0.));
#33019=DIRECTION('',(0.,-0.392820323027554,0.919615242270662));
#33020=DIRECTION('center_axis',(0.,0.919615242270662,0.392820323027554));
#33021=DIRECTION('ref_axis',(0.,-0.392820323027554,0.919615242270662));
#33022=DIRECTION('',(1.,0.,0.));
#33023=DIRECTION('',(0.,-0.392820323027554,0.919615242270662));
#33024=DIRECTION('center_axis',(1.,0.,0.));
#33025=DIRECTION('ref_axis',(0.,0.5,0.866025403784439));
#33026=DIRECTION('center_axis',(1.,0.,0.));
#33027=DIRECTION('ref_axis',(0.,1.,0.));
#33028=DIRECTION('center_axis',(0.,-0.054603421877848,-0.998508120307106));
#33029=DIRECTION('ref_axis',(0.,0.998508120307106,-0.054603421877848));
#33030=DIRECTION('',(-1.,0.,0.));
#33031=DIRECTION('',(0.,0.998508120307106,-0.054603421877848));
#33032=DIRECTION('',(1.,0.,0.));
#33033=DIRECTION('',(0.,0.998508120307106,-0.054603421877848));
#33034=DIRECTION('center_axis',(1.,0.,0.));
#33035=DIRECTION('ref_axis',(0.,0.642787609686539,0.766044443118978));
#33036=DIRECTION('center_axis',(-1.,0.,0.));
#33037=DIRECTION('ref_axis',(0.,1.,0.));
#33038=DIRECTION('',(0.,-0.227162988683262,0.973856753620618));
#33039=DIRECTION('center_axis',(0.,0.973856753620618,0.227162988683262));
#33040=DIRECTION('ref_axis',(0.,-0.227162988683262,0.973856753620618));
#33041=DIRECTION('',(1.,0.,0.));
#33042=DIRECTION('',(0.,-0.227162988683262,0.973856753620618));
#33043=DIRECTION('center_axis',(1.,0.,0.));
#33044=DIRECTION('ref_axis',(0.,0.642787609686539,0.766044443118978));
#33045=DIRECTION('center_axis',(1.,0.,0.));
#33046=DIRECTION('ref_axis',(0.,1.,0.));
#33047=DIRECTION('center_axis',(0.,-0.227162988683262,-0.973856753620618));
#33048=DIRECTION('ref_axis',(0.,0.973856753620618,-0.227162988683262));
#33049=DIRECTION('',(-1.,0.,0.));
#33050=DIRECTION('',(0.,0.973856753620618,-0.227162988683262));
#33051=DIRECTION('',(1.,0.,0.));
#33052=DIRECTION('',(0.,0.973856753620618,-0.227162988683262));
#33053=DIRECTION('center_axis',(1.,0.,0.));
#33054=DIRECTION('ref_axis',(0.,0.766044443118978,0.642787609686539));
#33055=DIRECTION('center_axis',(-1.,0.,0.));
#33056=DIRECTION('ref_axis',(0.,1.,0.));
#33057=DIRECTION('',(0.,-0.0546034218778478,0.998508120307106));
#33058=DIRECTION('center_axis',(0.,0.998508120307106,0.0546034218778478));
#33059=DIRECTION('ref_axis',(0.,-0.0546034218778478,0.998508120307106));
#33060=DIRECTION('',(1.,0.,0.));
#33061=DIRECTION('',(0.,-0.0546034218778478,0.998508120307106));
#33062=DIRECTION('center_axis',(1.,0.,0.));
#33063=DIRECTION('ref_axis',(0.,0.766044443118978,0.642787609686539));
#33064=DIRECTION('center_axis',(1.,0.,0.));
#33065=DIRECTION('ref_axis',(0.,1.,0.));
#33066=DIRECTION('center_axis',(0.,-0.392820323027554,-0.919615242270662));
#33067=DIRECTION('ref_axis',(0.,0.919615242270662,-0.392820323027554));
#33068=DIRECTION('',(-1.,0.,0.));
#33069=DIRECTION('',(0.,0.919615242270662,-0.392820323027554));
#33070=DIRECTION('',(1.,0.,0.));
#33071=DIRECTION('',(0.,0.919615242270662,-0.392820323027554));
#33072=DIRECTION('center_axis',(1.,0.,0.));
#33073=DIRECTION('ref_axis',(0.,0.866025403784439,0.5));
#33074=DIRECTION('center_axis',(-1.,0.,0.));
#33075=DIRECTION('ref_axis',(0.,1.,0.));
#33076=DIRECTION('',(0.,0.11961524227066,0.992820323027551));
#33077=DIRECTION('center_axis',(0.,0.992820323027551,-0.11961524227066));
#33078=DIRECTION('ref_axis',(0.,0.11961524227066,0.992820323027551));
#33079=DIRECTION('',(1.,0.,0.));
#33080=DIRECTION('',(0.,0.11961524227066,0.992820323027551));
#33081=DIRECTION('center_axis',(1.,0.,0.));
#33082=DIRECTION('ref_axis',(0.,0.866025403784439,0.5));
#33083=DIRECTION('center_axis',(1.,0.,0.));
#33084=DIRECTION('ref_axis',(0.,1.,0.));
#33085=DIRECTION('center_axis',(0.,-0.546542010633328,-0.837431687132078));
#33086=DIRECTION('ref_axis',(0.,0.837431687132078,-0.546542010633328));
#33087=DIRECTION('',(-1.,0.,0.));
#33088=DIRECTION('',(0.,0.837431687132078,-0.546542010633328));
#33089=DIRECTION('',(1.,0.,0.));
#33090=DIRECTION('',(0.,0.837431687132078,-0.546542010633328));
#33091=DIRECTION('center_axis',(1.,0.,0.));
#33092=DIRECTION('ref_axis',(0.,0.939692620785908,0.342020143325669));
#33093=DIRECTION('center_axis',(-1.,0.,0.));
#33094=DIRECTION('ref_axis',(0.,1.,0.));
#33095=DIRECTION('',(0.,0.290199457811007,0.956966182624129));
#33096=DIRECTION('center_axis',(0.,0.956966182624129,-0.290199457811007));
#33097=DIRECTION('ref_axis',(0.,0.290199457811007,0.956966182624129));
#33098=DIRECTION('',(1.,0.,0.));
#33099=DIRECTION('',(0.,0.290199457811007,0.956966182624129));
#33100=DIRECTION('center_axis',(1.,0.,0.));
#33101=DIRECTION('ref_axis',(0.,0.939692620785908,0.342020143325669));
#33102=DIRECTION('center_axis',(1.,0.,0.));
#33103=DIRECTION('ref_axis',(0.,1.,0.));
#33104=DIRECTION('center_axis',(0.,-0.683657295809611,-0.729803193940867));
#33105=DIRECTION('ref_axis',(0.,0.729803193940867,-0.683657295809611));
#33106=DIRECTION('',(-1.,0.,0.));
#33107=DIRECTION('',(0.,0.729803193940867,-0.683657295809611));
#33108=DIRECTION('',(1.,0.,0.));
#33109=DIRECTION('',(0.,0.729803193940867,-0.683657295809611));
#33110=DIRECTION('center_axis',(1.,0.,0.));
#33111=DIRECTION('ref_axis',(0.,0.984807753012208,0.17364817766693));
#33112=DIRECTION('center_axis',(-1.,0.,0.));
#33113=DIRECTION('ref_axis',(0.,1.,0.));
#33114=DIRECTION('',(0.,0.451966109673778,0.892035109009926));
#33115=DIRECTION('center_axis',(0.,0.892035109009926,-0.451966109673778));
#33116=DIRECTION('ref_axis',(0.,0.451966109673778,0.892035109009926));
#33117=DIRECTION('',(1.,0.,0.));
#33118=DIRECTION('',(0.,0.451966109673778,0.892035109009926));
#33119=DIRECTION('center_axis',(1.,0.,0.));
#33120=DIRECTION('ref_axis',(0.,0.984807753012208,0.17364817766693));
#33121=DIRECTION('center_axis',(1.,0.,0.));
#33122=DIRECTION('ref_axis',(0.,1.,0.));
#33123=DIRECTION('center_axis',(0.,-0.800000000000002,-0.599999999999998));
#33124=DIRECTION('ref_axis',(0.,0.599999999999998,-0.800000000000002));
#33125=DIRECTION('',(-1.,0.,0.));
#33126=DIRECTION('',(0.,0.599999999999998,-0.800000000000002));
#33127=DIRECTION('',(1.,0.,0.));
#33128=DIRECTION('',(0.,0.599999999999998,-0.800000000000002));
#33129=DIRECTION('center_axis',(1.,0.,0.));
#33130=DIRECTION('ref_axis',(0.,1.,-6.12323399573677E-17));
#33131=DIRECTION('center_axis',(-1.,0.,0.));
#33132=DIRECTION('ref_axis',(0.,1.,0.));
#33133=DIRECTION('',(0.,0.599999999999998,0.800000000000002));
#33134=DIRECTION('center_axis',(0.,0.800000000000002,-0.599999999999998));
#33135=DIRECTION('ref_axis',(0.,0.599999999999998,0.800000000000002));
#33136=DIRECTION('',(1.,0.,0.));
#33137=DIRECTION('',(0.,0.599999999999998,0.800000000000002));
#33138=DIRECTION('center_axis',(1.,0.,0.));
#33139=DIRECTION('ref_axis',(0.,1.,-6.12323399573677E-17));
#33140=DIRECTION('center_axis',(1.,0.,0.));
#33141=DIRECTION('ref_axis',(0.,1.,0.));
#33142=DIRECTION('center_axis',(0.,-0.892035109009926,-0.451966109673778));
#33143=DIRECTION('ref_axis',(0.,0.451966109673778,-0.892035109009926));
#33144=DIRECTION('',(-1.,0.,0.));
#33145=DIRECTION('',(0.,0.451966109673778,-0.892035109009926));
#33146=DIRECTION('',(1.,0.,0.));
#33147=DIRECTION('',(0.,0.451966109673778,-0.892035109009926));
#33148=DIRECTION('center_axis',(1.,0.,0.));
#33149=DIRECTION('ref_axis',(0.,0.984807753012208,-0.17364817766693));
#33150=DIRECTION('center_axis',(-1.,0.,0.));
#33151=DIRECTION('ref_axis',(0.,1.,0.));
#33152=DIRECTION('',(0.,0.729803193940867,0.68365729580961));
#33153=DIRECTION('center_axis',(0.,0.683657295809611,-0.729803193940867));
#33154=DIRECTION('ref_axis',(0.,0.729803193940867,0.68365729580961));
#33155=DIRECTION('',(1.,0.,0.));
#33156=DIRECTION('',(0.,0.729803193940867,0.68365729580961));
#33157=DIRECTION('center_axis',(1.,0.,0.));
#33158=DIRECTION('ref_axis',(0.,0.984807753012208,-0.17364817766693));
#33159=DIRECTION('center_axis',(1.,0.,0.));
#33160=DIRECTION('ref_axis',(0.,1.,0.));
#33161=DIRECTION('center_axis',(0.,-0.956966182624129,-0.290199457811007));
#33162=DIRECTION('ref_axis',(0.,0.290199457811007,-0.956966182624129));
#33163=DIRECTION('',(-1.,0.,0.));
#33164=DIRECTION('',(0.,0.290199457811007,-0.956966182624129));
#33165=DIRECTION('',(1.,0.,0.));
#33166=DIRECTION('',(0.,0.290199457811007,-0.956966182624129));
#33167=DIRECTION('center_axis',(1.,0.,0.));
#33168=DIRECTION('ref_axis',(0.,0.939692620785908,-0.342020143325669));
#33169=DIRECTION('center_axis',(-1.,0.,0.));
#33170=DIRECTION('ref_axis',(0.,1.,0.));
#33171=DIRECTION('',(0.,0.837431687132078,0.546542010633328));
#33172=DIRECTION('center_axis',(0.,0.546542010633328,-0.837431687132078));
#33173=DIRECTION('ref_axis',(0.,0.837431687132078,0.546542010633328));
#33174=DIRECTION('',(1.,0.,0.));
#33175=DIRECTION('',(0.,0.837431687132078,0.546542010633328));
#33176=DIRECTION('center_axis',(1.,0.,0.));
#33177=DIRECTION('ref_axis',(0.,0.939692620785908,-0.342020143325669));
#33178=DIRECTION('center_axis',(1.,0.,0.));
#33179=DIRECTION('ref_axis',(0.,1.,0.));
#33180=DIRECTION('center_axis',(0.,-0.992820323027551,-0.11961524227066));
#33181=DIRECTION('ref_axis',(0.,0.11961524227066,-0.992820323027551));
#33182=DIRECTION('',(-1.,0.,0.));
#33183=DIRECTION('',(0.,0.11961524227066,-0.992820323027551));
#33184=DIRECTION('',(1.,0.,0.));
#33185=DIRECTION('',(0.,0.11961524227066,-0.992820323027551));
#33186=DIRECTION('center_axis',(1.,0.,0.));
#33187=DIRECTION('ref_axis',(0.,0.866025403784439,-0.5));
#33188=DIRECTION('center_axis',(-1.,0.,0.));
#33189=DIRECTION('ref_axis',(0.,1.,0.));
#33190=DIRECTION('',(0.,0.919615242270662,0.392820323027554));
#33191=DIRECTION('center_axis',(0.,0.392820323027554,-0.919615242270662));
#33192=DIRECTION('ref_axis',(0.,0.919615242270662,0.392820323027554));
#33193=DIRECTION('',(1.,0.,0.));
#33194=DIRECTION('',(0.,0.919615242270662,0.392820323027554));
#33195=DIRECTION('center_axis',(1.,0.,0.));
#33196=DIRECTION('ref_axis',(0.,0.866025403784439,-0.5));
#33197=DIRECTION('center_axis',(1.,0.,0.));
#33198=DIRECTION('ref_axis',(0.,1.,0.));
#33199=DIRECTION('center_axis',(0.,-0.998508120307106,0.0546034218778478));
#33200=DIRECTION('ref_axis',(0.,-0.0546034218778478,-0.998508120307106));
#33201=DIRECTION('',(-1.,0.,0.));
#33202=DIRECTION('',(0.,-0.0546034218778478,-0.998508120307106));
#33203=DIRECTION('',(1.,0.,0.));
#33204=DIRECTION('',(0.,-0.0546034218778478,-0.998508120307106));
#33205=DIRECTION('center_axis',(1.,0.,0.));
#33206=DIRECTION('ref_axis',(0.,0.766044443118978,-0.642787609686539));
#33207=DIRECTION('center_axis',(-1.,0.,0.));
#33208=DIRECTION('ref_axis',(0.,1.,0.));
#33209=DIRECTION('',(0.,0.973856753620618,0.227162988683262));
#33210=DIRECTION('center_axis',(0.,0.227162988683262,-0.973856753620618));
#33211=DIRECTION('ref_axis',(0.,0.973856753620618,0.227162988683262));
#33212=DIRECTION('',(1.,0.,0.));
#33213=DIRECTION('',(0.,0.973856753620618,0.227162988683262));
#33214=DIRECTION('center_axis',(1.,0.,0.));
#33215=DIRECTION('ref_axis',(0.,0.766044443118978,-0.642787609686539));
#33216=DIRECTION('center_axis',(1.,0.,0.));
#33217=DIRECTION('ref_axis',(0.,1.,0.));
#33218=DIRECTION('center_axis',(0.,-0.973856753620618,0.227162988683262));
#33219=DIRECTION('ref_axis',(0.,-0.227162988683262,-0.973856753620618));
#33220=DIRECTION('',(-1.,0.,0.));
#33221=DIRECTION('',(0.,-0.227162988683262,-0.973856753620618));
#33222=DIRECTION('',(1.,0.,0.));
#33223=DIRECTION('',(0.,-0.227162988683262,-0.973856753620618));
#33224=DIRECTION('center_axis',(1.,0.,0.));
#33225=DIRECTION('ref_axis',(0.,0.642787609686539,-0.766044443118978));
#33226=DIRECTION('center_axis',(-1.,0.,0.));
#33227=DIRECTION('ref_axis',(0.,1.,0.));
#33228=DIRECTION('',(0.,0.998508120307106,0.0546034218778477));
#33229=DIRECTION('center_axis',(0.,0.0546034218778477,-0.998508120307106));
#33230=DIRECTION('ref_axis',(0.,0.998508120307106,0.0546034218778477));
#33231=DIRECTION('',(1.,0.,0.));
#33232=DIRECTION('',(0.,0.998508120307106,0.0546034218778477));
#33233=DIRECTION('center_axis',(1.,0.,0.));
#33234=DIRECTION('ref_axis',(0.,0.642787609686539,-0.766044443118978));
#33235=DIRECTION('center_axis',(1.,0.,0.));
#33236=DIRECTION('ref_axis',(0.,1.,0.));
#33237=DIRECTION('center_axis',(0.,-0.919615242270662,0.392820323027554));
#33238=DIRECTION('ref_axis',(0.,-0.392820323027554,-0.919615242270662));
#33239=DIRECTION('',(-1.,0.,0.));
#33240=DIRECTION('',(0.,-0.392820323027554,-0.919615242270662));
#33241=DIRECTION('',(1.,0.,0.));
#33242=DIRECTION('',(0.,-0.392820323027554,-0.919615242270662));
#33243=DIRECTION('center_axis',(1.,0.,0.));
#33244=DIRECTION('ref_axis',(0.,0.5,-0.866025403784439));
#33245=DIRECTION('center_axis',(-1.,0.,0.));
#33246=DIRECTION('ref_axis',(0.,1.,0.));
#33247=DIRECTION('',(0.,0.992820323027551,-0.11961524227066));
#33248=DIRECTION('center_axis',(0.,-0.11961524227066,-0.992820323027551));
#33249=DIRECTION('ref_axis',(0.,0.992820323027551,-0.11961524227066));
#33250=DIRECTION('',(1.,0.,0.));
#33251=DIRECTION('',(0.,0.992820323027551,-0.11961524227066));
#33252=DIRECTION('center_axis',(1.,0.,0.));
#33253=DIRECTION('ref_axis',(0.,0.5,-0.866025403784439));
#33254=DIRECTION('center_axis',(1.,0.,0.));
#33255=DIRECTION('ref_axis',(0.,1.,0.));
#33256=DIRECTION('center_axis',(0.,-0.837431687132078,0.546542010633328));
#33257=DIRECTION('ref_axis',(0.,-0.546542010633328,-0.837431687132078));
#33258=DIRECTION('',(-1.,0.,0.));
#33259=DIRECTION('',(0.,-0.546542010633328,-0.837431687132078));
#33260=DIRECTION('',(1.,0.,0.));
#33261=DIRECTION('',(0.,-0.546542010633328,-0.837431687132078));
#33262=DIRECTION('center_axis',(1.,0.,0.));
#33263=DIRECTION('ref_axis',(0.,0.342020143325669,-0.939692620785908));
#33264=DIRECTION('center_axis',(-1.,0.,0.));
#33265=DIRECTION('ref_axis',(0.,1.,0.));
#33266=DIRECTION('',(0.,0.956966182624129,-0.290199457811007));
#33267=DIRECTION('center_axis',(0.,-0.290199457811007,-0.956966182624129));
#33268=DIRECTION('ref_axis',(0.,0.956966182624129,-0.290199457811007));
#33269=DIRECTION('',(1.,0.,0.));
#33270=DIRECTION('',(0.,0.956966182624129,-0.290199457811007));
#33271=DIRECTION('center_axis',(1.,0.,0.));
#33272=DIRECTION('ref_axis',(0.,0.342020143325669,-0.939692620785908));
#33273=DIRECTION('center_axis',(1.,0.,0.));
#33274=DIRECTION('ref_axis',(0.,1.,0.));
#33275=DIRECTION('center_axis',(0.,-0.729803193940867,0.683657295809611));
#33276=DIRECTION('ref_axis',(0.,-0.683657295809611,-0.729803193940867));
#33277=DIRECTION('',(-1.,0.,0.));
#33278=DIRECTION('',(0.,-0.683657295809611,-0.729803193940867));
#33279=DIRECTION('',(1.,0.,0.));
#33280=DIRECTION('',(0.,-0.683657295809611,-0.729803193940867));
#33281=DIRECTION('center_axis',(1.,0.,0.));
#33282=DIRECTION('ref_axis',(0.,0.17364817766693,-0.984807753012208));
#33283=DIRECTION('center_axis',(-1.,0.,0.));
#33284=DIRECTION('ref_axis',(0.,1.,0.));
#33285=DIRECTION('',(0.,0.892035109009926,-0.451966109673778));
#33286=DIRECTION('center_axis',(0.,-0.451966109673778,-0.892035109009926));
#33287=DIRECTION('ref_axis',(0.,0.892035109009926,-0.451966109673778));
#33288=DIRECTION('',(1.,0.,0.));
#33289=DIRECTION('',(0.,0.892035109009926,-0.451966109673778));
#33290=DIRECTION('center_axis',(1.,0.,0.));
#33291=DIRECTION('ref_axis',(0.,0.17364817766693,-0.984807753012208));
#33292=DIRECTION('center_axis',(1.,0.,0.));
#33293=DIRECTION('ref_axis',(0.,1.,0.));
#33294=DIRECTION('center_axis',(0.,-0.599999999999998,0.800000000000002));
#33295=DIRECTION('ref_axis',(0.,-0.800000000000002,-0.599999999999998));
#33296=DIRECTION('',(-1.,0.,0.));
#33297=DIRECTION('',(0.,-0.800000000000002,-0.599999999999998));
#33298=DIRECTION('',(1.,0.,0.));
#33299=DIRECTION('',(0.,-0.800000000000002,-0.599999999999998));
#33300=DIRECTION('center_axis',(1.,0.,0.));
#33301=DIRECTION('ref_axis',(0.,0.,-1.));
#33302=DIRECTION('center_axis',(-1.,0.,0.));
#33303=DIRECTION('ref_axis',(0.,1.,0.));
#33304=DIRECTION('',(0.,0.800000000000002,-0.599999999999998));
#33305=DIRECTION('center_axis',(0.,-0.599999999999998,-0.800000000000002));
#33306=DIRECTION('ref_axis',(0.,0.800000000000002,-0.599999999999998));
#33307=DIRECTION('',(1.,0.,0.));
#33308=DIRECTION('',(0.,0.800000000000002,-0.599999999999998));
#33309=DIRECTION('center_axis',(1.,0.,0.));
#33310=DIRECTION('ref_axis',(0.,0.,-1.));
#33311=DIRECTION('center_axis',(1.,0.,0.));
#33312=DIRECTION('ref_axis',(0.,1.,0.));
#33313=DIRECTION('center_axis',(0.,0.5,0.866025403784439));
#33314=DIRECTION('ref_axis',(0.,0.866025403784439,-0.5));
#33315=DIRECTION('',(0.,0.866025403784439,-0.5));
#33316=DIRECTION('',(-1.,0.,0.));
#33317=DIRECTION('',(0.,0.866025403784439,-0.5));
#33318=DIRECTION('',(-1.,0.,0.));
#33319=DIRECTION('center_axis',(0.,-0.5,0.866025403784439));
#33320=DIRECTION('ref_axis',(0.,0.866025403784439,0.5));
#33321=DIRECTION('',(0.,0.866025403784439,0.5));
#33322=DIRECTION('',(-1.,0.,0.));
#33323=DIRECTION('',(0.,0.866025403784439,0.5));
#33324=DIRECTION('center_axis',(0.,-1.,-1.20185167898973E-16));
#33325=DIRECTION('ref_axis',(0.,-1.20185167898973E-16,1.));
#33326=DIRECTION('',(0.,-1.20185167898973E-16,1.));
#33327=DIRECTION('',(-1.,0.,0.));
#33328=DIRECTION('',(0.,-1.20185167898973E-16,1.));
#33329=DIRECTION('center_axis',(0.,-0.5,-0.866025403784439));
#33330=DIRECTION('ref_axis',(0.,-0.866025403784439,0.5));
#33331=DIRECTION('',(0.,-0.866025403784439,0.5));
#33332=DIRECTION('',(-1.,0.,0.));
#33333=DIRECTION('',(0.,-0.866025403784439,0.5));
#33334=DIRECTION('center_axis',(0.,0.5,-0.866025403784439));
#33335=DIRECTION('ref_axis',(0.,-0.866025403784439,-0.5));
#33336=DIRECTION('',(0.,-0.866025403784439,-0.5));
#33337=DIRECTION('',(-1.,0.,0.));
#33338=DIRECTION('',(0.,-0.866025403784439,-0.5));
#33339=DIRECTION('center_axis',(0.,1.,-3.60555503696918E-16));
#33340=DIRECTION('ref_axis',(0.,-3.60555503696918E-16,-1.));
#33341=DIRECTION('',(0.,-3.60555503696918E-16,-1.));
#33342=DIRECTION('',(0.,-3.60555503696918E-16,-1.));
#33343=DIRECTION('center_axis',(-1.,0.,0.));
#33344=DIRECTION('ref_axis',(0.,0.,1.));
#33345=DIRECTION('center_axis',(-1.,0.,0.));
#33346=DIRECTION('ref_axis',(0.,0.,1.));
#33347=DIRECTION('center_axis',(1.,0.,0.));
#33348=DIRECTION('ref_axis',(0.,0.,-1.));
#33349=DIRECTION('center_axis',(1.,0.,0.));
#33350=DIRECTION('ref_axis',(0.,1.,0.));
#33351=DIRECTION('',(-0.707106781186553,0.707106781186542,8.65956056235487E-17));
#33352=DIRECTION('center_axis',(1.,0.,0.));
#33353=DIRECTION('ref_axis',(0.,-0.992415828451704,-0.122926089332239));
#33354=DIRECTION('center_axis',(-1.,0.,0.));
#33355=DIRECTION('ref_axis',(0.,1.,0.));
#33356=DIRECTION('center_axis',(-1.,0.,0.));
#33357=DIRECTION('ref_axis',(0.,1.,0.));
#33358=DIRECTION('center_axis',(1.,0.,0.));
#33359=DIRECTION('ref_axis',(0.,0.,-1.));
#33360=DIRECTION('',(0.995037190209989,0.0995037190209994,1.21856911002324E-17));
#33361=DIRECTION('center_axis',(1.,0.,0.));
#33362=DIRECTION('ref_axis',(0.,1.,0.));
#33363=DIRECTION('center_axis',(1.,0.,0.));
#33364=DIRECTION('ref_axis',(0.,0.,-1.));
#33365=DIRECTION('',(-1.,0.,0.));
#33366=DIRECTION('center_axis',(-1.,0.,0.));
#33367=DIRECTION('ref_axis',(0.,0.,1.));
#33368=DIRECTION('center_axis',(1.,0.,0.));
#33369=DIRECTION('ref_axis',(0.,0.,-1.));
#33370=DIRECTION('center_axis',(1.,0.,0.));
#33371=DIRECTION('ref_axis',(0.,1.,0.));
#33372=DIRECTION('center_axis',(1.,0.,0.));
#33373=DIRECTION('ref_axis',(0.,0.,-1.));
#33374=DIRECTION('',(-1.,0.,0.));
#33375=DIRECTION('',(-1.,0.,0.));
#33376=DIRECTION('center_axis',(-1.,0.,0.));
#33377=DIRECTION('ref_axis',(0.,1.,0.));
#33378=DIRECTION('center_axis',(1.,0.,0.));
#33379=DIRECTION('ref_axis',(0.,0.,-1.));
#33380=DIRECTION('',(-0.707106781186547,-0.707106781186548,-8.65956056235494E-17));
#33381=DIRECTION('center_axis',(1.,0.,0.));
#33382=DIRECTION('ref_axis',(0.,0.,-1.));
#40729=CARTESIAN_POINT('',(0.,0.,0.));
#40730=CARTESIAN_POINT('Origin',(-74.75,0.,0.));
#40731=CARTESIAN_POINT('',(-89.0911584740964,-4.92496730081785,0.000125565713578885));
#40732=CARTESIAN_POINT('',(-89.3088415259036,-4.92497224643154,8.66411886420825E-5));
#40733=CARTESIAN_POINT('',(-74.75,-4.925,-6.03138548580071E-16));
#40734=CARTESIAN_POINT('',(-89.575,2.16848376312314,4.42201352087158));
#40735=CARTESIAN_POINT('Ctrl Pts',(-89.0911584740964,-4.92496730081785,
0.000125565713578885));
#40736=CARTESIAN_POINT('Ctrl Pts',(-89.1008019864049,-4.92516638575022,
0.199069300706784));
#40737=CARTESIAN_POINT('Ctrl Pts',(-89.1104454987134,-4.91333770780035,
0.39798946055041));
#40738=CARTESIAN_POINT('Ctrl Pts',(-89.1200890110219,-4.889294230975,0.595422009497546));
#40739=CARTESIAN_POINT('Ctrl Pts',(-89.1595997107719,-4.79078504019411,
1.40432834080175));
#40740=CARTESIAN_POINT('Ctrl Pts',(-89.1991104105219,-4.48723269016115,
2.18826296024533));
#40741=CARTESIAN_POINT('Ctrl Pts',(-89.2386211102719,-4.01529023278917,
2.85257156086601));
#40742=CARTESIAN_POINT('Ctrl Pts',(-89.278131810022,-3.5433477754172,3.51688016148669));
#40743=CARTESIAN_POINT('Ctrl Pts',(-89.317642509772,-2.90301521070621,4.06156274328447));
#40744=CARTESIAN_POINT('Ctrl Pts',(-89.357153209522,-2.17161165738311,4.42084202425627));
#40745=CARTESIAN_POINT('Ctrl Pts',(-89.396663909272,-1.44020810406001,4.78012130522807));
#40746=CARTESIAN_POINT('Ctrl Pts',(-89.4361746090221,-0.617733562124788,
4.95399728537389));
#40747=CARTESIAN_POINT('Ctrl Pts',(-89.4756853087721,0.196500867390113,
4.92149114064075));
#40748=CARTESIAN_POINT('Ctrl Pts',(-89.5087902058481,0.878724851154841,
4.89425516196826));
#40749=CARTESIAN_POINT('Ctrl Pts',(-89.5418951029241,1.55516403718748,4.72213295031185));
#40750=CARTESIAN_POINT('Ctrl Pts',(-89.575,2.16857165393607,4.42207223182617));
#40751=CARTESIAN_POINT('',(-89.575,-2.16839587231079,4.42195480991671));
#40752=CARTESIAN_POINT('Origin',(-89.575,0.,0.));
#40753=CARTESIAN_POINT('Ctrl Pts',(-89.575,-2.16839587231078,4.42195480991671));
#40754=CARTESIAN_POINT('Ctrl Pts',(-89.53548930025,-2.90023837919386,4.06308088665816));
#40755=CARTESIAN_POINT('Ctrl Pts',(-89.4959786004999,-3.54091307931629,
3.5192055949212));
#40756=CARTESIAN_POINT('Ctrl Pts',(-89.4564679007499,-4.01330868267018,
2.85533993012661));
#40757=CARTESIAN_POINT('Ctrl Pts',(-89.4169572009999,-4.48570428602409,
2.191474265332));
#40758=CARTESIAN_POINT('Ctrl Pts',(-89.3774465012498,-4.78982079260945,
1.40761822747977));
#40759=CARTESIAN_POINT('Ctrl Pts',(-89.3379358014998,-4.88889138955698,
0.598745942138952));
#40760=CARTESIAN_POINT('Ctrl Pts',(-89.3282377096344,-4.91320874552475,
0.400204337453629));
#40761=CARTESIAN_POINT('Ctrl Pts',(-89.318539617769,-4.92517248101639,0.200155552119072));
#40762=CARTESIAN_POINT('Ctrl Pts',(-89.3088415259036,-4.92497224643154,
8.66411886420825E-5));
#40763=CARTESIAN_POINT('Origin',(-74.75,0.,0.));
#40764=CARTESIAN_POINT('',(-87.5911584740964,-4.92530808678391,-7.85116754067894E-5));
#40765=CARTESIAN_POINT('',(-87.8088415259036,-4.92531071258075,-7.76212487999366E-5));
#40766=CARTESIAN_POINT('',(-74.75,-4.925,-6.03138548580071E-16));
#40767=CARTESIAN_POINT('Ctrl Pts',(-87.5911584740964,-4.92530808678391,
-7.85116754067894E-5));
#40768=CARTESIAN_POINT('Ctrl Pts',(-87.6266735894045,-4.9247489168746,0.732444837198349));
#40769=CARTESIAN_POINT('Ctrl Pts',(-87.6621887047127,-4.75913849024366,
1.46521259091458));
#40770=CARTESIAN_POINT('Ctrl Pts',(-87.6977038200208,-4.44298152154857,
2.1259445723498));
#40771=CARTESIAN_POINT('Ctrl Pts',(-87.7372145197708,-4.09125570127135,
2.8610113941026));
#40772=CARTESIAN_POINT('Ctrl Pts',(-87.7767252195208,-3.55320374873502,
3.50692208746224));
#40773=CARTESIAN_POINT('Ctrl Pts',(-87.8162359192709,-2.89379421649954,
3.98568440246682));
#40774=CARTESIAN_POINT('Ctrl Pts',(-87.8557466190209,-2.23438468426406,
4.46444671747141));
#40775=CARTESIAN_POINT('Ctrl Pts',(-87.895257318771,-1.45361757232942,4.77606065412094));
#40776=CARTESIAN_POINT('Ctrl Pts',(-87.934768018521,-0.645768738251389,
4.88289953469631));
#40777=CARTESIAN_POINT('Ctrl Pts',(-87.974278718271,0.162080095826638,4.98973841527168));
#40778=CARTESIAN_POINT('Ctrl Pts',(-88.013789418021,0.997010652048049,4.89180223977289));
#40779=CARTESIAN_POINT('Ctrl Pts',(-88.053300117771,1.75820696011884,4.60091658286799));
#40780=CARTESIAN_POINT('Ctrl Pts',(-88.0928108175211,2.51940326818962,4.3100309259631));
#40781=CARTESIAN_POINT('Ctrl Pts',(-88.1323215172712,3.20686532810979,3.8261957876521));
#40782=CARTESIAN_POINT('Ctrl Pts',(-88.1718322170212,3.73758365539158,3.20783315584934));
#40783=CARTESIAN_POINT('Ctrl Pts',(-88.2113429167712,4.26830198267335,2.58947052404659));
#40784=CARTESIAN_POINT('Ctrl Pts',(-88.2508536165212,4.64227657731676,1.83658039875207));
#40785=CARTESIAN_POINT('Ctrl Pts',(-88.2903643162712,4.81435085620369,1.04007256938689));
#40786=CARTESIAN_POINT('Ctrl Pts',(-88.3298750160212,4.98642513509063,0.243564740021695));
#40787=CARTESIAN_POINT('Ctrl Pts',(-88.3693857157714,4.9565990982211,-0.596560793414167));
#40788=CARTESIAN_POINT('Ctrl Pts',(-88.4088964155214,4.72847417035112,-1.37886080863689));
#40789=CARTESIAN_POINT('Ctrl Pts',(-88.4484071152714,4.50034924248114,-2.16116082385961));
#40790=CARTESIAN_POINT('Ctrl Pts',(-88.4879178150213,4.07392542361072,-2.88563532086918));
#40791=CARTESIAN_POINT('Ctrl Pts',(-88.5274285147714,3.50069242553572,-3.46480558750653));
#40792=CARTESIAN_POINT('Ctrl Pts',(-88.5669392145214,2.92745942746073,-4.04397585414388));
#40793=CARTESIAN_POINT('Ctrl Pts',(-88.6064499142716,2.20741725018117,-4.47784189040901));
#40794=CARTESIAN_POINT('Ctrl Pts',(-88.6459606140216,1.42750934685709,-4.71401547804238));
#40795=CARTESIAN_POINT('Ctrl Pts',(-88.6854713137716,0.647601443533018,
-4.95018906567576));
#40796=CARTESIAN_POINT('Ctrl Pts',(-88.7249820135216,-0.192172185835564,
-4.98867020467737));
#40797=CARTESIAN_POINT('Ctrl Pts',(-88.7644927132716,-0.990410768169421,
-4.82481214047709));
#40798=CARTESIAN_POINT('Ctrl Pts',(-88.8040034130216,-1.78864935050328,
-4.6609540762768));
#40799=CARTESIAN_POINT('Ctrl Pts',(-88.8435141127716,-2.54535288580243,
-4.2947568088746));
#40800=CARTESIAN_POINT('Ctrl Pts',(-88.8830248125217,-3.16915116407065,
-3.77043831961749));
#40801=CARTESIAN_POINT('Ctrl Pts',(-88.9225355122717,-3.79294944233888,
-3.24611983036038));
#40802=CARTESIAN_POINT('Ctrl Pts',(-88.9620462120217,-4.2838424635762,-2.56368011924835));
#40803=CARTESIAN_POINT('Ctrl Pts',(-89.0015569117718,-4.58255595843045,
-1.80552124210991));
#40804=CARTESIAN_POINT('Ctrl Pts',(-89.0314240992133,-4.80836142374944,
-1.23240880833286));
#40805=CARTESIAN_POINT('Ctrl Pts',(-89.0612912866549,-4.92435070939332,
-0.616028552547382));
#40806=CARTESIAN_POINT('Ctrl Pts',(-89.0911584740964,-4.92496730081785,
0.000125565713578885));
#40807=CARTESIAN_POINT('Ctrl Pts',(-89.3088415259036,-4.92497224643154,
8.66411886420825E-5));
#40808=CARTESIAN_POINT('Ctrl Pts',(-89.279028918019,-4.92435671141227,-0.614939084929097));
#40809=CARTESIAN_POINT('Ctrl Pts',(-89.2492163101344,-4.80879283960139,
-1.23015499597478));
#40810=CARTESIAN_POINT('Ctrl Pts',(-89.2194037022498,-4.58378991023707,
-1.80236265130469));
#40811=CARTESIAN_POINT('Ctrl Pts',(-89.1798930024997,-4.28559314665994,
-2.56071042657812));
#40812=CARTESIAN_POINT('Ctrl Pts',(-89.1403823027497,-3.79517493219598,
-3.2435174442956));
#40813=CARTESIAN_POINT('Ctrl Pts',(-89.1008716029996,-3.17173808087882,
-3.76827140867339));
#40814=CARTESIAN_POINT('Ctrl Pts',(-89.0613609032496,-2.54830122956167,
-4.29302537305117));
#40815=CARTESIAN_POINT('Ctrl Pts',(-89.0218502034996,-1.79184574139134,
-4.65972628408927));
#40816=CARTESIAN_POINT('Ctrl Pts',(-88.9823395037496,-0.993718901765311,
-4.82412795080569));
#40817=CARTESIAN_POINT('Ctrl Pts',(-88.9428288039996,-0.195592062139286,
-4.98852961752212));
#40818=CARTESIAN_POINT('Ctrl Pts',(-88.9033181042495,0.644206128942427,
-4.95063203991687));
#40819=CARTESIAN_POINT('Ctrl Pts',(-88.8638074044994,1.42427542185869,-4.71499532883177));
#40820=CARTESIAN_POINT('Ctrl Pts',(-88.8242967047494,2.20434471477496,-4.47935861774667));
#40821=CARTESIAN_POINT('Ctrl Pts',(-88.7847860049995,2.92468510952578,-4.04598277318171));
#40822=CARTESIAN_POINT('Ctrl Pts',(-88.7452753052494,3.49831541151597,-3.46720485621925));
#40823=CARTESIAN_POINT('Ctrl Pts',(-88.7057646054994,4.07194571350615,-2.88842693925679));
#40824=CARTESIAN_POINT('Ctrl Pts',(-88.6662539057493,4.49886592273571,-2.16424694989684));
#40825=CARTESIAN_POINT('Ctrl Pts',(-88.6267432059993,4.72752724946008,-1.38210405139087));
#40826=CARTESIAN_POINT('Ctrl Pts',(-88.5872325062492,4.95618857618444,-0.599961152884894));
#40827=CARTESIAN_POINT('Ctrl Pts',(-88.5477218064993,4.98659102040361,0.240144654767101));
#40828=CARTESIAN_POINT('Ctrl Pts',(-88.5082111067493,4.81506313048895,1.0367705513221));
#40829=CARTESIAN_POINT('Ctrl Pts',(-88.4687004069992,4.64353524057429,1.8333964478771));
#40830=CARTESIAN_POINT('Ctrl Pts',(-88.4291897072492,4.2700770165258,2.58654243333511));
#40831=CARTESIAN_POINT('Ctrl Pts',(-88.3896790074991,3.73978290287187,3.20526880665016));
#40832=CARTESIAN_POINT('Ctrl Pts',(-88.3501683077491,3.20948878921794,3.82399517996522));
#40833=CARTESIAN_POINT('Ctrl Pts',(-88.3106576079991,2.52235878595858,4.30830194113731));
#40834=CARTESIAN_POINT('Ctrl Pts',(-88.2711469082491,1.76136217724779,4.59970966687813));
#40835=CARTESIAN_POINT('Ctrl Pts',(-88.231636208499,1.000365568537,4.89111739261894));
#40836=CARTESIAN_POINT('Ctrl Pts',(-88.192125508749,0.165502354374793,4.98962608292848));
#40837=CARTESIAN_POINT('Ctrl Pts',(-88.1526148089989,-0.642419574094824,
4.8833412755425));
#40838=CARTESIAN_POINT('Ctrl Pts',(-88.1131041092489,-1.45034150256444,
4.77705646815652));
#40839=CARTESIAN_POINT('Ctrl Pts',(-88.0735934094989,-2.23132214534146,
4.46597816307502));
#40840=CARTESIAN_POINT('Ctrl Pts',(-88.0340827097488,-2.89105988744621,
3.98766824144186));
#40841=CARTESIAN_POINT('Ctrl Pts',(-87.9945720099988,-3.55079762955095,
3.50935831980869));
#40842=CARTESIAN_POINT('Ctrl Pts',(-87.9550613102488,-4.08929247098342,
2.86381678162386));
#40843=CARTESIAN_POINT('Ctrl Pts',(-87.9155506104988,-4.44152236847542,
2.12899136191391));
#40844=CARTESIAN_POINT('Ctrl Pts',(-87.8799809156337,-4.75861900446021,
1.46746129224844));
#40845=CARTESIAN_POINT('Ctrl Pts',(-87.8444112207687,-4.92475561418818,
0.733570332690291));
#40846=CARTESIAN_POINT('Ctrl Pts',(-87.8088415259036,-4.92531071258075,
-7.76212487999366E-5));
#40847=CARTESIAN_POINT('Origin',(-74.75,0.,0.));
#40848=CARTESIAN_POINT('',(-86.0911584740964,-4.92460688967043,-3.93952561872357E-5));
#40849=CARTESIAN_POINT('',(-86.3088415259036,-4.92460788888033,-4.03740411281871E-5));
#40850=CARTESIAN_POINT('',(-74.75,-4.925,-6.03138548580071E-16));
#40851=CARTESIAN_POINT('Ctrl Pts',(-86.0911584740964,-4.92460688967043,
-3.93952561872357E-5));
#40852=CARTESIAN_POINT('Ctrl Pts',(-86.1130344926542,-4.92447945269054,
0.451353233852372));
#40853=CARTESIAN_POINT('Ctrl Pts',(-86.1349105112119,-4.86294930864971,
0.902779916062517));
#40854=CARTESIAN_POINT('Ctrl Pts',(-86.1567865297696,-4.7404755378458,1.33701787580212));
#40855=CARTESIAN_POINT('Ctrl Pts',(-86.1962972295197,-4.5192732942697,2.12130344413084));
#40856=CARTESIAN_POINT('Ctrl Pts',(-86.2358079292698,-4.0992688572054,2.84951824818281));
#40857=CARTESIAN_POINT('Ctrl Pts',(-86.2753186290198,-3.53117680957672,
3.43373200244815));
#40858=CARTESIAN_POINT('Ctrl Pts',(-86.3148293287698,-2.96308476194804,
4.01794575671349));
#40859=CARTESIAN_POINT('Ctrl Pts',(-86.3543400285198,-2.24690510375498,
4.4581584611922));
#40860=CARTESIAN_POINT('Ctrl Pts',(-86.3938507282698,-1.46911490394863,
4.70121543051628));
#40861=CARTESIAN_POINT('Ctrl Pts',(-86.4333614280199,-0.691324704142275,
4.94427239984037));
#40862=CARTESIAN_POINT('Ctrl Pts',(-86.4728721277699,0.148076037277391,
4.99017363400982));
#40863=CARTESIAN_POINT('Ctrl Pts',(-86.51238282752,0.947731585107635,4.83337666313305));
#40864=CARTESIAN_POINT('Ctrl Pts',(-86.55189352727,1.74738713293789,4.67657969225627));
#40865=CARTESIAN_POINT('Ctrl Pts',(-86.59140422702,2.50729748717871,4.31708451633328));
#40866=CARTESIAN_POINT('Ctrl Pts',(-86.63091492677,3.13570519654186,3.79829936228145));
#40867=CARTESIAN_POINT('Ctrl Pts',(-86.67042562652,3.76411290590501,3.27951420822963));
#40868=CARTESIAN_POINT('Ctrl Pts',(-86.7099363262701,4.26101797039046,2.60143907604898));
#40869=CARTESIAN_POINT('Ctrl Pts',(-86.7494470260201,4.5664202307754,1.84594999961959));
#40870=CARTESIAN_POINT('Ctrl Pts',(-86.7889577257702,4.87182249116034,1.09046092319019));
#40871=CARTESIAN_POINT('Ctrl Pts',(-86.8284684255202,4.98572194744478,0.257557902512059));
#40872=CARTESIAN_POINT('Ctrl Pts',(-86.8679791252702,4.89436549868289,-0.552187912247182));
#40873=CARTESIAN_POINT('Ctrl Pts',(-86.9074898250202,4.803009049921,-1.36193372700643));
#40874=CARTESIAN_POINT('Ctrl Pts',(-86.9470005247703,4.50639669611276,-2.14852233584678));
#40875=CARTESIAN_POINT('Ctrl Pts',(-86.9865112245203,4.04034370606447,-2.81697494876789));
#40876=CARTESIAN_POINT('Ctrl Pts',(-87.0260219242703,3.57429071601619,-3.485427561689));
#40877=CARTESIAN_POINT('Ctrl Pts',(-87.0655326240203,2.93879708972785,-4.03574417869087));
#40878=CARTESIAN_POINT('Ctrl Pts',(-87.1050433237703,2.21059724084878,-4.40147531674411));
#40879=CARTESIAN_POINT('Ctrl Pts',(-87.1445540235204,1.48239739196973,-4.76720645479734));
#40880=CARTESIAN_POINT('Ctrl Pts',(-87.1840647232705,0.661491320499941,
-4.94835211390195));
#40881=CARTESIAN_POINT('Ctrl Pts',(-87.2235754230205,-0.152998427797419,
-4.9230393667081));
#40882=CARTESIAN_POINT('Ctrl Pts',(-87.2630861227705,-0.967488176094782,
-4.89772661951426));
#40883=CARTESIAN_POINT('Ctrl Pts',(-87.3025968225205,-1.77556160121972,
-4.66595546602198));
#40884=CARTESIAN_POINT('Ctrl Pts',(-87.3421075222705,-2.47964567033799,
-4.25571174714818));
#40885=CARTESIAN_POINT('Ctrl Pts',(-87.3816182220206,-3.18372973945627,
-3.84546802827438));
#40886=CARTESIAN_POINT('Ctrl Pts',(-87.4211289217706,-3.78382445256787,
-3.25675174401907));
#40887=CARTESIAN_POINT('Ctrl Pts',(-87.4606396215206,-4.20746973448743,
-2.56064905021327));
#40888=CARTESIAN_POINT('Ctrl Pts',(-87.5001503212707,-4.63111501640699,
-1.86454635640747));
#40889=CARTESIAN_POINT('Ctrl Pts',(-87.5396610210207,-4.87831086713451,
-1.06105725305119));
#40890=CARTESIAN_POINT('Ctrl Pts',(-87.5791717207707,-4.91920894848921,
-0.247201226300066));
#40891=CARTESIAN_POINT('Ctrl Pts',(-87.5831673052126,-4.92334483417583,
-0.164898698149252));
#40892=CARTESIAN_POINT('Ctrl Pts',(-87.5871628896545,-4.92537099550801,
-0.0824901516404431));
#40893=CARTESIAN_POINT('Ctrl Pts',(-87.5911584740964,-4.92530808678391,
-7.85116754067894E-5));
#40894=CARTESIAN_POINT('Ctrl Pts',(-87.8088415259036,-4.92531071258075,
-7.76212487999366E-5));
#40895=CARTESIAN_POINT('Ctrl Pts',(-87.8049005210186,-4.92537221565197,
-0.0813633950316671));
#40896=CARTESIAN_POINT('Ctrl Pts',(-87.8009595161336,-4.92340105512627,
-0.162646185699621));
#40897=CARTESIAN_POINT('Ctrl Pts',(-87.7970185112487,-4.91937734387943,
-0.243827242497861));
#40898=CARTESIAN_POINT('Ctrl Pts',(-87.7575078114986,-4.87903746823992,
-1.05771112596459));
#40899=CARTESIAN_POINT('Ctrl Pts',(-87.7179971117486,-4.63239276340937,
-1.86136959166297));
#40900=CARTESIAN_POINT('Ctrl Pts',(-87.6784864119986,-4.20922501477751,
-2.55776268860029));
#40901=CARTESIAN_POINT('Ctrl Pts',(-87.6389757122486,-3.78605726614565,
-3.25415578553761));
#40902=CARTESIAN_POINT('Ctrl Pts',(-87.5994650124986,-3.18636647371249,
-3.84328351371386));
#40903=CARTESIAN_POINT('Ctrl Pts',(-87.5599543127485,-2.48256394173379,
-4.25401004368527));
#40904=CARTESIAN_POINT('Ctrl Pts',(-87.5204436129985,-1.77876140975508,
-4.66473657365668));
#40905=CARTESIAN_POINT('Ctrl Pts',(-87.4809329132484,-0.970847138230837,
-4.89706190542324));
#40906=CARTESIAN_POINT('Ctrl Pts',(-87.4414222134984,-0.156374941776677,
-4.92293327867082));
#40907=CARTESIAN_POINT('Ctrl Pts',(-87.4019115137484,0.658097254677483,
-4.9488046519184));
#40908=CARTESIAN_POINT('Ctrl Pts',(-87.3624008139984,1.47912737606156,-4.768222066647));
#40909=CARTESIAN_POINT('Ctrl Pts',(-87.3228901142484,2.20757789747824,-4.4029904621196));
#40910=CARTESIAN_POINT('Ctrl Pts',(-87.2833794144984,2.93602841889492,-4.03775885759221));
#40911=CARTESIAN_POINT('Ctrl Pts',(-87.2438687147483,3.57189934034421,-3.48787823380882));
#40912=CARTESIAN_POINT('Ctrl Pts',(-87.2043580149983,4.03841069083489,-2.81974542771263));
#40913=CARTESIAN_POINT('Ctrl Pts',(-87.1648473152482,4.50492204132558,-2.15161262161645));
#40914=CARTESIAN_POINT('Ctrl Pts',(-87.1253366154982,4.80207382085767,-1.36522763320748));
#40915=CARTESIAN_POINT('Ctrl Pts',(-87.0858259157482,4.89398562609676,-0.555544666224829));
#40916=CARTESIAN_POINT('Ctrl Pts',(-87.0463152159981,4.98589743133585,0.254138300757821));
#40917=CARTESIAN_POINT('Ctrl Pts',(-87.0068045162482,4.87256926228193,1.08711924631414));
#40918=CARTESIAN_POINT('Ctrl Pts',(-86.9672938164981,4.56768523829136,1.84281761124461));
#40919=CARTESIAN_POINT('Ctrl Pts',(-86.9277831167481,4.26280121430078,2.59851597617508));
#40920=CARTESIAN_POINT('Ctrl Pts',(-86.888272416998,3.76636133537354,3.2769317604797));
#40921=CARTESIAN_POINT('Ctrl Pts',(-86.848761717248,3.13830959060805,3.79614779719784));
#40922=CARTESIAN_POINT('Ctrl Pts',(-86.8092510174979,2.51025784584256,4.31536383391598));
#40923=CARTESIAN_POINT('Ctrl Pts',(-86.769740317748,1.75059423523883,4.67538012304765));
#40924=CARTESIAN_POINT('Ctrl Pts',(-86.7302296179979,0.951046416362449,
4.83272551449205));
#40925=CARTESIAN_POINT('Ctrl Pts',(-86.6907189182479,0.15149859748607,4.99007090593645));
#40926=CARTESIAN_POINT('Ctrl Pts',(-86.6512082184979,-0.687933429662953,
4.94474539969359));
#40927=CARTESIAN_POINT('Ctrl Pts',(-86.6116975187478,-1.4658901522069,4.70222194778708));
#40928=CARTESIAN_POINT('Ctrl Pts',(-86.5721868189978,-2.24384687475085,
4.45969849588057));
#40929=CARTESIAN_POINT('Ctrl Pts',(-86.5326761192478,-2.96032829268972,
4.01997709831041));
#40930=CARTESIAN_POINT('Ctrl Pts',(-86.4931654194977,-3.52882090026483,
3.4361531162634));
#40931=CARTESIAN_POINT('Ctrl Pts',(-86.4536547197477,-4.09731350783993,
2.85232913421639));
#40932=CARTESIAN_POINT('Ctrl Pts',(-86.4141440199977,-4.51781730505126,
2.12440256769253));
#40933=CARTESIAN_POINT('Ctrl Pts',(-86.3746333202476,-4.73955741237156,
1.34026889816745));
#40934=CARTESIAN_POINT('Ctrl Pts',(-86.3527027221329,-4.86263529280175,
0.905031848878518));
#40935=CARTESIAN_POINT('Ctrl Pts',(-86.3307721240183,-4.92447692699912,
0.452478196132976));
#40936=CARTESIAN_POINT('Ctrl Pts',(-86.3088415259036,-4.92460788888033,
-4.03740411281871E-5));
#40937=CARTESIAN_POINT('Origin',(-74.75,0.,0.));
#40938=CARTESIAN_POINT('',(-84.5911584740964,-4.92505771915203,0.000122489528405073));
#40939=CARTESIAN_POINT('',(-84.8088415259036,-4.9250542018855,0.000122701850775453));
#40940=CARTESIAN_POINT('',(-74.75,-4.925,-6.03138548580071E-16));
#40941=CARTESIAN_POINT('Ctrl Pts',(-84.5911584740964,-4.92505771915203,
0.000122489528405073));
#40942=CARTESIAN_POINT('Ctrl Pts',(-84.5993953959038,-4.92523071445293,
0.170039545814198));
#40943=CARTESIAN_POINT('Ctrl Pts',(-84.6076323177112,-4.91660717945727,
0.339939127731318));
#40944=CARTESIAN_POINT('Ctrl Pts',(-84.6158692395186,-4.89905445633691,
0.508911150373288));
#40945=CARTESIAN_POINT('Ctrl Pts',(-84.6553799392686,-4.81485790946881,
1.31943272735152));
#40946=CARTESIAN_POINT('Ctrl Pts',(-84.6948906390186,-4.52520881587572,
2.10861200392612));
#40947=CARTESIAN_POINT('Ctrl Pts',(-84.7344013387686,-4.06508164649063,
2.78115737283848));
#40948=CARTESIAN_POINT('Ctrl Pts',(-84.7739120385187,-3.60495447710555,
3.45370274175085));
#40949=CARTESIAN_POINT('Ctrl Pts',(-84.8134227382687,-2.97434923192847,
4.00961420300098));
#40950=CARTESIAN_POINT('Ctrl Pts',(-84.8529334380187,-2.24941006367898,
4.38176670882289));
#40951=CARTESIAN_POINT('Ctrl Pts',(-84.8924441377688,-1.52447089542949,
4.7539192146448));
#40952=CARTESIAN_POINT('Ctrl Pts',(-84.9319548375188,-0.705197804107595,
4.9423127650385));
#40953=CARTESIAN_POINT('Ctrl Pts',(-84.9714655372688,0.109483843170341,
4.92419926619684));
#40954=CARTESIAN_POINT('Ctrl Pts',(-85.0109762370189,0.924165490448288,
4.90608576735518));
#40955=CARTESIAN_POINT('Ctrl Pts',(-85.0504869367689,1.73425569368228,4.68146521927817));
#40956=CARTESIAN_POINT('Ctrl Pts',(-85.0899976365189,2.44193789865959,4.27746004355608));
#40957=CARTESIAN_POINT('Ctrl Pts',(-85.129508336269,3.14962010363691,3.87345486783399));
#40958=CARTESIAN_POINT('Ctrl Pts',(-85.1690190360189,3.75489431035756,3.29006506446682));
#40959=CARTESIAN_POINT('Ctrl Pts',(-85.208529735769,4.1846750315278,2.59773362869188));
#40960=CARTESIAN_POINT('Ctrl Pts',(-85.248040435519,4.61445575269803,1.90540219291694));
#40961=CARTESIAN_POINT('Ctrl Pts',(-85.2875511352691,4.86874298831785,1.10412912473424));
#40962=CARTESIAN_POINT('Ctrl Pts',(-85.3270618350191,4.91683213158013,0.290666329302215));
#40963=CARTESIAN_POINT('Ctrl Pts',(-85.3665725347691,4.96492127484241,-0.522796466129817));
#40964=CARTESIAN_POINT('Ctrl Pts',(-85.4060832345191,4.80681232574716,-1.34844898881116));
#40965=CARTESIAN_POINT('Ctrl Pts',(-85.4455939342692,4.46159658120049,-2.08659556976164));
#40966=CARTESIAN_POINT('Ctrl Pts',(-85.4851046340192,4.11638083665383,-2.82474215071212));
#40967=CARTESIAN_POINT('Ctrl Pts',(-85.5246153337692,3.58405829665576,-3.47538278993172));
#40968=CARTESIAN_POINT('Ctrl Pts',(-85.5641260335192,2.92890570024658,-3.95995410632395));
#40969=CARTESIAN_POINT('Ctrl Pts',(-85.6036367332693,2.27375310383739,-4.44452542271619));
#40970=CARTESIAN_POINT('Ctrl Pts',(-85.6431474330193,1.49577045101708,-4.76302741628104));
#40971=CARTESIAN_POINT('Ctrl Pts',(-85.6826581327693,0.688897382127365,
-4.87700169387165));
#40972=CARTESIAN_POINT('Ctrl Pts',(-85.7221688325194,-0.117975686762337,
-4.99097597146226));
#40973=CARTESIAN_POINT('Ctrl Pts',(-85.7616795322694,-0.953739171721445,
-4.90042253307862));
#40974=CARTESIAN_POINT('Ctrl Pts',(-85.8011902320194,-1.71747652801316,
-4.61627550096966));
#40975=CARTESIAN_POINT('Ctrl Pts',(-85.8407009317694,-2.48121388430487,
-4.3321284688607));
#40976=CARTESIAN_POINT('Ctrl Pts',(-85.8802116315195,-3.17292511192919,
-3.85438784302641));
#40977=CARTESIAN_POINT('Ctrl Pts',(-85.9197223312695,-3.70908764941538,
-3.24073972020018));
#40978=CARTESIAN_POINT('Ctrl Pts',(-85.9592330310196,-4.24525018690158,
-2.62709159737394));
#40979=CARTESIAN_POINT('Ctrl Pts',(-85.9987437307696,-4.62586403424964,
-1.87753597755575));
#40980=CARTESIAN_POINT('Ctrl Pts',(-86.0382544305196,-4.80497093287972,
-1.08258000134392));
#40981=CARTESIAN_POINT('Ctrl Pts',(-86.0558891117119,-4.88491112823595,
-0.727769904557915));
#40982=CARTESIAN_POINT('Ctrl Pts',(-86.0735237929042,-4.92470961908193,
-0.363915714242581));
#40983=CARTESIAN_POINT('Ctrl Pts',(-86.0911584740964,-4.92460688967043,
-3.93952561872357E-5));
#40984=CARTESIAN_POINT('Ctrl Pts',(-86.3088415259036,-4.92460788888033,
-4.03740411281871E-5));
#40985=CARTESIAN_POINT('Ctrl Pts',(-86.2912614242683,-4.92471287111428,
-0.362790282362978));
#40986=CARTESIAN_POINT('Ctrl Pts',(-86.273681322633,-4.88516247587605,-0.725517646567889));
#40987=CARTESIAN_POINT('Ctrl Pts',(-86.2561012209976,-4.80571231438,-1.07928417758196));
#40988=CARTESIAN_POINT('Ctrl Pts',(-86.2165905212476,-4.62715069163887,
-1.87436281128003));
#40989=CARTESIAN_POINT('Ctrl Pts',(-86.1770798214975,-4.24705102872735,
-2.62417930614987));
#40990=CARTESIAN_POINT('Ctrl Pts',(-86.1375691217475,-3.71130949762144,
-3.2381950215242));
#40991=CARTESIAN_POINT('Ctrl Pts',(-86.0980584219974,-3.17556796651552,
-3.85221073689853));
#40992=CARTESIAN_POINT('Ctrl Pts',(-86.0585477222474,-2.4841845672152,-4.33042567277734));
#40993=CARTESIAN_POINT('Ctrl Pts',(-86.0190370224974,-1.72064227666466,
-4.6150964605646));
#40994=CARTESIAN_POINT('Ctrl Pts',(-85.9795263227474,-0.957099986114123,
-4.89976724835186));
#40995=CARTESIAN_POINT('Ctrl Pts',(-85.9400156229973,-0.121398804313364,
-4.99089388804757));
#40996=CARTESIAN_POINT('Ctrl Pts',(-85.9005049232473,0.685552246965759,
-4.87747304464519));
#40997=CARTESIAN_POINT('Ctrl Pts',(-85.8609942234973,1.49250329824487,-4.76405220124282));
#40998=CARTESIAN_POINT('Ctrl Pts',(-85.8214835237472,2.27070421900234,-4.44608387474238));
#40999=CARTESIAN_POINT('Ctrl Pts',(-85.7819728239972,2.92618901353828,-3.9619620192032));
#41000=CARTESIAN_POINT('Ctrl Pts',(-85.7424621242472,3.58167380807422,-3.47784016366402));
#41001=CARTESIAN_POINT('Ctrl Pts',(-85.7029514244972,4.11444247638863,-2.82756477908611));
#41002=CARTESIAN_POINT('Ctrl Pts',(-85.6634407247471,4.4601644104591,-2.08965514289672));
#41003=CARTESIAN_POINT('Ctrl Pts',(-85.6239300249971,4.80588634452957,-1.35174550670734));
#41004=CARTESIAN_POINT('Ctrl Pts',(-85.5844193252471,4.9645615443561,-0.526201618906478));
#41005=CARTESIAN_POINT('Ctrl Pts',(-85.544908625497,4.91703033954142,0.287293968941061));
#41006=CARTESIAN_POINT('Ctrl Pts',(-85.505397925747,4.86949913472673,1.1007895567886));
#41007=CARTESIAN_POINT('Ctrl Pts',(-85.465887225997,4.61576152527082,1.90223684468283));
#41008=CARTESIAN_POINT('Ctrl Pts',(-85.426376526247,4.18645575186844,2.59486289083034));
#41009=CARTESIAN_POINT('Ctrl Pts',(-85.386865826497,3.75714997846606,3.28748893697786));
#41010=CARTESIAN_POINT('Ctrl Pts',(-85.3473551267469,3.15227604111722,3.87129374137866));
#41011=CARTESIAN_POINT('Ctrl Pts',(-85.3078444269969,2.44487109549709,4.27578419836216));
#41012=CARTESIAN_POINT('Ctrl Pts',(-85.2683337272468,1.73746614987695,4.68027465534567));
#41013=CARTESIAN_POINT('Ctrl Pts',(-85.2288230274968,0.927530195985523,
4.90545076491186));
#41014=CARTESIAN_POINT('Ctrl Pts',(-85.1893123277468,0.112861162777333,
4.92412302268102));
#41015=CARTESIAN_POINT('Ctrl Pts',(-85.1498016279967,-0.701807870430851,
4.94279528045018));
#41016=CARTESIAN_POINT('Ctrl Pts',(-85.1102909282467,-1.5212099829558,4.75496368642231));
#41017=CARTESIAN_POINT('Ctrl Pts',(-85.0707802284967,-2.24640422866356,
4.38330847944828));
#41018=CARTESIAN_POINT('Ctrl Pts',(-85.0312695287467,-2.97159847437131,
4.01165327247425));
#41019=CARTESIAN_POINT('Ctrl Pts',(-84.9917588289967,-3.60258485326187,
3.45617445255406));
#41020=CARTESIAN_POINT('Ctrl Pts',(-84.9522481292466,-4.06317319158446,
2.78394482699462));
#41021=CARTESIAN_POINT('Ctrl Pts',(-84.9127374294966,-4.52376152990704,
2.11171520143517));
#41022=CARTESIAN_POINT('Ctrl Pts',(-84.8732267297466,-4.81395182766163,
1.32273477023646));
#41023=CARTESIAN_POINT('Ctrl Pts',(-84.8337160299966,-4.89870426474054,
0.51227113052908));
#41024=CARTESIAN_POINT('Ctrl Pts',(-84.8254245286322,-4.91648995196233,
0.342191622525732));
#41025=CARTESIAN_POINT('Ctrl Pts',(-84.8171330272679,-4.92522837245193,
0.171166016675559));
#41026=CARTESIAN_POINT('Ctrl Pts',(-84.8088415259036,-4.9250542018855,0.000122701850775453));
#41027=CARTESIAN_POINT('Origin',(-74.75,0.,0.));
#41028=CARTESIAN_POINT('',(-83.0911584740965,-4.92523349004336,-9.88184705141837E-5));
#41029=CARTESIAN_POINT('',(-83.3088415259037,-4.92523661103536,-9.81287755307904E-5));
#41030=CARTESIAN_POINT('',(-74.75,-4.925,-6.03138548580071E-16));
#41031=CARTESIAN_POINT('Ctrl Pts',(-83.0911584740965,-4.92523349004336,
-9.88184705141837E-5));
#41032=CARTESIAN_POINT('Ctrl Pts',(-83.1252669989035,-4.92459715090507,
0.70344350101895));
#41033=CARTESIAN_POINT('Ctrl Pts',(-83.1593755237105,-4.77223537727082,
1.40725258976148));
#41034=CARTESIAN_POINT('Ctrl Pts',(-83.1934840485175,-4.47986315706691,
2.04708358868986));
#41035=CARTESIAN_POINT('Ctrl Pts',(-83.2329947482675,-4.14118445216601,
2.78825227400949));
#41036=CARTESIAN_POINT('Ctrl Pts',(-83.2725054480176,-3.61463290306591,
3.44357203880708));
#41037=CARTESIAN_POINT('Ctrl Pts',(-83.3120161477676,-2.96378841474844,
3.93391450818797));
#41038=CARTESIAN_POINT('Ctrl Pts',(-83.3515268475176,-2.31294392643097,
4.42425697756886));
#41039=CARTESIAN_POINT('Ctrl Pts',(-83.3910375472677,-1.53780649889613,
4.74962215153305));
#41040=CARTESIAN_POINT('Ctrl Pts',(-83.4305482470177,-0.731972217987289,
4.87072292347077));
#41041=CARTESIAN_POINT('Ctrl Pts',(-83.4700589467677,0.0738620629215621,
4.99182369540848));
#41042=CARTESIAN_POINT('Ctrl Pts',(-83.5095696465177,0.910393197204418,
4.90866006531972));
#41043=CARTESIAN_POINT('Ctrl Pts',(-83.5490803462678,1.67661194821018,4.6312738528668));
#41044=CARTESIAN_POINT('Ctrl Pts',(-83.5885910460178,2.44283069921593,4.35388764041389));
#41045=CARTESIAN_POINT('Ctrl Pts',(-83.6281017457678,3.1387370669446,3.88227884559683));
#41046=CARTESIAN_POINT('Ctrl Pts',(-83.6676124455178,3.68030193627522,3.2733931604648));
#41047=CARTESIAN_POINT('Ctrl Pts',(-83.7071231452679,4.22186680560584,2.66450747533277));
#41048=CARTESIAN_POINT('Ctrl Pts',(-83.7466338450179,4.60909017653842,1.91834489988576));
#41049=CARTESIAN_POINT('Ctrl Pts',(-83.786144544768,4.79521570551511,1.12500287231193));
#41050=CARTESIAN_POINT('Ctrl Pts',(-83.825655244518,4.9813412344918,0.33166084473811));
#41051=CARTESIAN_POINT('Ctrl Pts',(-83.865165944268,4.96636892151259,-0.508860634962529));
#41052=CARTESIAN_POINT('Ctrl Pts',(-83.9046766440181,4.7521066394025,-1.29507050498247));
#41053=CARTESIAN_POINT('Ctrl Pts',(-83.9441873437681,4.5378443572924,-2.0812803750024));
#41054=CARTESIAN_POINT('Ctrl Pts',(-83.9836980435181,4.12429210605142,-2.81317863534163));
#41055=CARTESIAN_POINT('Ctrl Pts',(-84.0232087432682,3.56138538180307,-3.40239023150024));
#41056=CARTESIAN_POINT('Ctrl Pts',(-84.0627194430182,2.99847865755472,-3.99160182765885));
#41057=CARTESIAN_POINT('Ctrl Pts',(-84.1022301427682,2.286217460299,-4.43812675963685));
#41058=CARTESIAN_POINT('Ctrl Pts',(-84.1417408425183,1.51060571371853,-4.68804815491584));
#41059=CARTESIAN_POINT('Ctrl Pts',(-84.1812515422683,0.734993967138068,
-4.93796955019483));
#41060=CARTESIAN_POINT('Ctrl Pts',(-84.2207622420183,-0.103968328767144,
-4.99128740877481));
#41061=CARTESIAN_POINT('Ctrl Pts',(-84.2602729417683,-0.90497838009561,
-4.84156372019293));
#41062=CARTESIAN_POINT('Ctrl Pts',(-84.2997836415183,-1.70598843142406,
-4.69184003161104));
#41063=CARTESIAN_POINT('Ctrl Pts',(-84.3392943412683,-2.46904623817577,
-4.33907479586728));
#41064=CARTESIAN_POINT('Ctrl Pts',(-84.3788050410184,-3.10201430131225,
-3.82586361486961));
#41065=CARTESIAN_POINT('Ctrl Pts',(-84.4183157407684,-3.73498236444874,
-3.31265243387192));
#41066=CARTESIAN_POINT('Ctrl Pts',(-84.4578264405184,-4.23786068397,-2.6389953076203));
#41067=CARTESIAN_POINT('Ctrl Pts',(-84.4973371402685,-4.54992784365907,
-1.88623480580356));
#41068=CARTESIAN_POINT('Ctrl Pts',(-84.5286109182111,-4.79693736556213,
-1.2904046907523));
#41069=CARTESIAN_POINT('Ctrl Pts',(-84.5598846961538,-4.92440089409629,
-0.645015149412324));
#41070=CARTESIAN_POINT('Ctrl Pts',(-84.5911584740964,-4.92505771915203,
0.000122489528405073));
#41071=CARTESIAN_POINT('Ctrl Pts',(-84.8088415259036,-4.9250542018855,0.000122701850775453));
#41072=CARTESIAN_POINT('Ctrl Pts',(-84.7776223275179,-4.92439841408211,
-0.643890359650401));
#41073=CARTESIAN_POINT('Ctrl Pts',(-84.7464031291322,-4.79739091687878,
-1.28815447712395));
#41074=CARTESIAN_POINT('Ctrl Pts',(-84.7151839307465,-4.55122048505408,
-1.88311371961037));
#41075=CARTESIAN_POINT('Ctrl Pts',(-84.6756732309964,-4.23966969188548,
-2.63608808182635));
#41076=CARTESIAN_POINT('Ctrl Pts',(-84.6361625312464,-3.73725352914504,
-3.31008995804226));
#41077=CARTESIAN_POINT('Ctrl Pts',(-84.5966518314964,-3.10463760866692,
-3.82373515079322));
#41078=CARTESIAN_POINT('Ctrl Pts',(-84.5571411317463,-2.4720216881888,-4.33738034354418));
#41079=CARTESIAN_POINT('Ctrl Pts',(-84.5176304319963,-1.70920600997301,
-4.6906688528302));
#41080=CARTESIAN_POINT('Ctrl Pts',(-84.4781197322463,-0.908298836586612,
-4.84094189265024));
#41081=CARTESIAN_POINT('Ctrl Pts',(-84.4386090324963,-0.107391663200203,
-4.99121493247029));
#41082=CARTESIAN_POINT('Ctrl Pts',(-84.3990983327462,0.731607005356798,
-4.93847250282434));
#41083=CARTESIAN_POINT('Ctrl Pts',(-84.3595876329962,1.50738998326773,-4.68908313243696));
#41084=CARTESIAN_POINT('Ctrl Pts',(-84.3200769332462,2.28317296117865,-4.43969376204958));
#41085=CARTESIAN_POINT('Ctrl Pts',(-84.2805662334961,2.99574024844349,-3.99365745092077));
#41086=CARTESIAN_POINT('Ctrl Pts',(-84.2410555337461,3.55905096170545,-3.40483207170988));
#41087=CARTESIAN_POINT('Ctrl Pts',(-84.2015448339961,4.12236167496742,-2.81600669249899));
#41088=CARTESIAN_POINT('Ctrl Pts',(-84.162034134246,4.53641581422651,-2.084392245206));
#41089=CARTESIAN_POINT('Ctrl Pts',(-84.122523434496,4.75121728151961,-1.29832951454941));
#41090=CARTESIAN_POINT('Ctrl Pts',(-84.0830127347459,4.96601874881271,-0.512266783892823));
#41091=CARTESIAN_POINT('Ctrl Pts',(-84.043502034996,4.98156754413983,0.32824423012738));
#41092=CARTESIAN_POINT('Ctrl Pts',(-84.0039913352459,4.79598618574032,1.12171372941084));
#41093=CARTESIAN_POINT('Ctrl Pts',(-83.964480635496,4.6104048273408,1.9151832286943));
#41094=CARTESIAN_POINT('Ctrl Pts',(-83.9249699357459,4.22369331521466,2.66161121324101));
#41095=CARTESIAN_POINT('Ctrl Pts',(-83.8854592359959,3.68254618713009,3.27086819731618));
#41096=CARTESIAN_POINT('Ctrl Pts',(-83.8459485362458,3.14139905904551,3.88012518139135));
#41097=CARTESIAN_POINT('Ctrl Pts',(-83.8064378364957,2.44581631500251,4.35221116499496));
#41098=CARTESIAN_POINT('Ctrl Pts',(-83.7669271367457,1.67978799329618,4.63012283661445));
#41099=CARTESIAN_POINT('Ctrl Pts',(-83.7274164369957,0.91375967158985,4.90803450823395));
#41100=CARTESIAN_POINT('Ctrl Pts',(-83.6879057372457,0.0772857722201863,
4.99177186786932));
#41101=CARTESIAN_POINT('Ctrl Pts',(-83.6483950374957,-0.728631379147621,
4.87122381931709));
#41102=CARTESIAN_POINT('Ctrl Pts',(-83.6088843377457,-1.53454853051542,
4.75067577076485));
#41103=CARTESIAN_POINT('Ctrl Pts',(-83.5693736379956,-2.30990893388137,
4.42584231402501));
#41104=CARTESIAN_POINT('Ctrl Pts',(-83.5298629382456,-2.96108957957636,
3.9359463520588));
#41105=CARTESIAN_POINT('Ctrl Pts',(-83.4903522384955,-3.61227022527137,
3.44605039009258));
#41106=CARTESIAN_POINT('Ctrl Pts',(-83.4508415387455,-4.13927111329541,
2.79109192289997));
#41107=CARTESIAN_POINT('Ctrl Pts',(-83.4113308389955,-4.47845808201097,
2.05015569950951));
#41108=CARTESIAN_POINT('Ctrl Pts',(-83.3771677346316,-4.77173762108358,
1.40950185923659));
#41109=CARTESIAN_POINT('Ctrl Pts',(-83.3430046302676,-4.92460232693747,
0.704568692162481));
#41110=CARTESIAN_POINT('Ctrl Pts',(-83.3088415259037,-4.92523661103536,
-9.81287755307904E-5));
#41111=CARTESIAN_POINT('Origin',(-74.75,0.,0.));
#41112=CARTESIAN_POINT('',(-81.5911584740964,-4.92458990475544,-1.34620480526926E-5));
#41113=CARTESIAN_POINT('',(-81.8088415259037,-4.92459025730219,-1.44866882854098E-5));
#41114=CARTESIAN_POINT('',(-74.75,-4.925,-6.03138548580071E-16));
#41115=CARTESIAN_POINT('Ctrl Pts',(-81.5911584740964,-4.92458990475544,
-1.34620480526926E-5));
#41116=CARTESIAN_POINT('Ctrl Pts',(-81.6116279021531,-4.92454933037037,
0.422359563629195));
#41117=CARTESIAN_POINT('Ctrl Pts',(-81.6320973302098,-4.87076599946272,
0.844742733033155));
#41118=CARTESIAN_POINT('Ctrl Pts',(-81.6525667582664,-4.7633665661891,1.25302197955212));
#41119=CARTESIAN_POINT('Ctrl Pts',(-81.6920774580165,-4.55606098101821,
2.04109474244191));
#41120=CARTESIAN_POINT('Ctrl Pts',(-81.7315881577664,-4.14899321709825,
2.77661929238658));
#41121=CARTESIAN_POINT('Ctrl Pts',(-81.7710988575164,-3.5913157834199,3.37078270864319));
#41122=CARTESIAN_POINT('Ctrl Pts',(-81.8106095572665,-3.03363834974155,
3.9649461248998));
#41123=CARTESIAN_POINT('Ctrl Pts',(-81.8501202570166,-2.32535124630482,
4.41774840746836));
#41124=CARTESIAN_POINT('Ctrl Pts',(-81.8896309567666,-1.55197853397958,
4.67451470798793));
#41125=CARTESIAN_POINT('Ctrl Pts',(-81.9291416565166,-0.77860582165434,
4.93128100850749));
#41126=CARTESIAN_POINT('Ctrl Pts',(-81.9686523562666,0.059852499559401,
4.99201132697805));
#41127=CARTESIAN_POINT('Ctrl Pts',(-82.0081630560166,0.862154489560794,
4.84937261522138));
#41128=CARTESIAN_POINT('Ctrl Pts',(-82.0476737557666,1.66445647956217,4.70673390346471));
#41129=CARTESIAN_POINT('Ctrl Pts',(-82.0871844555167,2.43060213835121,4.36072616148081));
#41130=CARTESIAN_POINT('Ctrl Pts',(-82.1266951552668,3.06808111576122,3.85312903913666));
#41131=CARTESIAN_POINT('Ctrl Pts',(-82.1662058550168,3.70556009317124,3.34553191679251));
#41132=CARTESIAN_POINT('Ctrl Pts',(-82.2057165547668,4.21437238920223,2.67634541408811));
#41133=CARTESIAN_POINT('Ctrl Pts',(-82.2452272545168,4.53308007343595,1.9263722830613));
#41134=CARTESIAN_POINT('Ctrl Pts',(-82.2847379542668,4.85178775766967,1.17639915203446));
#41135=CARTESIAN_POINT('Ctrl Pts',(-82.3242486540168,4.98039083010609,0.345639392685209));
#41136=CARTESIAN_POINT('Ctrl Pts',(-82.3637593537669,4.90336076150653,-0.46559463876525));
#41137=CARTESIAN_POINT('Ctrl Pts',(-82.4032700535169,4.82633069290697,-1.27682867021569));
#41138=CARTESIAN_POINT('Ctrl Pts',(-82.442780753267,4.54366748327143,-2.06853697376733));
#41139=CARTESIAN_POINT('Ctrl Pts',(-82.482291453017,4.0895020738937,-2.74512256789163));
#41140=CARTESIAN_POINT('Ctrl Pts',(-82.521802152767,3.63533666451597,-3.42170816201595));
#41141=CARTESIAN_POINT('Ctrl Pts',(-82.5613128525171,3.00966905539604,-3.98317104671292));
#41142=CARTESIAN_POINT('Ctrl Pts',(-82.6008235522671,2.28804719090147,-4.36171585242972));
#41143=CARTESIAN_POINT('Ctrl Pts',(-82.6403342520171,1.56642532640689,-4.74026065814652));
#41144=CARTESIAN_POINT('Ctrl Pts',(-82.6798449517671,0.748849206537666,
-4.93588738488314));
#41145=CARTESIAN_POINT('Ctrl Pts',(-82.7193556515172,-0.0659607070428713,
-4.92497454919873));
#41146=CARTESIAN_POINT('Ctrl Pts',(-82.7588663512672,-0.88077062062342,
-4.91406171351432));
#41147=CARTESIAN_POINT('Ctrl Pts',(-82.7983770510173,-1.69281432791528,
-4.69660931540887));
#41148=CARTESIAN_POINT('Ctrl Pts',(-82.8378877507673,-2.40403939352261,
-4.29887423862577));
#41149=CARTESIAN_POINT('Ctrl Pts',(-82.8773984505173,-3.11526445912993,
-3.90113916184267));
#41150=CARTESIAN_POINT('Ctrl Pts',(-82.9169091502673,-3.72567088305271,
-3.32312140638193));
#41151=CARTESIAN_POINT('Ctrl Pts',(-82.9564198500173,-4.16155347441339,
-2.63461530488356));
#41152=CARTESIAN_POINT('Ctrl Pts',(-82.9959305497674,-4.59743606577406,
-1.94610920338519));
#41153=CARTESIAN_POINT('Ctrl Pts',(-83.0354412495174,-4.85879482457262,
-1.14711475584919));
#41154=CARTESIAN_POINT('Ctrl Pts',(-83.0749519492675,-4.91407127362106,
-0.334108729160355));
#41155=CARTESIAN_POINT('Ctrl Pts',(-83.0803541242105,-4.92162905037208,
-0.222948946780624));
#41156=CARTESIAN_POINT('Ctrl Pts',(-83.0857562991535,-4.92533427468202,
-0.1115272285582));
#41157=CARTESIAN_POINT('Ctrl Pts',(-83.0911584740965,-4.92523349004336,
-9.88184705141837E-5));
#41158=CARTESIAN_POINT('Ctrl Pts',(-83.3088415259037,-4.92523661103536,
-9.81287755307904E-5));
#41159=CARTESIAN_POINT('Ctrl Pts',(-83.3034939305176,-4.92533589635437,
-0.110400547438018));
#41160=CARTESIAN_POINT('Ctrl Pts',(-83.2981463351315,-4.9217052242449,-0.220696440074123));
#41161=CARTESIAN_POINT('Ctrl Pts',(-83.2927987397455,-4.91429927793192,
-0.330738252215514));
#41162=CARTESIAN_POINT('Ctrl Pts',(-83.2532880399954,-4.85958045573022,
-1.14378200096181));
#41163=CARTESIAN_POINT('Ctrl Pts',(-83.2137773402453,-4.59876976191972,
-1.94295551886606));
#41164=CARTESIAN_POINT('Ctrl Pts',(-83.1742666404953,-4.1633594960845,-2.63176041670279));
#41165=CARTESIAN_POINT('Ctrl Pts',(-83.1347559407453,-3.72794923024929,
-3.32056531453952));
#41166=CARTESIAN_POINT('Ctrl Pts',(-83.0952452409953,-3.11793939238936,
-3.89900159230872));
#41167=CARTESIAN_POINT('Ctrl Pts',(-83.0557345412453,-2.40698728651493,
-4.29722438175111));
#41168=CARTESIAN_POINT('Ctrl Pts',(-83.0162238414952,-1.69603518064051,
-4.69544717119349));
#41169=CARTESIAN_POINT('Ctrl Pts',(-82.9767131417452,-0.884140806751607,
-4.91345647230907));
#41170=CARTESIAN_POINT('Ctrl Pts',(-82.9372024419952,-0.0693385685744247,
-4.92492815657942));
#41171=CARTESIAN_POINT('Ctrl Pts',(-82.8976917422451,0.74546366960277,-4.93639984084977));
#41172=CARTESIAN_POINT('Ctrl Pts',(-82.858181042495,1.56317377206823,-4.74133390827489));
#41173=CARTESIAN_POINT('Ctrl Pts',(-82.818670342745,2.2850550990641,-4.36328412767286));
#41174=CARTESIAN_POINT('Ctrl Pts',(-82.779159642995,3.00693642605996,-3.98523434707082));
#41175=CARTESIAN_POINT('Ctrl Pts',(-82.739648943245,3.63298897758623,-3.42420071844163));
#41176=CARTESIAN_POINT('Ctrl Pts',(-82.700138243495,4.0876183283531,-2.74792677964179));
#41177=CARTESIAN_POINT('Ctrl Pts',(-82.660627543745,4.54224767911996,-2.07165284084196));
#41178=CARTESIAN_POINT('Ctrl Pts',(-82.6211168439949,4.82545382912743,-1.28013859187147));
#41179=CARTESIAN_POINT('Ctrl Pts',(-82.5816061442449,4.90304027826355,-0.468957582608441));
#41180=CARTESIAN_POINT('Ctrl Pts',(-82.5420954444948,4.98062672739968,0.342223426654603));
#41181=CARTESIAN_POINT('Ctrl Pts',(-82.5025847447448,4.85259347566446,1.17307119621018));
#41182=CARTESIAN_POINT('Ctrl Pts',(-82.4630740449948,4.53440024773965,1.92326274280435));
#41183=CARTESIAN_POINT('Ctrl Pts',(-82.4235633452448,4.21620701981484,2.67345428939852));
#41184=CARTESIAN_POINT('Ctrl Pts',(-82.3840526454948,3.70785381570044,3.34298961303128));
#41185=CARTESIAN_POINT('Ctrl Pts',(-82.3445419457448,3.07072313150732,3.85102384232903));
#41186=CARTESIAN_POINT('Ctrl Pts',(-82.3050312459947,2.43359244731419,4.35905807162678));
#41187=CARTESIAN_POINT('Ctrl Pts',(-82.2655205462446,1.66768428304235,4.70559120658953));
#41188=CARTESIAN_POINT('Ctrl Pts',(-82.2260098464946,0.865480311934301,
4.84878015734007));
#41189=CARTESIAN_POINT('Ctrl Pts',(-82.1864991467446,0.0632763408262584,
4.9919691080906));
#41190=CARTESIAN_POINT('Ctrl Pts',(-82.1469884469946,-0.775223437117998,
4.93181387462891));
#41191=CARTESIAN_POINT('Ctrl Pts',(-82.1074777472446,-1.54877207599144,
4.67557806492309));
#41192=CARTESIAN_POINT('Ctrl Pts',(-82.0679670474946,-2.32232071486487,
4.41934225521726));
#41193=CARTESIAN_POINT('Ctrl Pts',(-82.0284563477445,-3.0309182146675,3.9670258692673));
#41194=CARTESIAN_POINT('Ctrl Pts',(-81.9889456479944,-3.58900303487245,
3.37324508451981));
#41195=CARTESIAN_POINT('Ctrl Pts',(-81.9494349482444,-4.14708785507741,
2.7794642997723));
#41196=CARTESIAN_POINT('Ctrl Pts',(-81.9099242484944,-4.55465999568467,
2.04421911622726));
#41197=CARTESIAN_POINT('Ctrl Pts',(-81.8704135487444,-4.76250604536285,
1.25628872176862));
#41198=CARTESIAN_POINT('Ctrl Pts',(-81.8498895411308,-4.87047259450106,
0.846994795891583));
#41199=CARTESIAN_POINT('Ctrl Pts',(-81.8293655335172,-4.92454647447177,
0.423484667070903));
#41200=CARTESIAN_POINT('Ctrl Pts',(-81.8088415259037,-4.92459025730219,
-1.44866882854098E-5));
#41201=CARTESIAN_POINT('Origin',(-74.75,0.,0.));
#41202=CARTESIAN_POINT('',(-80.0911584740964,-4.92514750914162,0.000113799890342631));
#41203=CARTESIAN_POINT('',(-80.3088415259036,-4.92514409493932,0.00011425152402452));
#41204=CARTESIAN_POINT('',(-74.75,-4.925,-6.03138548580071E-16));
#41205=CARTESIAN_POINT('Ctrl Pts',(-80.0911584740964,-4.92514750914162,
0.000113799890342631));
#41206=CARTESIAN_POINT('Ctrl Pts',(-80.0979888054027,-4.92528677249564,
0.141007302869867));
#41207=CARTESIAN_POINT('Ctrl Pts',(-80.104819136709,-4.91936056283244,0.281889128591955));
#41208=CARTESIAN_POINT('Ctrl Pts',(-80.1116494680152,-4.90728407783657,
0.42224176076328));
#41209=CARTESIAN_POINT('Ctrl Pts',(-80.1511601677652,-4.83742650412431,
1.23412488329213));
#41210=CARTESIAN_POINT('Ctrl Pts',(-80.1906708675153,-4.56177125654089,
2.02830037553067));
#41211=CARTESIAN_POINT('Ctrl Pts',(-80.2301815672654,-4.1136030808575,2.70887334851438));
#41212=CARTESIAN_POINT('Ctrl Pts',(-80.2696922670154,-3.6654349051741,3.3894463214981));
#41213=CARTESIAN_POINT('Ctrl Pts',(-80.3092029667654,-3.04475380139071,
3.95641677522698));
#41214=CARTESIAN_POINT('Ctrl Pts',(-80.3487136665154,-2.32650560467001,
4.34132431368209));
#41215=CARTESIAN_POINT('Ctrl Pts',(-80.3882243662655,-1.60825740794929,
4.72623185213721));
#41216=CARTESIAN_POINT('Ctrl Pts',(-80.4277350660155,-0.792442118291283,
4.92907647531854));
#41217=CARTESIAN_POINT('Ctrl Pts',(-80.4672457657655,0.0224324188948811,
4.92536515516476));
#41218=CARTESIAN_POINT('Ctrl Pts',(-80.5067564655156,0.837306956081022,
4.92165383501097));
#41219=CARTESIAN_POINT('Ctrl Pts',(-80.5462671652656,1.65124074079532,4.71138657152206));
#41220=CARTESIAN_POINT('Ctrl Pts',(-80.5857778650156,2.36595311508063,4.31995265973708));
#41221=CARTESIAN_POINT('Ctrl Pts',(-80.6252885647656,3.08066548936595,3.92851874795209));
#41222=CARTESIAN_POINT('Ctrl Pts',(-80.6647992645157,3.69615645322232,3.35591818787104));
#41223=CARTESIAN_POINT('Ctrl Pts',(-80.7043099642657,4.13810686911053,2.67129119808172));
#41224=CARTESIAN_POINT('Ctrl Pts',(-80.7438206640157,4.58005728499876,1.98666420829237));
#41225=CARTESIAN_POINT('Ctrl Pts',(-80.7833313637658,4.84846715291882,1.19001078879474));
#41226=CARTESIAN_POINT('Ctrl Pts',(-80.8228420635158,4.91092659025283,0.377525032648988));
#41227=CARTESIAN_POINT('Ctrl Pts',(-80.8623527632658,4.97338602758685,-0.434960723496752));
#41228=CARTESIAN_POINT('Ctrl Pts',(-80.9018634630158,4.82989503433481,-1.26327881629061));
#41229=CARTESIAN_POINT('Ctrl Pts',(-80.9413741627658,4.49777982239817,-2.0074117152086));
#41230=CARTESIAN_POINT('Ctrl Pts',(-80.9808848625159,4.16566461046152,-2.75154461412658));
#41231=CARTESIAN_POINT('Ctrl Pts',(-81.0203955622659,3.64492517984028,-3.41149231916869));
#41232=CARTESIAN_POINT('Ctrl Pts',(-81.059906262016,2.9984396353957,-3.90756764215502));
#41233=CARTESIAN_POINT('Ctrl Pts',(-81.099416961766,2.35195409095114,-4.40364296514134));
#41234=CARTESIAN_POINT('Ctrl Pts',(-81.138927661516,1.57972243268324,-4.7358459060719));
#41235=CARTESIAN_POINT('Ctrl Pts',(-81.178438361266,0.774989881388653,-4.86406371348835));
#41236=CARTESIAN_POINT('Ctrl Pts',(-81.2179490610161,-0.0297426699059256,
-4.99228152090479));
#41237=CARTESIAN_POINT('Ctrl Pts',(-81.2574597607661,-0.8669761142272,-4.91651419480714));
#41238=CARTESIAN_POINT('Ctrl Pts',(-81.2969704605161,-1.63561641258026,
-4.64591046793058));
#41239=CARTESIAN_POINT('Ctrl Pts',(-81.3364811602662,-2.40425671093334,
-4.37530674105401));
#41240=CARTESIAN_POINT('Ctrl Pts',(-81.3759918600162,-3.1043038633182,-3.90986661339851));
#41241=CARTESIAN_POINT('Ctrl Pts',(-81.4155025597662,-3.65122876426073,
-3.30579092444817));
#41242=CARTESIAN_POINT('Ctrl Pts',(-81.4550132595162,-4.19815366520325,
-2.70171523549784));
#41243=CARTESIAN_POINT('Ctrl Pts',(-81.4945239592662,-4.59195631470344,
-1.95900398525268));
#41244=CARTESIAN_POINT('Ctrl Pts',(-81.5340346590163,-4.78508593624262,
-1.16733787221264));
#41245=CARTESIAN_POINT('Ctrl Pts',(-81.5530759307097,-4.87816030898299,
-0.78581262350264));
#41246=CARTESIAN_POINT('Ctrl Pts',(-81.572117202403,-4.924627648257,-0.392917431597961));
#41247=CARTESIAN_POINT('Ctrl Pts',(-81.5911584740964,-4.92458990475544,
-1.34620480526926E-5));
#41248=CARTESIAN_POINT('Ctrl Pts',(-81.8088415259037,-4.92459025730219,
-1.44866882854098E-5));
#41249=CARTESIAN_POINT('Ctrl Pts',(-81.7898548337672,-4.92463076065503,
-0.391792164998725));
#41250=CARTESIAN_POINT('Ctrl Pts',(-81.7708681416308,-4.8784320938656,-0.783560450808273));
#41251=CARTESIAN_POINT('Ctrl Pts',(-81.7518814494943,-4.78588545501263,
-1.16405566707921));
#41252=CARTESIAN_POINT('Ctrl Pts',(-81.7123707497443,-4.59329885623518,
-1.95585405609618));
#41253=CARTESIAN_POINT('Ctrl Pts',(-81.6728600499942,-4.20000569993118,
-2.69883522875792));
#41254=CARTESIAN_POINT('Ctrl Pts',(-81.6333493502442,-3.65349524247176,
-3.30328589404503));
#41255=CARTESIAN_POINT('Ctrl Pts',(-81.5938386504941,-3.10698478501233,
-3.90773655933216));
#41256=CARTESIAN_POINT('Ctrl Pts',(-81.5543279507441,-2.40725702639747,
-4.37365671724465));
#41257=CARTESIAN_POINT('Ctrl Pts',(-81.5148172509941,-1.63880250602815,
-4.64478756573394));
#41258=CARTESIAN_POINT('Ctrl Pts',(-81.4753065512441,-0.87034798565884,
-4.91591841422321));
#41259=CARTESIAN_POINT('Ctrl Pts',(-81.4357958514941,-0.0331667035350426,
-4.99225995328928));
#41260=CARTESIAN_POINT('Ctrl Pts',(-81.3962851517441,0.771653599815262,
-4.86459411528371));
#41261=CARTESIAN_POINT('Ctrl Pts',(-81.356774451994,1.57647390316558,-4.73692827727813));
#41262=CARTESIAN_POINT('Ctrl Pts',(-81.3172637522439,2.34893322774243,-4.40525506220092));
#41263=CARTESIAN_POINT('Ctrl Pts',(-81.2777530524939,2.9957588625589,-3.90962325831537));
#41264=CARTESIAN_POINT('Ctrl Pts',(-81.2382423527439,3.64258449737536,-3.41399145442983));
#41265=CARTESIAN_POINT('Ctrl Pts',(-81.1987316529939,4.16377644243144,-2.75440106173597));
#41266=CARTESIAN_POINT('Ctrl Pts',(-81.1592209532439,4.49640195277443,-2.01049612375826));
#41267=CARTESIAN_POINT('Ctrl Pts',(-81.1197102534938,4.82902746311742,-1.26659118578055));
#41268=CARTESIAN_POINT('Ctrl Pts',(-81.0801995537438,4.97308653874732,-0.438371702519009));
#41269=CARTESIAN_POINT('Ctrl Pts',(-81.0406888539937,4.91118437310442,0.374156702379712));
#41270=CARTESIAN_POINT('Ctrl Pts',(-81.0011781542437,4.84928220746151,1.18668510727843));
#41271=CARTESIAN_POINT('Ctrl Pts',(-80.9616674544937,4.5814188005458,1.98352243381432));
#41272=CARTESIAN_POINT('Ctrl Pts',(-80.9221567547437,4.13993805104853,2.66845238256957));
#41273=CARTESIAN_POINT('Ctrl Pts',(-80.8826460549936,3.69845730155124,3.35338233132484));
#41274=CARTESIAN_POINT('Ctrl Pts',(-80.8431353552436,3.08335920947238,3.92640490229945));
#41275=CARTESIAN_POINT('Ctrl Pts',(-80.8036246554936,2.36891547397553,4.31832892004766));
#41276=CARTESIAN_POINT('Ctrl Pts',(-80.7641139557436,1.65447173847872,4.71025293779585));
#41277=CARTESIAN_POINT('Ctrl Pts',(-80.7246032559935,0.840682359563916,
4.92107840231764));
#41278=CARTESIAN_POINT('Ctrl Pts',(-80.6850925562435,0.0258105585151022,
4.92534861706558));
#41279=CARTESIAN_POINT('Ctrl Pts',(-80.6455818564935,-0.789061242533735,
4.92961883181351));
#41280=CARTESIAN_POINT('Ctrl Pts',(-80.6060711567434,-1.6050154657166,4.72733379678758));
#41281=CARTESIAN_POINT('Ctrl Pts',(-80.5665604569934,-2.32352748971546,
4.34291897104901));
#41282=CARTESIAN_POINT('Ctrl Pts',(-80.5270497572434,-3.04203951371433,
3.95850414531044));
#41283=CARTESIAN_POINT('Ctrl Pts',(-80.4875390574934,-3.66310933852919,
3.39195952885925));
#41284=CARTESIAN_POINT('Ctrl Pts',(-80.4480283577434,-4.11174419181654,
2.71169409882889));
#41285=CARTESIAN_POINT('Ctrl Pts',(-80.4085176579933,-4.56037904510389,
2.03142866879854));
#41286=CARTESIAN_POINT('Ctrl Pts',(-80.3690069582432,-4.83657892686373,
1.23744242518903));
#41287=CARTESIAN_POINT('Ctrl Pts',(-80.3294962584932,-4.90699332797998,
0.425607405622822));
#41288=CARTESIAN_POINT('Ctrl Pts',(-80.32261134763,-4.91926334289337,0.284141631017383));
#41289=CARTESIAN_POINT('Ctrl Pts',(-80.3157264367668,-4.92528476922512,
0.142133885922626));
#41290=CARTESIAN_POINT('Ctrl Pts',(-80.3088415259036,-4.92514409493932,
0.00011425152402452));
#41291=CARTESIAN_POINT('Origin',(-74.75,0.,0.));
#41292=CARTESIAN_POINT('',(-78.5911584740964,-4.92514886808152,-0.000113620830927696));
#41293=CARTESIAN_POINT('',(-78.8088415259036,-4.92515227384714,-0.000113155077916571));
#41294=CARTESIAN_POINT('',(-74.75,-4.925,-6.03138548580071E-16));
#41295=CARTESIAN_POINT('Ctrl Pts',(-78.5911584740964,-4.92514886808152,
-0.000113620830927696));
#41296=CARTESIAN_POINT('Ctrl Pts',(-78.6238604084024,-4.92448268450825,
0.674449036085999));
#41297=CARTESIAN_POINT('Ctrl Pts',(-78.6565623427083,-4.78477403277793,
1.3492791421555));
#41298=CARTESIAN_POINT('Ctrl Pts',(-78.6892642770142,-4.51534517405622,
1.96758304872409));
#41299=CARTESIAN_POINT('Ctrl Pts',(-78.7287749767642,-4.18981939196155,
2.71462203969505));
#41300=CARTESIAN_POINT('Ctrl Pts',(-78.7682856765143,-3.67493276089278,
3.37914613668745));
#41301=CARTESIAN_POINT('Ctrl Pts',(-78.8077963762643,-3.03285665751499,
3.88091556574396));
#41302=CARTESIAN_POINT('Ctrl Pts',(-78.8473070760143,-2.39078055413719,
4.38268499480047));
#41303=CARTESIAN_POINT('Ctrl Pts',(-78.8868177757644,-1.62151497845036,
4.72169975592108));
#41304=CARTESIAN_POINT('Ctrl Pts',(-78.9263284755144,-0.817947011417411,
4.85702458424017));
#41305=CARTESIAN_POINT('Ctrl Pts',(-78.9658391752644,-0.014379044384451,
4.99234941255926));
#41306=CARTESIAN_POINT('Ctrl Pts',(-79.0053498750145,0.823491313994628,
4.92398430807683));
#41307=CARTESIAN_POINT('Ctrl Pts',(-79.0448605747645,1.59449312272436,4.66018420284231));
#41308=CARTESIAN_POINT('Ctrl Pts',(-79.0843712745145,2.36549493145408,4.39638409760781));
#41309=CARTESIAN_POINT('Ctrl Pts',(-79.1238819742645,3.06962819053445,3.93714899162124));
#41310=CARTESIAN_POINT('Ctrl Pts',(-79.1633926740146,3.62187040442806,3.33793048168948));
#41311=CARTESIAN_POINT('Ctrl Pts',(-79.2029033737646,4.17411261832166,2.73871197175773));
#41312=CARTESIAN_POINT('Ctrl Pts',(-79.2424140735147,4.5744637870285,1.99951005788078));
#41313=CARTESIAN_POINT('Ctrl Pts',(-79.2819247732647,4.7745824161603,1.20958169434623));
#41314=CARTESIAN_POINT('Ctrl Pts',(-79.3214354730147,4.9747010452921,0.41965333081168));
#41315=CARTESIAN_POINT('Ctrl Pts',(-79.3609461727647,4.97458713484887,-0.421001482380465));
#41316=CARTESIAN_POINT('Ctrl Pts',(-79.4004568725147,4.77425443877746,-1.2108755838017));
#41317=CARTESIAN_POINT('Ctrl Pts',(-79.4399675722647,4.57392174270606,-2.00074968522294));
#41318=CARTESIAN_POINT('Ctrl Pts',(-79.4794782720148,4.17337026100648,-2.73984307487328));
#41319=CARTESIAN_POINT('Ctrl Pts',(-79.5189889717648,3.62096567661331,-3.33891190266436));
#41320=CARTESIAN_POINT('Ctrl Pts',(-79.5584996715148,3.06856109222011,-3.93798073045547));
#41321=CARTESIAN_POINT('Ctrl Pts',(-79.5980103712648,2.36430340513331,-4.39702499638732));
#41322=CARTESIAN_POINT('Ctrl Pts',(-79.6375210710149,1.59323013322142,-4.66061614679244));
#41323=CARTESIAN_POINT('Ctrl Pts',(-79.677031770765,0.822156861309541,-4.92420729719755));
#41324=CARTESIAN_POINT('Ctrl Pts',(-79.716542470515,-0.0157319954274157,
-4.99234533207592));
#41325=CARTESIAN_POINT('Ctrl Pts',(-79.756053170265,-0.819263258373394,
-4.85680273828705));
#41326=CARTESIAN_POINT('Ctrl Pts',(-79.7955638700151,-1.62279452131937,
-4.72126014449818));
#41327=CARTESIAN_POINT('Ctrl Pts',(-79.835074569765,-2.39196819047438,-4.38203692204205));
#41328=CARTESIAN_POINT('Ctrl Pts',(-79.8745852695151,-3.03390829031882,
-3.88009350545033));
#41329=CARTESIAN_POINT('Ctrl Pts',(-79.9140959692651,-3.67584839016326,
-3.37815008885861));
#41330=CARTESIAN_POINT('Ctrl Pts',(-79.9536066690152,-4.19055492069714,
-2.71348647813129));
#41331=CARTESIAN_POINT('Ctrl Pts',(-79.9931173687652,-4.51587823604353,
-1.96635929635804));
#41332=CARTESIAN_POINT('Ctrl Pts',(-80.025797737209,-4.78496194947119,-1.34839019611011));
#41333=CARTESIAN_POINT('Ctrl Pts',(-80.0584781056527,-4.92448119040597,
-0.674004538186427));
#41334=CARTESIAN_POINT('Ctrl Pts',(-80.0911584740964,-4.92514750914162,
0.000113799890342631));
#41335=CARTESIAN_POINT('Ctrl Pts',(-80.3088415259036,-4.92514409493932,
0.00011425152402452));
#41336=CARTESIAN_POINT('Ctrl Pts',(-80.2762157370168,-4.92447747635248,
-0.672879589897553));
#41337=CARTESIAN_POINT('Ctrl Pts',(-80.24358994813,-4.78543695671404,-1.34614041322281));
#41338=CARTESIAN_POINT('Ctrl Pts',(-80.2109641592432,-4.51722584013875,
-1.96326154491532));
#41339=CARTESIAN_POINT('Ctrl Pts',(-80.1714534594932,-4.19241503070861,
-2.71061168036438));
#41340=CARTESIAN_POINT('Ctrl Pts',(-80.1319427597431,-3.67816449137567,
-3.37562815573959));
#41341=CARTESIAN_POINT('Ctrl Pts',(-80.0924320599931,-3.03656880809882,
-3.87801174034342));
#41342=CARTESIAN_POINT('Ctrl Pts',(-80.052921360243,-2.39497312482196,-4.38039532494726));
#41343=CARTESIAN_POINT('Ctrl Pts',(-80.013410660493,-1.62603229760119,-4.72014601877972));
#41344=CARTESIAN_POINT('Ctrl Pts',(-79.9738999607429,-0.822594186851031,
-4.85623969634145));
#41345=CARTESIAN_POINT('Ctrl Pts',(-79.9343892609929,-0.0191560761008687,
-4.99233337390319));
#41346=CARTESIAN_POINT('Ctrl Pts',(-79.894878561243,0.818779318178687,-4.9247700351942));
#41347=CARTESIAN_POINT('Ctrl Pts',(-79.8553678614929,1.59003319812982,-4.66170780008762));
#41348=CARTESIAN_POINT('Ctrl Pts',(-79.8158571617429,2.36128707808095,-4.39864556498104));
#41349=CARTESIAN_POINT('Ctrl Pts',(-79.7763464619928,3.06585944370365,-3.94008443347687));
#41350=CARTESIAN_POINT('Ctrl Pts',(-79.7368357622428,3.61867478028739,-3.3413946218741));
#41351=CARTESIAN_POINT('Ctrl Pts',(-79.6973250624928,4.17149011687114,-2.74270481027132));
#41352=CARTESIAN_POINT('Ctrl Pts',(-79.6578143627428,4.57254842441591,-2.00388631856993));
#41353=CARTESIAN_POINT('Ctrl Pts',(-79.6183036629927,4.77342282216329,-1.2141498035192));
#41354=CARTESIAN_POINT('Ctrl Pts',(-79.5787929632427,4.97429721991067,-0.424413288468484));
#41355=CARTESIAN_POINT('Ctrl Pts',(-79.5392822634927,4.97498770786068,0.41624124993158));
#41356=CARTESIAN_POINT('Ctrl Pts',(-79.4997715637427,4.77541091114282,1.2063066833617));
#41357=CARTESIAN_POINT('Ctrl Pts',(-79.4602608639926,4.57583411442495,1.99637211679183));
#41358=CARTESIAN_POINT('Ctrl Pts',(-79.4207501642425,4.17599003303919,2.73584844525202));
#41359=CARTESIAN_POINT('Ctrl Pts',(-79.3812394644925,3.62415893273268,3.3354455796599));
#41360=CARTESIAN_POINT('Ctrl Pts',(-79.3417287647425,3.07232783242618,3.93504271406778));
#41361=CARTESIAN_POINT('Ctrl Pts',(-79.3022180649925,2.36850971319893,4.39476065442336));
#41362=CARTESIAN_POINT('Ctrl Pts',(-79.2627073652425,1.5976890161471,4.65908950247587));
#41363=CARTESIAN_POINT('Ctrl Pts',(-79.2231966654925,0.826868319095288,
4.92341835052838));
#41364=CARTESIAN_POINT('Ctrl Pts',(-79.1836859657424,-0.0109549557811001,
4.99235810627783));
#41365=CARTESIAN_POINT('Ctrl Pts',(-79.1441752659924,-0.814615548646616,
4.85758445042045));
#41366=CARTESIAN_POINT('Ctrl Pts',(-79.1046645662423,-1.61827614151215,
4.72281079456307));
#41367=CARTESIAN_POINT('Ctrl Pts',(-79.0651538664923,-2.38777405236682,
4.38432372709884));
#41368=CARTESIAN_POINT('Ctrl Pts',(-79.0256431667423,-3.0301941544924,3.88299479390851));
#41369=CARTESIAN_POINT('Ctrl Pts',(-78.9861324669923,-3.67261425661798,
3.38166586071818));
#41370=CARTESIAN_POINT('Ctrl Pts',(-78.9466217672422,-4.18795655001448,
2.71749506180175));
#41371=CARTESIAN_POINT('Ctrl Pts',(-78.9071110674922,-4.5139946213317,1.97067951353778));
#41372=CARTESIAN_POINT('Ctrl Pts',(-78.8743545536294,-4.78429787261529,
1.35152890333658));
#41373=CARTESIAN_POINT('Ctrl Pts',(-78.8415980397665,-4.92448647070407,
0.675573998008652));
#41374=CARTESIAN_POINT('Ctrl Pts',(-78.8088415259036,-4.92515227384714,
-0.000113155077916571));
#41375=CARTESIAN_POINT('Origin',(-74.75,0.,0.));
#41376=CARTESIAN_POINT('',(-77.0911584740964,-4.92453797299891,2.34045202216906E-5));
#41377=CARTESIAN_POINT('',(-77.3088415259036,-4.92459132837391,1.46844578195527E-5));
#41378=CARTESIAN_POINT('',(-74.75,-4.925,-6.03138548580071E-16));
#41379=CARTESIAN_POINT('Ctrl Pts',(-77.0911584740964,-4.9245376769549,2.34195166788631E-5));
#41380=CARTESIAN_POINT('Ctrl Pts',(-77.110221311652,-4.92460351006797,0.393366610892078));
#41381=CARTESIAN_POINT('Ctrl Pts',(-77.1292841492075,-4.87806963749634,
0.786699148933148));
#41382=CARTESIAN_POINT('Ctrl Pts',(-77.1483469867631,-4.78480271173096,
1.1686279851341));
#41383=CARTESIAN_POINT('Ctrl Pts',(-77.1878576865131,-4.59149248234959,
1.96023498115633));
#41384=CARTESIAN_POINT('Ctrl Pts',(-77.2273683862632,-4.1974216441505,2.702852793555));
#41385=CARTESIAN_POINT('Ctrl Pts',(-77.2668790860132,-3.65031620861451,
3.30678359219156));
#41386=CARTESIAN_POINT('Ctrl Pts',(-77.3063897857632,-3.10321077307853,
3.9107143908281));
#41387=CARTESIAN_POINT('Ctrl Pts',(-77.3459004855133,-2.40307074020566,
4.37595817570254));
#41388=CARTESIAN_POINT('Ctrl Pts',(-77.3854111852633,-1.63436550044067,
4.64635192368507));
#41389=CARTESIAN_POINT('Ctrl Pts',(-77.4249218850133,-0.865660260675676,
4.9167456716676));
#41390=CARTESIAN_POINT('Ctrl Pts',(-77.4644325847633,-0.0283898140185719,
4.99228938275823));
#41391=CARTESIAN_POINT('Ctrl Pts',(-77.5039432845133,0.776312113685768,
4.86385431998651));
#41392=CARTESIAN_POINT('Ctrl Pts',(-77.5434539842634,1.58101404139012,4.73541925721478));
#41393=CARTESIAN_POINT('Ctrl Pts',(-77.5829646840134,2.3531474501417,4.40300542058071));
#41394=CARTESIAN_POINT('Ctrl Pts',(-77.6224753837634,2.99949646977121,3.90675450502815));
#41395=CARTESIAN_POINT('Ctrl Pts',(-77.6619860835135,3.64584548940072,3.41050358947558));
#41396=CARTESIAN_POINT('Ctrl Pts',(-77.7014967832635,4.16641011990815,2.75041559500453));
#41397=CARTESIAN_POINT('Ctrl Pts',(-77.7410074830135,4.49832468022958,2.006192922343));
#41398=CARTESIAN_POINT('Ctrl Pts',(-77.7805181827635,4.83023924055099,1.2619702496815));
#41399=CARTESIAN_POINT('Ctrl Pts',(-77.8200288825136,4.9735037306864,0.433612898829542));
#41400=CARTESIAN_POINT('Ctrl Pts',(-77.8595395822637,4.91082359979706,-0.378856001820336));
#41401=CARTESIAN_POINT('Ctrl Pts',(-77.8990502820137,4.84814346890771,-1.19132490247023));
#41402=CARTESIAN_POINT('Ctrl Pts',(-77.9385609817636,4.57951871699359,-1.98790535291803));
#41403=CARTESIAN_POINT('Ctrl Pts',(-77.9780716815137,4.13738303272748,-2.67241249674817));
#41404=CARTESIAN_POINT('Ctrl Pts',(-78.0175823812637,3.69524734846136,-3.35691964057832));
#41405=CARTESIAN_POINT('Ctrl Pts',(-78.0570930810138,3.07960073184324,-3.92935347779079));
#41406=CARTESIAN_POINT('Ctrl Pts',(-78.0966037807638,2.36478217805084,-4.32059370978506));
#41407=CARTESIAN_POINT('Ctrl Pts',(-78.1361144805139,1.64996362425846,-4.71183394177931));
#41408=CARTESIAN_POINT('Ctrl Pts',(-78.1756251802638,0.835973133291798,
-4.92188056855537));
#41409=CARTESIAN_POINT('Ctrl Pts',(-78.2151358800138,0.0210976824875499,
-4.92537104143333));
#41410=CARTESIAN_POINT('Ctrl Pts',(-78.2546465797639,-0.793777768316698,
-4.92886151431129));
#41411=CARTESIAN_POINT('Ctrl Pts',(-78.2941572795139,-1.60953817895853,
-4.72579583329114));
#41412=CARTESIAN_POINT('Ctrl Pts',(-78.333667979264,-2.32768206849062,-4.34069366654293));
#41413=CARTESIAN_POINT('Ctrl Pts',(-78.373178679014,-3.04582595802271,-3.95559149979471));
#41414=CARTESIAN_POINT('Ctrl Pts',(-78.412689378764,-3.66635332644505,-3.38845284731842));
#41415=CARTESIAN_POINT('Ctrl Pts',(-78.452200078514,-4.11433703191033,-2.70775844063091));
#41416=CARTESIAN_POINT('Ctrl Pts',(-78.4917107782641,-4.56232073737562,
-2.02706403394338));
#41417=CARTESIAN_POINT('Ctrl Pts',(-78.5312214780141,-4.83776077988383,
-1.23281387304462));
#41418=CARTESIAN_POINT('Ctrl Pts',(-78.5707321777641,-4.90739833457764,
-0.420911850120484));
#41419=CARTESIAN_POINT('Ctrl Pts',(-78.5775409432082,-4.91939877443344,
-0.280999105657526));
#41420=CARTESIAN_POINT('Ctrl Pts',(-78.5843497086523,-4.92528757203862,
-0.140562160214772));
#41421=CARTESIAN_POINT('Ctrl Pts',(-78.5911584740964,-4.92514886808152,
-0.000113620830927696));
#41422=CARTESIAN_POINT('Ctrl Pts',(-78.8088415259036,-4.92515227384714,
-0.000113155077916571));
#41423=CARTESIAN_POINT('Ctrl Pts',(-78.8020873400165,-4.92528955824227,
-0.139435570540877));
#41424=CARTESIAN_POINT('Ctrl Pts',(-78.7953331541293,-4.91949491513351,
-0.278746602294923));
#41425=CARTESIAN_POINT('Ctrl Pts',(-78.7885789682421,-4.90768586809107,
-0.417545928509096));
#41426=CARTESIAN_POINT('Ctrl Pts',(-78.7490682684921,-4.83860519429525,
-1.22949552468054));
#41427=CARTESIAN_POINT('Ctrl Pts',(-78.7095575687421,-4.56370999746566,
-2.02393441941193));
#41428=CARTESIAN_POINT('Ctrl Pts',(-78.670046868992,-4.11619324668281,-2.704935921754));
#41429=CARTESIAN_POINT('Ctrl Pts',(-78.630536169242,-3.66867649589997,-3.38593742409605));
#41430=CARTESIAN_POINT('Ctrl Pts',(-78.591025469492,-3.04853819116387,-3.9535015340488));
#41431=CARTESIAN_POINT('Ctrl Pts',(-78.551514769742,-2.33065863049451,-4.33909616636603));
#41432=CARTESIAN_POINT('Ctrl Pts',(-78.5120040699919,-1.61277906982514,
-4.72469079868326));
#41433=CARTESIAN_POINT('Ctrl Pts',(-78.4724933702418,-0.797158253222491,
-4.92831595336498));
#41434=CARTESIAN_POINT('Ctrl Pts',(-78.4329826704918,0.0177194653744605,
-4.92538436820628));
#41435=CARTESIAN_POINT('Ctrl Pts',(-78.3934719707418,0.832597183971412,
-4.92245278304758));
#41436=CARTESIAN_POINT('Ctrl Pts',(-78.3539612709918,1.64673180456268,-4.71296445804845));
#41437=CARTESIAN_POINT('Ctrl Pts',(-78.3144505712418,2.36181840000114,-4.32221460647475));
#41438=CARTESIAN_POINT('Ctrl Pts',(-78.2749398714918,3.0769049954396,-3.93146475490105));
#41439=CARTESIAN_POINT('Ctrl Pts',(-78.2354291717417,3.69294356572525,-3.35945337675278));
#41440=CARTESIAN_POINT('Ctrl Pts',(-78.1959184719917,4.13554888877892,-2.67524960205178));
#41441=CARTESIAN_POINT('Ctrl Pts',(-78.1564077722416,4.57815421183259,-1.9910458273508));
#41442=CARTESIAN_POINT('Ctrl Pts',(-78.1168970724916,4.84732628765426,-1.1946496560971));
#41443=CARTESIAN_POINT('Ctrl Pts',(-78.0773863727416,4.91056312282638,-0.382224010811509));
#41444=CARTESIAN_POINT('Ctrl Pts',(-78.0378756729916,4.9737999579985,0.430201634474102));
#41445=CARTESIAN_POINT('Ctrl Pts',(-77.9983649732415,4.83110155252106,1.2586567537916));
#41446=CARTESIAN_POINT('Ctrl Pts',(-77.9588542734915,4.49969856804995,2.00310705263756));
#41447=CARTESIAN_POINT('Ctrl Pts',(-77.9193435737415,4.16829558357886,2.74755735148348));
#41448=CARTESIAN_POINT('Ctrl Pts',(-77.8798328739914,3.6481880201141,3.40800282985787));
#41449=CARTESIAN_POINT('Ctrl Pts',(-77.8403221742414,3.00217737795472,3.90469663436248));
#41450=CARTESIAN_POINT('Ctrl Pts',(-77.8008114744914,2.35616673579532,4.40139043886709));
#41451=CARTESIAN_POINT('Ctrl Pts',(-77.7613007747414,1.58425301494129,4.73433256950191));
#41452=CARTESIAN_POINT('Ctrl Pts',(-77.7217900749914,0.779643666424622,
4.86332013350593));
#41453=CARTESIAN_POINT('Ctrl Pts',(-77.6822793752413,-0.0249656820920473,
4.99230769750994));
#41454=CARTESIAN_POINT('Ctrl Pts',(-77.6427686754913,-0.86227065827136,
4.91734069488313));
#41455=CARTESIAN_POINT('Ctrl Pts',(-77.6032579757413,-1.6311698355519,4.64747300536884));
#41456=CARTESIAN_POINT('Ctrl Pts',(-77.5637472759912,-2.40006901283244,
4.37760531585456));
#41457=CARTESIAN_POINT('Ctrl Pts',(-77.5242365762412,-3.10056239121421,
3.91283693945278));
#41458=CARTESIAN_POINT('Ctrl Pts',(-77.4847258764912,-3.64806446717552,
3.30928400931355));
#41459=CARTESIAN_POINT('Ctrl Pts',(-77.4452151767411,-4.19556654313682,
2.70573107917432));
#41460=CARTESIAN_POINT('Ctrl Pts',(-77.4057044769911,-4.59007731667766,
1.96339359529763));
#41461=CARTESIAN_POINT('Ctrl Pts',(-77.3661937772411,-4.78396557727188,
1.17191436367405));
#41462=CARTESIAN_POINT('Ctrl Pts',(-77.3470763601286,-4.87777922204265,
0.788953831399374));
#41463=CARTESIAN_POINT('Ctrl Pts',(-77.3279589430161,-4.92462415434814,
0.394488485502017));
#41464=CARTESIAN_POINT('Ctrl Pts',(-77.3088415259036,-4.92459132837391,
1.46844578195527E-5));
#41465=CARTESIAN_POINT('Origin',(-74.75,0.,0.));
#41466=CARTESIAN_POINT('',(-75.5911584740964,-4.93145818296612,0.00170945267300153));
#41467=CARTESIAN_POINT('',(-75.8088415259036,-4.93185981856261,0.00388372659001099));
#41468=CARTESIAN_POINT('',(-74.75,-4.925,-6.03138548580071E-16));
#41469=CARTESIAN_POINT('Ctrl Pts',(-75.5911584740964,-4.93145818296612,
0.00170945267300153));
#41470=CARTESIAN_POINT('Ctrl Pts',(-75.5965822149016,-4.93204081057214,
0.113167419548451));
#41471=CARTESIAN_POINT('Ctrl Pts',(-75.6020059557068,-4.92860871675615,
0.224592305800187));
#41472=CARTESIAN_POINT('Ctrl Pts',(-75.607429696512,-4.92105000563757,0.335738029486276));
#41473=CARTESIAN_POINT('Ctrl Pts',(-75.686451096012,-4.810923074344,1.95507990985986));
#41474=CARTESIAN_POINT('Ctrl Pts',(-75.7654724955121,-3.82483311757502,
3.51516354851337));
#41475=CARTESIAN_POINT('Ctrl Pts',(-75.8444938950122,-2.40735607849465,
4.30649291473166));
#41476=CARTESIAN_POINT('Ctrl Pts',(-75.9235152945122,-0.989879039414278,
5.09782228094995));
#41477=CARTESIAN_POINT('Ctrl Pts',(-76.0025366940123,0.85898508197749,5.12039737473303));
#41478=CARTESIAN_POINT('Ctrl Pts',(-76.0815580935123,2.29413116832581,4.36708108920334));
#41479=CARTESIAN_POINT('Ctrl Pts',(-76.1605794930124,3.72927725467414,3.61376480367365));
#41480=CARTESIAN_POINT('Ctrl Pts',(-76.2396008925124,4.75070530597902,2.08455713883121));
#41481=CARTESIAN_POINT('Ctrl Pts',(-76.3186222920125,4.90865109371366,0.464760615946058));
#41482=CARTESIAN_POINT('Ctrl Pts',(-76.3581329917625,4.98762398758099,-0.345137645496505));
#41483=CARTESIAN_POINT('Ctrl Pts',(-76.3976436915125,4.85072631555575,-1.17768312144974));
#41484=CARTESIAN_POINT('Ctrl Pts',(-76.4371543912626,4.52998832978331,-1.92803440327652));
#41485=CARTESIAN_POINT('Ctrl Pts',(-76.4766650910126,4.20925034401087,-2.6783856851033));
#41486=CARTESIAN_POINT('Ctrl Pts',(-76.5161757907626,3.70467204449123,-3.34654277280362));
#41487=CARTESIAN_POINT('Ctrl Pts',(-76.5556864905126,3.06815643951909,-3.85374200240443));
#41488=CARTESIAN_POINT('Ctrl Pts',(-76.5951971902627,2.43164083454696,-4.36094123200524));
#41489=CARTESIAN_POINT('Ctrl Pts',(-76.6347078900127,1.66318792412234,-4.70718260350654));
#41490=CARTESIAN_POINT('Ctrl Pts',(-76.6742185897627,0.86029094445069,-4.84971500783713));
#41491=CARTESIAN_POINT('Ctrl Pts',(-76.7137292895128,0.0573939647790152,
-4.99224741216772));
#41492=CARTESIAN_POINT('Ctrl Pts',(-76.7532399892629,-0.779947084139697,
-4.93107084932759));
#41493=CARTESIAN_POINT('Ctrl Pts',(-76.7927506890129,-1.5529731345604,-4.67403983231761));
#41494=CARTESIAN_POINT('Ctrl Pts',(-76.8322613887629,-2.3259991849811,-4.41700881530763));
#41495=CARTESIAN_POINT('Ctrl Pts',(-76.8717720885129,-3.03471023690379,
-3.96412334412782));
#41496=CARTESIAN_POINT('Ctrl Pts',(-76.9112827882629,-3.59236424510066,
-3.36983619140984));
#41497=CARTESIAN_POINT('Ctrl Pts',(-76.9507934880129,-4.15001825329752,
-2.77554903869188));
#41498=CARTESIAN_POINT('Ctrl Pts',(-76.990304187763,-4.55661521776857,-2.03986020443576));
#41499=CARTESIAN_POINT('Ctrl Pts',(-77.029814887513,-4.76363888972227,-1.25171769748482));
#41500=CARTESIAN_POINT('Ctrl Pts',(-77.0502627497075,-4.87077927300793,
-0.843832505025608));
#41501=CARTESIAN_POINT('Ctrl Pts',(-77.070710611902,-4.92446706068804,-0.421898413942657));
#41502=CARTESIAN_POINT('Ctrl Pts',(-77.0911584740964,-4.9245376769549,2.34195166788631E-5));
#41503=CARTESIAN_POINT('Ctrl Pts',(-77.3088415259036,-4.92459132837391,
1.46844578195527E-5));
#41504=CARTESIAN_POINT('Ctrl Pts',(-77.2884482432661,-4.9245563116472,-0.420785660613278));
#41505=CARTESIAN_POINT('Ctrl Pts',(-77.2680549606285,-4.87117765087757,
-0.841595627056218));
#41506=CARTESIAN_POINT('Ctrl Pts',(-77.247661677991,-4.76456575302619,-1.24846007914821));
#41507=CARTESIAN_POINT('Ctrl Pts',(-77.208150978241,-4.55801192053866,-2.03673431097644));
#41508=CARTESIAN_POINT('Ctrl Pts',(-77.1686402784909,-4.15163850791598,
-2.77266179526241));
#41509=CARTESIAN_POINT('Ctrl Pts',(-77.1291295787409,-3.59453475390508,
-3.36735158860536));
#41510=CARTESIAN_POINT('Ctrl Pts',(-77.0896188789909,-3.03743099989419,
-3.96204138194831));
#41511=CARTESIAN_POINT('Ctrl Pts',(-77.0501081792409,-2.32959690449509,
-4.41549348434824));
#41512=CARTESIAN_POINT('Ctrl Pts',(-77.0105974794909,-1.55646039394619,
-4.6730137396139));
#41513=CARTESIAN_POINT('Ctrl Pts',(-76.9710867797408,-0.783323883397288,
-4.93053399487957));
#41514=CARTESIAN_POINT('Ctrl Pts',(-76.9315760799908,0.055115042301422,
-4.99212240301097));
#41515=CARTESIAN_POINT('Ctrl Pts',(-76.8920653802408,0.857533325507661,
-4.85022314878024));
#41516=CARTESIAN_POINT('Ctrl Pts',(-76.8525546804907,1.65995160871392,-4.70832389454951));
#41517=CARTESIAN_POINT('Ctrl Pts',(-76.8130439807407,2.42634924942772,-4.36293697795663));
#41518=CARTESIAN_POINT('Ctrl Pts',(-76.7735332809906,3.06435357769784,-3.85600708998388));
#41519=CARTESIAN_POINT('Ctrl Pts',(-76.7340225812406,3.70235790596796,-3.34907720201115));
#41520=CARTESIAN_POINT('Ctrl Pts',(-76.6945118814906,4.21196892179439,-2.68060434265857));
#41521=CARTESIAN_POINT('Ctrl Pts',(-76.6550011817406,4.53131364928107,-1.9308216777245));
#41522=CARTESIAN_POINT('Ctrl Pts',(-76.6154904819906,4.85065837676774,-1.18103901279044));
#41523=CARTESIAN_POINT('Ctrl Pts',(-76.5759797822405,4.97973681591463,-0.349946542274868));
#41524=CARTESIAN_POINT('Ctrl Pts',(-76.5364690824904,4.90364501449345,0.461129615068031));
#41525=CARTESIAN_POINT('Ctrl Pts',(-76.4969583827404,4.82755321307227,1.27220577241095));
#41526=CARTESIAN_POINT('Ctrl Pts',(-76.4574476829904,4.54629117108303,2.06326561658121));
#41527=CARTESIAN_POINT('Ctrl Pts',(-76.4179369832404,4.09244767227833,2.74074969716858));
#41528=CARTESIAN_POINT('Ctrl Pts',(-76.3784262834904,3.63860417347364,3.41823377775594));
#41529=CARTESIAN_POINT('Ctrl Pts',(-76.3389155837403,3.01217921785349,3.9821420947604));
#41530=CARTESIAN_POINT('Ctrl Pts',(-76.2994048839903,2.29156928683899,4.36046055554361));
#41531=CARTESIAN_POINT('Ctrl Pts',(-76.2598941842403,1.57095935582447,4.73877901632683));
#41532=CARTESIAN_POINT('Ctrl Pts',(-76.2203834844902,0.756164449415575,
4.9315076208888));
#41533=CARTESIAN_POINT('Ctrl Pts',(-76.1808727847402,-0.059816786502471,
4.92285971725886));
#41534=CARTESIAN_POINT('Ctrl Pts',(-76.1413620849902,-0.875798022420494,
4.91421181362892));
#41535=CARTESIAN_POINT('Ctrl Pts',(-76.1018513852402,-1.69296558784768,
4.70418740180709));
#41536=CARTESIAN_POINT('Ctrl Pts',(-76.0623406854901,-2.40245776805243,
4.30569922684081));
#41537=CARTESIAN_POINT('Ctrl Pts',(-75.9833192859901,-3.82144212846192,
3.50872287690825));
#41538=CARTESIAN_POINT('Ctrl Pts',(-75.90429788649,-4.80972494798167,1.9578914743979));
#41539=CARTESIAN_POINT('Ctrl Pts',(-75.8252764869899,-4.92120160549743,
0.340887420253297));
#41540=CARTESIAN_POINT('Ctrl Pts',(-75.8197981666278,-4.92892995309229,
0.228785302453847));
#41541=CARTESIAN_POINT('Ctrl Pts',(-75.8143198462657,-4.93244416019434,
0.116365143036017));
#41542=CARTESIAN_POINT('Ctrl Pts',(-75.8088415259036,-4.93185981856261,
0.00388372659001099));
#41543=CARTESIAN_POINT('Origin',(-74.75,0.,0.));
#41544=CARTESIAN_POINT('',(-74.0911584740964,-4.91843222427485,0.00245724012685411));
#41545=CARTESIAN_POINT('',(-74.3088415259036,-4.91847745023605,0.00259239093822753));
#41546=CARTESIAN_POINT('',(-74.75,-4.925,-6.03138548580071E-16));
#41547=CARTESIAN_POINT('Ctrl Pts',(-74.0911584740964,-4.91843222427485,
0.00245724012685411));
#41548=CARTESIAN_POINT('Ctrl Pts',(-74.1224538179012,-4.92156279260847,
0.650146294184244));
#41549=CARTESIAN_POINT('Ctrl Pts',(-74.153749161706,-4.80268279810373,1.29675391287114));
#41550=CARTESIAN_POINT('Ctrl Pts',(-74.1850445055109,-4.55640455625903,
1.89046313642067));
#41551=CARTESIAN_POINT('Ctrl Pts',(-74.264065905011,-3.93454683012746,3.3895913784221));
#41552=CARTESIAN_POINT('Ctrl Pts',(-74.3430873045111,-2.50043215929785,
4.55145368693655));
#41553=CARTESIAN_POINT('Ctrl Pts',(-74.4221087040112,-0.905034099899794,
4.84914491655614));
#41554=CARTESIAN_POINT('Ctrl Pts',(-74.5011301035112,0.690363959498285,
5.14683614617574));
#41555=CARTESIAN_POINT('Ctrl Pts',(-74.5801515030112,2.4470454074648,4.58035629690046));
#41556=CARTESIAN_POINT('Ctrl Pts',(-74.6591729025113,3.56776108938243,3.40663242401753));
#41557=CARTESIAN_POINT('Ctrl Pts',(-74.7381943020113,4.68847677130004,2.23290855113462));
#41558=CARTESIAN_POINT('Ctrl Pts',(-74.8172157015114,5.17322668716877,0.451940654644055));
#41559=CARTESIAN_POINT('Ctrl Pts',(-74.8962371010115,4.80217577389113,-1.12800752674652));
#41560=CARTESIAN_POINT('Ctrl Pts',(-74.9752585005115,4.43112486061349,-2.70795570813711));
#41561=CARTESIAN_POINT('Ctrl Pts',(-75.0542799000116,3.2042731181895,-4.08688417442772));
#41562=CARTESIAN_POINT('Ctrl Pts',(-75.1333012995116,1.67802622625532,-4.63884698329907));
#41563=CARTESIAN_POINT('Ctrl Pts',(-75.2123226990117,0.151779334321143,
-5.19080979217042));
#41564=CARTESIAN_POINT('Ctrl Pts',(-75.2913440985118,-1.6738627071232,-4.91580694362251));
#41565=CARTESIAN_POINT('Ctrl Pts',(-75.3703654980118,-2.96960177493628,
-3.93900545830171));
#41566=CARTESIAN_POINT('Ctrl Pts',(-75.4439631567067,-4.17640603648892,
-3.02924806620143));
#41567=CARTESIAN_POINT('Ctrl Pts',(-75.5175608154016,-4.92355219533978,
-1.51072369993773));
#41568=CARTESIAN_POINT('Ctrl Pts',(-75.5911584740964,-4.93145818296612,
0.00170945267300153));
#41569=CARTESIAN_POINT('Ctrl Pts',(-75.8088415259036,-4.93185981856261,
0.00388372659001099));
#41570=CARTESIAN_POINT('Ctrl Pts',(-75.7352984467657,-4.92401539179933,
-1.50611006063952));
#41571=CARTESIAN_POINT('Ctrl Pts',(-75.6617553676277,-4.1775546932613,-3.02714322807678));
#41572=CARTESIAN_POINT('Ctrl Pts',(-75.5882122884898,-2.97212463234744,
-3.93798622059295));
#41573=CARTESIAN_POINT('Ctrl Pts',(-75.5091908889897,-1.67690050616995,
-4.91667910151568));
#41574=CARTESIAN_POINT('Ctrl Pts',(-75.4301694894897,0.148218241696821,
-5.19088815758227));
#41575=CARTESIAN_POINT('Ctrl Pts',(-75.3511480899896,1.67475699940288,-4.63946497019405));
#41576=CARTESIAN_POINT('Ctrl Pts',(-75.2721266904895,3.20129575710896,-4.08804178280584));
#41577=CARTESIAN_POINT('Ctrl Pts',(-75.1931052909895,4.42925452465434,-2.71098635196282));
#41578=CARTESIAN_POINT('Ctrl Pts',(-75.1140838914894,4.80143977898294,-1.13156518854111));
#41579=CARTESIAN_POINT('Ctrl Pts',(-75.0350624919894,5.17362503331154,0.447855974880574));
#41580=CARTESIAN_POINT('Ctrl Pts',(-74.9560410924893,4.69003677442338,2.22964287088094));
#41581=CARTESIAN_POINT('Ctrl Pts',(-74.8770196929893,3.57008894292872,3.4042977373349));
#41582=CARTESIAN_POINT('Ctrl Pts',(-74.7979982934892,2.45014111143405,4.57895260378886));
#41583=CARTESIAN_POINT('Ctrl Pts',(-74.7189768939892,0.693833707332852,
5.14647544069641));
#41584=CARTESIAN_POINT('Ctrl Pts',(-74.6399554944891,-0.90172743084978,
4.84975223650184));
#41585=CARTESIAN_POINT('Ctrl Pts',(-74.560934094989,-2.49728856903242,4.55302903230727));
#41586=CARTESIAN_POINT('Ctrl Pts',(-74.4819126954889,-3.93210344129651,
3.3920597870106));
#41587=CARTESIAN_POINT('Ctrl Pts',(-74.4028912959889,-4.55505162183579,
1.89350503658887));
#41588=CARTESIAN_POINT('Ctrl Pts',(-74.3715413726271,-4.80219198940474,
1.29898789469625));
#41589=CARTESIAN_POINT('Ctrl Pts',(-74.3401914492653,-4.92155077598789,
0.651337387434103));
#41590=CARTESIAN_POINT('Ctrl Pts',(-74.3088415259036,-4.91847745023605,
0.00259239093822753));
#41591=CARTESIAN_POINT('Origin',(-74.75,0.,0.));
#41592=CARTESIAN_POINT('',(-72.5911584740964,-4.92473478262889,-0.000479420352050008));
#41593=CARTESIAN_POINT('',(-72.8088415259036,-4.92403075528272,-0.00394394407346908));
#41594=CARTESIAN_POINT('',(-74.75,-4.925,-6.03138548580071E-16));
#41595=CARTESIAN_POINT('Ctrl Pts',(-72.5911584740964,-4.92473478262889,
-0.000479420352050008));
#41596=CARTESIAN_POINT('Ctrl Pts',(-72.6088147211509,-4.92488354658816,
0.363652102799084));
#41597=CARTESIAN_POINT('Ctrl Pts',(-72.6264709682053,-4.88500686021711,
0.727870072460014));
#41598=CARTESIAN_POINT('Ctrl Pts',(-72.6441272152598,-4.80481154670615,
1.08333843603181));
#41599=CARTESIAN_POINT('Ctrl Pts',(-72.6836379150098,-4.62535251763178,
1.87879648214977));
#41600=CARTESIAN_POINT('Ctrl Pts',(-72.7231486147599,-4.24399252838692,
2.63043969636934));
#41601=CARTESIAN_POINT('Ctrl Pts',(-72.7626593145099,-3.70793942458222,
3.24285315456735));
#41602=CARTESIAN_POINT('Ctrl Pts',(-72.8021700142599,-3.17188632077752,
3.85526661276537));
#41603=CARTESIAN_POINT('Ctrl Pts',(-72.8416807140099,-2.481140102413,4.32845031494182));
#41604=CARTESIAN_POINT('Ctrl Pts',(-72.88119141376,-1.71677733901996,4.61419402457444));
#41605=CARTESIAN_POINT('Ctrl Pts',(-72.92070211351,-0.952414575626897,4.89993773420706));
#41606=CARTESIAN_POINT('Ctrl Pts',(-72.96021281326,-0.11443526720532,4.99824145129583));
#41607=CARTESIAN_POINT('Ctrl Pts',(-72.9997235130101,0.690951841327282,
4.8819507927587));
#41608=CARTESIAN_POINT('Ctrl Pts',(-73.0787449125101,2.30172605839249,4.64936947568446));
#41609=CARTESIAN_POINT('Ctrl Pts',(-73.1577663120102,3.78213147590179,3.55841065610665));
#41610=CARTESIAN_POINT('Ctrl Pts',(-73.2367877115102,4.46836735735957,2.09000675043046));
#41611=CARTESIAN_POINT('Ctrl Pts',(-73.3158091110103,5.15460323881732,0.621602844754309));
#41612=CARTESIAN_POINT('Ctrl Pts',(-73.3948305105104,5.0466695842236,-1.2242461470202));
#41613=CARTESIAN_POINT('Ctrl Pts',(-73.4738519100104,4.19072380063174,-2.603666364978));
#41614=CARTESIAN_POINT('Ctrl Pts',(-73.5528733095105,3.33477801703989,-3.98308658293581));
#41615=CARTESIAN_POINT('Ctrl Pts',(-73.6318947090105,1.73082010444989,-4.8960780270769));
#41616=CARTESIAN_POINT('Ctrl Pts',(-73.7109161085106,0.10812014196865,-4.93130441337073));
#41617=CARTESIAN_POINT('Ctrl Pts',(-73.7899375080106,-1.51457982051261,
-4.96653079966455));
#41618=CARTESIAN_POINT('Ctrl Pts',(-73.8689589075107,-3.15602183288511,
-4.12399212811109));
#41619=CARTESIAN_POINT('Ctrl Pts',(-73.9479803070108,-4.07194244835461,
-2.78452570459015));
#41620=CARTESIAN_POINT('Ctrl Pts',(-73.995706362706,-4.62512523912847,-1.97553662650135));
#41621=CARTESIAN_POINT('Ctrl Pts',(-74.0434324184012,-4.91365804190512,
-0.985282152029947));
#41622=CARTESIAN_POINT('Ctrl Pts',(-74.0911584740964,-4.91843222427485,
0.00245724012685411));
#41623=CARTESIAN_POINT('Ctrl Pts',(-74.3088415259036,-4.91847745023605,
0.00259239093822753));
#41624=CARTESIAN_POINT('Ctrl Pts',(-74.2611700497653,-4.91380407436992,
-0.983905447139712));
#41625=CARTESIAN_POINT('Ctrl Pts',(-74.213498573627,-4.62603089007891,-1.97293407298634));
#41626=CARTESIAN_POINT('Ctrl Pts',(-74.1658270974888,-4.07396738632402,
-2.78151743232188));
#41627=CARTESIAN_POINT('Ctrl Pts',(-74.0868056979887,-3.15885348145848,
-4.12184489526421));
#41628=CARTESIAN_POINT('Ctrl Pts',(-74.0077842984886,-1.51754418291289,
-4.96635956560206));
#41629=CARTESIAN_POINT('Ctrl Pts',(-73.9287628989886,0.104965517004485,
-4.93181901953187));
#41630=CARTESIAN_POINT('Ctrl Pts',(-73.8497414994885,1.72747521692181,-4.89727847346167));
#41631=CARTESIAN_POINT('Ctrl Pts',(-73.7707200999884,3.33118531821094,-3.98368271098348));
#41632=CARTESIAN_POINT('Ctrl Pts',(-73.6916987004883,4.18850610344658,-2.60569102857425));
#41633=CARTESIAN_POINT('Ctrl Pts',(-73.6126773009883,5.04582688868223,-1.227699346165));
#41634=CARTESIAN_POINT('Ctrl Pts',(-73.5336559014883,5.1567583578644,0.614688256175252));
#41635=CARTESIAN_POINT('Ctrl Pts',(-73.4546345019882,4.47052726991194,2.08546495386977));
#41636=CARTESIAN_POINT('Ctrl Pts',(-73.3756131024882,3.78429618195948,3.55624165156429));
#41637=CARTESIAN_POINT('Ctrl Pts',(-73.2965917029881,2.30090253687238,4.65540744461303));
#41638=CARTESIAN_POINT('Ctrl Pts',(-73.217570303488,0.69438387466605,4.88386064110368));
#41639=CARTESIAN_POINT('Ctrl Pts',(-73.138548903988,-0.912134787540277,
5.11231383759433));
#41640=CARTESIAN_POINT('Ctrl Pts',(-73.0595275044879,-2.64177846686585,
4.47005443752691));
#41641=CARTESIAN_POINT('Ctrl Pts',(-72.9805061049879,-3.71118316350073,
3.24908690921855));
#41642=CARTESIAN_POINT('Ctrl Pts',(-72.9232845786265,-4.48556794315112,
2.36495139593291));
#41643=CARTESIAN_POINT('Ctrl Pts',(-72.866063052265,-4.91374989924659,1.1773645668908));
#41644=CARTESIAN_POINT('Ctrl Pts',(-72.8088415259036,-4.92403075528272,
-0.00394394407346908));
#41645=CARTESIAN_POINT('Origin',(-74.75,0.,0.));
#41646=CARTESIAN_POINT('',(-71.0911584740964,-4.92530702679097,7.89345770752653E-5));
#41647=CARTESIAN_POINT('',(-71.3088415259036,-4.92529298732208,6.25886409129966E-5));
#41648=CARTESIAN_POINT('',(-74.75,-4.925,-6.03138548580071E-16));
#41649=CARTESIAN_POINT('Ctrl Pts',(-71.0911584740964,-4.92530702679097,
7.89345770752653E-5));
#41650=CARTESIAN_POINT('Ctrl Pts',(-71.0951756244005,-4.92537049355805,
0.0829354331087285));
#41651=CARTESIAN_POINT('Ctrl Pts',(-71.0991927747046,-4.92332239207377,
0.165788792394246));
#41652=CARTESIAN_POINT('Ctrl Pts',(-71.1032099250087,-4.91914176021086,
0.248534405960264));
#41653=CARTESIAN_POINT('Ctrl Pts',(-71.1427206247587,-4.87802313685915,
1.06237925759848));
#41654=CARTESIAN_POINT('Ctrl Pts',(-71.1822313245088,-4.63060960650741,
1.86580109561577));
#41655=CARTESIAN_POINT('Ctrl Pts',(-71.2217420242588,-4.20677566240803,
2.56178907813124));
#41656=CARTESIAN_POINT('Ctrl Pts',(-71.2612527240088,-3.78294171830867,
3.2577770606467));
#41657=CARTESIAN_POINT('Ctrl Pts',(-71.3007634237588,-3.18268736046168,
3.84633118766033));
#41658=CARTESIAN_POINT('Ctrl Pts',(-71.3402741235088,-2.47849220107993,
4.25638383154797));
#41659=CARTESIAN_POINT('Ctrl Pts',(-71.3797848232589,-1.77429704169817,
4.6664364754356));
#41660=CARTESIAN_POINT('Ctrl Pts',(-71.4192955230089,-0.966161080781646,
4.89798763619723));
#41661=CARTESIAN_POINT('Ctrl Pts',(-71.458806222759,-0.15166437801373,4.92308015523622));
#41662=CARTESIAN_POINT('Ctrl Pts',(-71.498316922509,0.662832324754209,4.94817267427521));
#41663=CARTESIAN_POINT('Ctrl Pts',(-71.537827622259,1.48368976937354,4.76680655159155));
#41664=CARTESIAN_POINT('Ctrl Pts',(-71.577338322009,2.21179022592752,4.40087706791648));
#41665=CARTESIAN_POINT('Ctrl Pts',(-71.616849021759,2.93989068248148,4.03494758424142));
#41666=CARTESIAN_POINT('Ctrl Pts',(-71.6563597215091,3.57523415097011,3.48445473957497));
#41667=CARTESIAN_POINT('Ctrl Pts',(-71.6958704212591,4.04110647518502,2.81587788992091));
#41668=CARTESIAN_POINT('Ctrl Pts',(-71.7353811210091,4.50697879939993,2.14730104026684));
#41669=CARTESIAN_POINT('Ctrl Pts',(-71.7748918207592,4.80337997934113,1.36064018562517));
#41670=CARTESIAN_POINT('Ctrl Pts',(-71.8144025205092,4.89451596279089,0.550865531588069));
#41671=CARTESIAN_POINT('Ctrl Pts',(-71.8539132202592,4.98565194624065,-0.258909122449052));
#41672=CARTESIAN_POINT('Ctrl Pts',(-71.8934239200093,4.87152273319896,-1.09179757588159));
#41673=CARTESIAN_POINT('Ctrl Pts',(-71.9329346197593,4.56591779143395,-1.84719557969087));
#41674=CARTESIAN_POINT('Ctrl Pts',(-71.9724453195093,4.26031284966897,-2.6025935835001));
#41675=CARTESIAN_POINT('Ctrl Pts',(-72.0119560192594,3.76323217918069,-3.28050113768607));
#41676=CARTESIAN_POINT('Ctrl Pts',(-72.0514667190094,3.13467977422752,-3.79913264594829));
#41677=CARTESIAN_POINT('Ctrl Pts',(-72.0909774187594,2.50612736927432,-4.31776415421053));
#41678=CARTESIAN_POINT('Ctrl Pts',(-72.1304881185094,1.74610322985622,-4.677119616549));
#41679=CARTESIAN_POINT('Ctrl Pts',(-72.1699988182594,0.946413527352501,
-4.83366628896438));
#41680=CARTESIAN_POINT('Ctrl Pts',(-72.2095095180095,0.146723824848781,
-4.99021296137976));
#41681=CARTESIAN_POINT('Ctrl Pts',(-72.2490202177595,-0.692631440740558,
-4.94395084387207));
#41682=CARTESIAN_POINT('Ctrl Pts',(-72.2885309175095,-1.47037247590722,
-4.70075073237942));
#41683=CARTESIAN_POINT('Ctrl Pts',(-72.3280416172596,-2.24811351107383,
-4.45755062088678));
#41684=CARTESIAN_POINT('Ctrl Pts',(-72.3675523170096,-2.96424031581777,
-4.01741251540921));
#41685=CARTESIAN_POINT('Ctrl Pts',(-72.4070630167596,-3.53214031702749,
-3.43290862203499));
#41686=CARTESIAN_POINT('Ctrl Pts',(-72.4465737165097,-4.10004031823723,
-2.84840472866075));
#41687=CARTESIAN_POINT('Ctrl Pts',(-72.4860844162597,-4.51971351591273,
-2.11953504738984));
#41688=CARTESIAN_POINT('Ctrl Pts',(-72.5255951160097,-4.74077108029855,
-1.3354637677462));
#41689=CARTESIAN_POINT('Ctrl Pts',(-72.5474495687053,-4.86304408772266,
-0.901772418331122));
#41690=CARTESIAN_POINT('Ctrl Pts',(-72.5693040214009,-4.92455064639084,
-0.451192141074852));
#41691=CARTESIAN_POINT('Ctrl Pts',(-72.5911584740964,-4.92473478262889,
-0.000479420352050008));
#41692=CARTESIAN_POINT('Ctrl Pts',(-72.8088415259036,-4.92403075528272,
-0.00394394407346908));
#41693=CARTESIAN_POINT('Ctrl Pts',(-72.7870416527649,-4.92794748682757,
-0.453990933627024));
#41694=CARTESIAN_POINT('Ctrl Pts',(-72.7652417796263,-4.87120978213869,
-0.903126684029842));
#41695=CARTESIAN_POINT('Ctrl Pts',(-72.7434419064877,-4.74985310581452,
-1.33422478502333));
#41696=CARTESIAN_POINT('Ctrl Pts',(-72.6644205069876,-4.30995263754923,
-2.89689329440753));
#41697=CARTESIAN_POINT('Ctrl Pts',(-72.5853991074877,-3.02098598707447,
-4.22255465662663));
#41698=CARTESIAN_POINT('Ctrl Pts',(-72.5063777079876,-1.47439201801798,
-4.7075043974958));
#41699=CARTESIAN_POINT('Ctrl Pts',(-72.4273563084875,0.0722019510385211,
-5.19245413836497));
#41700=CARTESIAN_POINT('Ctrl Pts',(-72.3483349089873,1.87642323867679,-4.83669225788416));
#41701=CARTESIAN_POINT('Ctrl Pts',(-72.2693135094873,3.13536286416929,-3.8053053582178));
#41702=CARTESIAN_POINT('Ctrl Pts',(-72.2298028097373,3.76483267691556,-3.28961190838461));
#41703=CARTESIAN_POINT('Ctrl Pts',(-72.1902921099873,4.25798207412539,-2.60501220375502));
#41704=CARTESIAN_POINT('Ctrl Pts',(-72.1507814102373,4.56314662709562,-1.84819336201149));
#41705=CARTESIAN_POINT('Ctrl Pts',(-72.1112707104872,4.86831118006585,-1.09137452026796));
#41706=CARTESIAN_POINT('Ctrl Pts',(-72.0717600107372,4.98549088879648,-0.262336541410498));
#41707=CARTESIAN_POINT('Ctrl Pts',(-72.0322493109872,4.89552659992533,0.546557739181261));
#41708=CARTESIAN_POINT('Ctrl Pts',(-71.9927386112371,4.80556231105419,1.35545201977297));
#41709=CARTESIAN_POINT('Ctrl Pts',(-71.9532279114871,4.50845402458131,2.14420260209896));
#41710=CARTESIAN_POINT('Ctrl Pts',(-71.9137172117371,4.04272711232429,2.81357323489973));
#41711=CARTESIAN_POINT('Ctrl Pts',(-71.8742065119871,3.57700020006725,3.48294386770051));
#41712=CARTESIAN_POINT('Ctrl Pts',(-71.834695812237,2.94265466202609,4.03293455097604));
#41713=CARTESIAN_POINT('Ctrl Pts',(-71.795185112487,2.21496146205706,4.39912726249893));
#41714=CARTESIAN_POINT('Ctrl Pts',(-71.755674412737,1.48726826208804,4.76531997402182));
#41715=CARTESIAN_POINT('Ctrl Pts',(-71.7161637129869,0.666227400191101,
4.94771471379208));
#41716=CARTESIAN_POINT('Ctrl Pts',(-71.6766530132369,-0.148363863695565,
4.92329807174835));
#41717=CARTESIAN_POINT('Ctrl Pts',(-71.6371423134869,-0.962955127582231,
4.89888142970463));
#41718=CARTESIAN_POINT('Ctrl Pts',(-71.5976316137369,-1.77109679345867,
4.66765340584695));
#41719=CARTESIAN_POINT('Ctrl Pts',(-71.5581209139868,-2.47553452990664,
4.25802563618345));
#41720=CARTESIAN_POINT('Ctrl Pts',(-71.5186102142368,-3.17997226635464,
3.84839786651993));
#41721=CARTESIAN_POINT('Ctrl Pts',(-71.4790995144868,-3.78070607337414,
3.26037035105059));
#41722=CARTESIAN_POINT('Ctrl Pts',(-71.4395888147368,-4.20503638745672,
2.56470212256411));
#41723=CARTESIAN_POINT('Ctrl Pts',(-71.4000781149867,-4.6293667015393,1.86903389407766));
#41724=CARTESIAN_POINT('Ctrl Pts',(-71.3605674152367,-4.87729352268495,
1.0657249525741));
#41725=CARTESIAN_POINT('Ctrl Pts',(-71.3210567154866,-4.91896083613891,
0.251894146567503));
#41726=CARTESIAN_POINT('Ctrl Pts',(-71.3169849856256,-4.92325481335249,
0.168025745967216));
#41727=CARTESIAN_POINT('Ctrl Pts',(-71.3129132557646,-4.92535829464761,
0.084045602148368));
#41728=CARTESIAN_POINT('Ctrl Pts',(-71.3088415259036,-4.92529298732208,
6.25886409129967E-5));
#41729=CARTESIAN_POINT('Origin',(-74.75,0.,0.));
#41730=CARTESIAN_POINT('',(-69.5911584740964,-4.92496870099469,-0.000124982963756182));
#41731=CARTESIAN_POINT('',(-69.8088415259036,-4.92497217740552,-0.000124998403726498));
#41732=CARTESIAN_POINT('',(-74.75,-4.925,-6.03138548580071E-16));
#41733=CARTESIAN_POINT('Ctrl Pts',(-69.5911584740964,-4.92496870099469,
-0.000124982963756182));
#41734=CARTESIAN_POINT('Ctrl Pts',(-69.6210472274001,-4.92435129484291,
0.616473474605334));
#41735=CARTESIAN_POINT('Ctrl Pts',(-69.6509359807039,-4.80819041294167,
1.23329802162961));
#41736=CARTESIAN_POINT('Ctrl Pts',(-69.6808247340076,-4.58206647380057,
1.80676283856513));
#41737=CARTESIAN_POINT('Ctrl Pts',(-69.7203354337577,-4.28314751338414,
2.56484049971359));
#41738=CARTESIAN_POINT('Ctrl Pts',(-69.7598461335077,-3.79206958950924,
3.24714761574599));
#41739=CARTESIAN_POINT('Ctrl Pts',(-69.7993568332577,-3.16812924736071,
3.77129715044878));
#41740=CARTESIAN_POINT('Ctrl Pts',(-69.8388675330078,-2.54418890521218,
4.29544668515157));
#41741=CARTESIAN_POINT('Ctrl Pts',(-69.8783782327578,-1.78738614479,4.66143863852477));
#41742=CARTESIAN_POINT('Ctrl Pts',(-69.9178889325078,-0.989103182537478,
4.82508031227747));
#41743=CARTESIAN_POINT('Ctrl Pts',(-69.9573996322578,-0.190820220284935,
4.98872198603017));
#41744=CARTESIAN_POINT('Ctrl Pts',(-69.9969103320079,0.648942943797969,
4.95001338016238));
#41745=CARTESIAN_POINT('Ctrl Pts',(-70.0364210317579,1.42878681291189,4.71362847149133));
#41746=CARTESIAN_POINT('Ctrl Pts',(-70.0759317315079,2.20863068202582,4.47724356282029));
#41747=CARTESIAN_POINT('Ctrl Pts',(-70.1154424312579,2.92855525617078,4.043182351346));
#41748=CARTESIAN_POINT('Ctrl Pts',(-70.154953131008,3.50163127605336,3.46385674265386));
#41749=CARTESIAN_POINT('Ctrl Pts',(-70.194463830758,4.0747072959359,2.88453113396175));
#41750=CARTESIAN_POINT('Ctrl Pts',(-70.233974530508,4.5009347615561,2.15994112805179));
#41751=CARTESIAN_POINT('Ctrl Pts',(-70.2734852302581,4.72884767388748,1.37757932621148));
#41752=CARTESIAN_POINT('Ctrl Pts',(-70.3129959300081,4.95676058621888,0.595217524371109));
#41753=CARTESIAN_POINT('Ctrl Pts',(-70.3525066297581,4.98635894526144,-0.244916073399569));
#41754=CARTESIAN_POINT('Ctrl Pts',(-70.3920173295082,4.81406881534808,-1.04137724504295));
#41755=CARTESIAN_POINT('Ctrl Pts',(-70.4315280292582,4.64177868543473,-1.83783841668626));
#41756=CARTESIAN_POINT('Ctrl Pts',(-70.4710387290082,4.26760006656548,-2.59062716220222));
#41757=CARTESIAN_POINT('Ctrl Pts',(-70.5105494287582,3.73671418001747,-3.20884594057165));
#41758=CARTESIAN_POINT('Ctrl Pts',(-70.5500601285083,3.20582829346942,-3.8270647189411));
#41759=CARTESIAN_POINT('Ctrl Pts',(-70.5895708282583,2.51823513924258,-4.31071353016401));
#41760=CARTESIAN_POINT('Ctrl Pts',(-70.6290815280083,1.75696002688706,-4.60139289329005));
#41761=CARTESIAN_POINT('Ctrl Pts',(-70.6685922277584,0.995684914531562,
-4.89207225641608));
#41762=CARTESIAN_POINT('Ctrl Pts',(-70.7081029275084,0.160727844047372,
-4.98978217144526));
#41763=CARTESIAN_POINT('Ctrl Pts',(-70.7476136272584,-0.647092004691638,
-4.88272435605896));
#41764=CARTESIAN_POINT('Ctrl Pts',(-70.7871243270084,-1.45491185343067,
-4.77566654067266));
#41765=CARTESIAN_POINT('Ctrl Pts',(-70.8266350267585,-2.23559448042453,
-4.46384099487087));
#41766=CARTESIAN_POINT('Ctrl Pts',(-70.8661457265085,-2.89487424539605,
-3.98490000982449));
#41767=CARTESIAN_POINT('Ctrl Pts',(-70.9056564262585,-3.55415401036755,
-3.50595902477813));
#41768=CARTESIAN_POINT('Ctrl Pts',(-70.9451671260085,-4.09203091331672,
-2.85990260048719));
#41769=CARTESIAN_POINT('Ctrl Pts',(-70.9846778257586,-4.44355750661547,
-2.12474045571216));
#41770=CARTESIAN_POINT('Ctrl Pts',(-71.0201713752045,-4.75934352406771,
-1.46432405961079));
#41771=CARTESIAN_POINT('Ctrl Pts',(-71.0556649246505,-4.92474626588707,
-0.732000028104022));
#41772=CARTESIAN_POINT('Ctrl Pts',(-71.0911584740964,-4.92530702679097,
7.89345770752653E-5));
#41773=CARTESIAN_POINT('Ctrl Pts',(-71.3088415259036,-4.92529298732208,
6.25886409129967E-5));
#41774=CARTESIAN_POINT('Ctrl Pts',(-71.2734025560146,-4.92472457428331,
-0.730897369035472));
#41775=CARTESIAN_POINT('Ctrl Pts',(-71.2379635861256,-4.75986224148064,
-1.46207471644967));
#41776=CARTESIAN_POINT('Ctrl Pts',(-71.2025246162366,-4.44501837891349,
-2.12168528048715));
#41777=CARTESIAN_POINT('Ctrl Pts',(-71.1630139164866,-4.09400080247182,
-2.85708123102559));
#41778=CARTESIAN_POINT('Ctrl Pts',(-71.1235032167365,-3.55655784382619,
-3.50352046159282));
#41779=CARTESIAN_POINT('Ctrl Pts',(-71.0839925169864,-2.89760438390271,
-3.98291704891334));
#41780=CARTESIAN_POINT('Ctrl Pts',(-71.0444818172364,-2.23865092397924,
-4.46231363623386));
#41781=CARTESIAN_POINT('Ctrl Pts',(-71.0049711174864,-1.4581869627779,-4.77466758030767));
#41782=CARTESIAN_POINT('Ctrl Pts',(-70.9654604177364,-0.650441891689018,
-4.8822776719318));
#41783=CARTESIAN_POINT('Ctrl Pts',(-70.9259497179864,0.157303179399837,
-4.98988776355592));
#41784=CARTESIAN_POINT('Ctrl Pts',(-70.8864390182364,0.99232936037624,-4.89275400273038));
#41785=CARTESIAN_POINT('Ctrl Pts',(-70.8469283184863,1.75380423846729,-4.60259771260765));
#41786=CARTESIAN_POINT('Ctrl Pts',(-70.8074176187363,2.51527911655836,-4.31244142248491));
#41787=CARTESIAN_POINT('Ctrl Pts',(-70.7679069189862,3.20320269176403,-3.82926260306501));
#41788=CARTESIAN_POINT('Ctrl Pts',(-70.7283962192362,3.73451218366536,-3.21140765367798));
#41789=CARTESIAN_POINT('Ctrl Pts',(-70.6888855194861,4.26582167556667,-2.59355270429097));
#41790=CARTESIAN_POINT('Ctrl Pts',(-70.6493748197361,4.64051708416361,-1.8410216249368));
#41791=CARTESIAN_POINT('Ctrl Pts',(-70.6098641199861,4.81335358220714,-1.04467902257766));
#41792=CARTESIAN_POINT('Ctrl Pts',(-70.5703534202361,4.98619008025067,-0.248336420218513));
#41793=CARTESIAN_POINT('Ctrl Pts',(-70.5308427204861,4.95716766774084,0.591817705145609));
#41794=CARTESIAN_POINT('Ctrl Pts',(-70.491332020736,4.72979133424381,1.37433574850428));
#41795=CARTESIAN_POINT('Ctrl Pts',(-70.451821320986,4.50241500074678,2.15685379186298));
#41796=CARTESIAN_POINT('Ctrl Pts',(-70.412310621236,4.07668474626254,2.88173575321616));
#41797=CARTESIAN_POINT('Ctrl Pts',(-70.372799921486,3.50400623574574,3.46145422727098));
#41798=CARTESIAN_POINT('Ctrl Pts',(-70.3332892217359,2.93132772522894,4.04117270132579));
#41799=CARTESIAN_POINT('Ctrl Pts',(-70.2937785219859,2.21170095867957,4.47572768808224));
#41800=CARTESIAN_POINT('Ctrl Pts',(-70.2542678222359,1.43201938322806,4.7126474368196));
#41801=CARTESIAN_POINT('Ctrl Pts',(-70.2147571224859,0.652337807776577,
4.94956718555696));
#41802=CARTESIAN_POINT('Ctrl Pts',(-70.1752464227358,-0.187398576577069,
4.98885169627524));
#41803=CARTESIAN_POINT('Ctrl Pts',(-70.1357357229858,-0.985793579818551,
4.82575756361085));
#41804=CARTESIAN_POINT('Ctrl Pts',(-70.0962250232358,-1.78418858306003,
4.66266343094646));
#41805=CARTESIAN_POINT('Ctrl Pts',(-70.0567143234858,-2.54124220518937,
4.29719065489939));
#41806=CARTESIAN_POINT('Ctrl Pts',(-70.0172036237357,-3.16554190244308,
3.7734691893382));
#41807=CARTESIAN_POINT('Ctrl Pts',(-69.9776929239857,-3.7898415996968,3.249747723777));
#41808=CARTESIAN_POINT('Ctrl Pts',(-69.9381822242356,-4.2813873720749,2.56777756870168));
#41809=CARTESIAN_POINT('Ctrl Pts',(-69.8986715244856,-4.58082620078788,
1.80990510032964));
#41810=CARTESIAN_POINT('Ctrl Pts',(-69.8687281916249,-4.80775704676852,
1.23554859108091));
#41811=CARTESIAN_POINT('Ctrl Pts',(-69.8387848587642,-4.92435274109235,
0.61759816956164));
#41812=CARTESIAN_POINT('Ctrl Pts',(-69.8088415259036,-4.92497217740552,
-0.000124998403726498));
#41813=CARTESIAN_POINT('Origin',(-74.75,0.,0.));
#41814=CARTESIAN_POINT('',(-68.0911584740964,-4.92463956541989,6.32542101904054E-5));
#41815=CARTESIAN_POINT('',(-68.3088415259036,-4.92463799521373,6.23586074887003E-5));
#41816=CARTESIAN_POINT('',(-74.75,-4.925,-6.03138548580071E-16));
#41817=CARTESIAN_POINT('Ctrl Pts',(-68.0911584740964,-4.92463956541989,
6.32542101904054E-5));
#41818=CARTESIAN_POINT('Ctrl Pts',(-68.1074081306498,-4.92479283391617,
0.335354424754706));
#41819=CARTESIAN_POINT('Ctrl Pts',(-68.1236577872031,-4.89104471897482,
0.670615165879185));
#41820=CARTESIAN_POINT('Ctrl Pts',(-68.1399074437565,-4.82308424351426,
0.998791021732417));
#41821=CARTESIAN_POINT('Ctrl Pts',(-68.1794181435065,-4.65783977007121,
1.79674374542491));
#41822=CARTESIAN_POINT('Ctrl Pts',(-68.2189288432566,-4.29032872667458,
2.55280998655433));
#41823=CARTESIAN_POINT('Ctrl Pts',(-68.2584395430066,-3.76492723805302,
3.1756964617695));
#41824=CARTESIAN_POINT('Ctrl Pts',(-68.2979502427567,-3.23952574943144,
3.7985829369847));
#41825=CARTESIAN_POINT('Ctrl Pts',(-68.3374609425067,-2.55623381558493,
4.28828964628564));
#41826=CARTESIAN_POINT('Ctrl Pts',(-68.3769716422567,-1.79755738736115,
4.58568561550747));
#41827=CARTESIAN_POINT('Ctrl Pts',(-68.4164823420067,-1.03888095913735,
4.88308158472931));
#41828=CARTESIAN_POINT('Ctrl Pts',(-68.4559930417568,-0.204820036536274,
4.98816681387202));
#41829=CARTESIAN_POINT('Ctrl Pts',(-68.4955037415068,0.603914416247443,
4.88825249992034));
#41830=CARTESIAN_POINT('Ctrl Pts',(-68.5350144412568,1.41264886903114,4.78833818596866));
#41831=CARTESIAN_POINT('Ctrl Pts',(-68.5745251410068,2.19605685199747,4.4834243289226));
#41832=CARTESIAN_POINT('Ctrl Pts',(-68.6140358407569,2.85954362849792,4.01032858527148));
#41833=CARTESIAN_POINT('Ctrl Pts',(-68.6535465405069,3.52303040499837,3.53723284162036));
#41834=CARTESIAN_POINT('Ctrl Pts',(-68.6930572402569,4.06659597503293,2.89595521136418));
#41835=CARTESIAN_POINT('Ctrl Pts',(-68.732567940007,4.42460602919109,2.16392851350848));
#41836=CARTESIAN_POINT('Ctrl Pts',(-68.772078639757,4.78261608334925,1.43190181565276));
#41837=CARTESIAN_POINT('Ctrl Pts',(-68.811589339507,4.955070621631,0.609126050197518));
#41838=CARTESIAN_POINT('Ctrl Pts',(-68.851100039257,4.92114614978146,-0.205050475785254));
#41839=CARTESIAN_POINT('Ctrl Pts',(-68.890610739007,4.88722167793191,-1.019227001768));
#41840=CARTESIAN_POINT('Ctrl Pts',(-68.9301214387571,4.64691819595108,-1.82480428827828));
#41841=CARTESIAN_POINT('Ctrl Pts',(-68.9696321385071,4.2292518041185,-2.52451070556032));
#41842=CARTESIAN_POINT('Ctrl Pts',(-69.0091428382571,3.81158541228592,-3.22421712284235));
#41843=CARTESIAN_POINT('Ctrl Pts',(-69.0486535380071,3.21655611060158,-3.81805267089615));
#41844=CARTESIAN_POINT('Ctrl Pts',(-69.0881642377572,2.51601233731885,-4.23431305450968));
#41845=CARTESIAN_POINT('Ctrl Pts',(-69.1276749375072,1.81546856403611,-4.65057343812322));
#41846=CARTESIAN_POINT('Ctrl Pts',(-69.1671856372573,1.00941031915496,-4.88925865729649));
#41847=CARTESIAN_POINT('Ctrl Pts',(-69.2066963370073,0.195167307063327,
-4.92154801331598));
#41848=CARTESIAN_POINT('Ctrl Pts',(-69.2462070367574,-0.619075705028329,
-4.95383736933547));
#41849=CARTESIAN_POINT('Ctrl Pts',(-69.2857177365074,-1.44150348433047,
-4.77973086220116));
#41850=CARTESIAN_POINT('Ctrl Pts',(-69.3252284362574,-2.17280974230828,
-4.4202514576521));
#41851=CARTESIAN_POINT('Ctrl Pts',(-69.3647391360074,-2.90411600028601,
-4.06077205310308));
#41852=CARTESIAN_POINT('Ctrl Pts',(-69.4042498357574,-3.54430073693943,
-3.51591975113934));
#41853=CARTESIAN_POINT('Ctrl Pts',(-69.4437605355075,-4.01606309768947,
-2.85148423114699));
#41854=CARTESIAN_POINT('Ctrl Pts',(-69.4832712352575,-4.48782545843955,
-2.18704871115457));
#41855=CARTESIAN_POINT('Ctrl Pts',(-69.5227819350075,-4.79116544328623,
-1.40302997313351));
#41856=CARTESIAN_POINT('Ctrl Pts',(-69.5622926347576,-4.88945543723059,
-0.594096500990709));
#41857=CARTESIAN_POINT('Ctrl Pts',(-69.5719145812038,-4.91339176495756,
-0.397098862457078));
#41858=CARTESIAN_POINT('Ctrl Pts',(-69.5815365276501,-4.92516745966715,
-0.198623638203757));
#41859=CARTESIAN_POINT('Ctrl Pts',(-69.5911584740964,-4.92496870099469,
-0.000124982963756182));
#41860=CARTESIAN_POINT('Ctrl Pts',(-69.8088415259036,-4.92497217740552,
-0.000124998403726498));
#41861=CARTESIAN_POINT('Ctrl Pts',(-69.7992741590142,-4.92517009707265,
-0.197497288638803));
#41862=CARTESIAN_POINT('Ctrl Pts',(-69.7897067921249,-4.91352796301374,
-0.394846378484991));
#41863=CARTESIAN_POINT('Ctrl Pts',(-69.7801394252355,-4.88986176534154,
-0.590742844833311));
#41864=CARTESIAN_POINT('Ctrl Pts',(-69.7406287254855,-4.7921266161344,-1.39974353995548));
#41865=CARTESIAN_POINT('Ctrl Pts',(-69.7011180257355,-4.48932443267227,
-2.18397014853107));
#41866=CARTESIAN_POINT('Ctrl Pts',(-69.6616073259854,-4.01801789610363,
-2.84872908003258));
#41867=CARTESIAN_POINT('Ctrl Pts',(-69.6220966262354,-3.54671135953497,
-3.51348801153412));
#41868=CARTESIAN_POINT('Ctrl Pts',(-69.5825859264854,-2.90690046985979,
-4.05877926596156));
#41869=CARTESIAN_POINT('Ctrl Pts',(-69.5430752267353,-2.17584093827506,
-4.41876016475229));
#41870=CARTESIAN_POINT('Ctrl Pts',(-69.5035645269853,-1.44478140669035,
-4.778741063543));
#41871=CARTESIAN_POINT('Ctrl Pts',(-69.4640538272353,-0.622473233196095,
-4.95341160669699));
#41872=CARTESIAN_POINT('Ctrl Pts',(-69.4245431274853,0.191791734706842,
-4.92168072074847));
#41873=CARTESIAN_POINT('Ctrl Pts',(-69.3850324277353,1.00605670260978,-4.88994983479994));
#41874=CARTESIAN_POINT('Ctrl Pts',(-69.3455217279852,1.8122784649214,-4.65181751974888));
#41875=CARTESIAN_POINT('Ctrl Pts',(-69.3060110282352,2.51310757343917,-4.23603771321305));
#41876=CARTESIAN_POINT('Ctrl Pts',(-69.2665003284852,3.21393668195695,-3.82025790667721));
#41877=CARTESIAN_POINT('Ctrl Pts',(-69.2269896287351,3.80937313668088,-3.22683060865659));
#41878=CARTESIAN_POINT('Ctrl Pts',(-69.1874789289851,4.2275193362816,-2.52741081868947));
#41879=CARTESIAN_POINT('Ctrl Pts',(-69.147968229235,4.64566553588232,-1.82799102872235));
#41880=CARTESIAN_POINT('Ctrl Pts',(-69.108457529485,4.88652148035984,-1.02257874680874));
#41881=CARTESIAN_POINT('Ctrl Pts',(-69.068946829735,4.92100436097563,-0.208425678976473));
#41882=CARTESIAN_POINT('Ctrl Pts',(-69.029436129985,4.95548724159141,0.60572738885575));
#41883=CARTESIAN_POINT('Ctrl Pts',(-68.989925430235,4.78359705834548,1.42862124260663));
#41884=CARTESIAN_POINT('Ctrl Pts',(-68.9504147304849,4.42608916083589,2.16089331641106));
#41885=CARTESIAN_POINT('Ctrl Pts',(-68.9109040307349,4.06858126332627,2.89316539021553));
#41886=CARTESIAN_POINT('Ctrl Pts',(-68.8713933309848,3.52545565155298,3.53481568407353));
#41887=CARTESIAN_POINT('Ctrl Pts',(-68.8318826312348,2.86229351099765,4.00836638064507));
#41888=CARTESIAN_POINT('Ctrl Pts',(-68.7923719314848,2.19913137044234,4.4819170772166));
#41889=CARTESIAN_POINT('Ctrl Pts',(-68.7528612317348,1.41593270110502,4.78736817650169));
#41890=CARTESIAN_POINT('Ctrl Pts',(-68.7133505319847,0.607266965471941,
4.88783715125428));
#41891=CARTESIAN_POINT('Ctrl Pts',(-68.6738398322347,-0.201398770161134,
4.98830612600687));
#41892=CARTESIAN_POINT('Ctrl Pts',(-68.6343291324847,-1.03553157208996,
4.88379297622697));
#41893=CARTESIAN_POINT('Ctrl Pts',(-68.5948184327347,-1.79441179684599,
4.58691742763232));
#41894=CARTESIAN_POINT('Ctrl Pts',(-68.5553077329847,-2.55329202160205,
4.29004187903766));
#41895=CARTESIAN_POINT('Ctrl Pts',(-68.5157970332346,-3.23691966918531,
3.80080393162825));
#41896=CARTESIAN_POINT('Ctrl Pts',(-68.4762863334846,-3.76274825208007,
3.17827795764013));
#41897=CARTESIAN_POINT('Ctrl Pts',(-68.4367756337345,-4.28857683497483,
2.55575198365201));
#41898=CARTESIAN_POINT('Ctrl Pts',(-68.3972649339845,-4.65660635318109,
1.79993798308518));
#41899=CARTESIAN_POINT('Ctrl Pts',(-68.3577542342345,-4.82239807731116,
1.0020987818121));
#41900=CARTESIAN_POINT('Ctrl Pts',(-68.3414499981242,-4.89081264431328,
0.672867490088553));
#41901=CARTESIAN_POINT('Ctrl Pts',(-68.3251457620139,-4.92478953903053,
0.336480018204721));
#41902=CARTESIAN_POINT('Ctrl Pts',(-68.3088415259036,-4.92463799521373,
6.23586074887003E-5));
#41903=CARTESIAN_POINT('Origin',(-74.75,0.,0.));
#41904=CARTESIAN_POINT('',(-66.5911584740964,-4.92536651616557,5.39754973401252E-5));
#41905=CARTESIAN_POINT('',(-66.8088415259036,-4.92536456956953,5.50140474394305E-5));
#41906=CARTESIAN_POINT('',(-74.75,-4.925,-6.03138548580071E-16));
#41907=CARTESIAN_POINT('Ctrl Pts',(-66.5911584740964,-4.92536651616557,
5.39754973401252E-5));
#41908=CARTESIAN_POINT('Ctrl Pts',(-66.5937690338994,-4.92539680548438,
0.0538966888551685));
#41909=CARTESIAN_POINT('Ctrl Pts',(-66.5963795937024,-4.92453210201228,
0.107738427698145));
#41910=CARTESIAN_POINT('Ctrl Pts',(-66.5989901535054,-4.92276614638168,
0.161550590117274));
#41911=CARTESIAN_POINT('Ctrl Pts',(-66.6385008532554,-4.89603849102888,
0.975995135615054));
#41912=CARTESIAN_POINT('Ctrl Pts',(-66.6780115530054,-4.66286388744967,
1.78366470433721));
#41913=CARTESIAN_POINT('Ctrl Pts',(-66.7175222527555,-4.25139764002992,
2.48703502819659));
#41914=CARTESIAN_POINT('Ctrl Pts',(-66.7570329525055,-3.83993139261016,
3.19040535205602));
#41915=CARTESIAN_POINT('Ctrl Pts',(-66.7965436522555,-3.25017350134988,
3.78947643105268));
#41916=CARTESIAN_POINT('Ctrl Pts',(-66.8360543520055,-2.5533358936523,4.21191179149275));
#41917=CARTESIAN_POINT('Ctrl Pts',(-66.8755650517556,-1.85649828595472,
4.63434715193282));
#41918=CARTESIAN_POINT('Ctrl Pts',(-66.9150757515056,-1.05258096181989,
4.88014679381625));
#41919=CARTESIAN_POINT('Ctrl Pts',(-66.9545864512556,-0.23865511431353,
4.91963096802401));
#41920=CARTESIAN_POINT('Ctrl Pts',(-66.9940971510057,0.57527073319281,4.95911514223177));
#41921=CARTESIAN_POINT('Ctrl Pts',(-67.0336078507557,1.39920510407067,4.79228384876389));
#41922=CARTESIAN_POINT('Ctrl Pts',(-67.0731185505057,2.13365979227223,4.43928158782135));
#41923=CARTESIAN_POINT('Ctrl Pts',(-67.1126292502557,2.86811448047378,4.08627932687882));
#41924=CARTESIAN_POINT('Ctrl Pts',(-67.1521399500058,3.51308948599901,3.54710609846165));
#41925=CARTESIAN_POINT('Ctrl Pts',(-67.1916506497558,3.99070554016657,2.88686584669476));
#41926=CARTESIAN_POINT('Ctrl Pts',(-67.2311613495058,4.46832159433413,2.22662559492788));
#41927=CARTESIAN_POINT('Ctrl Pts',(-67.2706720492559,4.77857869714402,1.44531831981123));
#41928=CARTESIAN_POINT('Ctrl Pts',(-67.3101827490059,4.88401400730307,0.637285102286454));
#41929=CARTESIAN_POINT('Ctrl Pts',(-67.3496934487559,4.98944931746212,-0.170748115238346));
#41930=CARTESIAN_POINT('Ctrl Pts',(-67.389204148506,4.89006283497034,-1.00550727517133));
#41931=CARTESIAN_POINT('Ctrl Pts',(-67.428714848256,4.59785525211343,-1.76619710274414));
#41932=CARTESIAN_POINT('Ctrl Pts',(-67.468225548006,4.30564766925652,-2.52688693031692));
#41933=CARTESIAN_POINT('Ctrl Pts',(-67.5077362477561,3.8206189860345,-3.21350742552951));
#41934=CARTESIAN_POINT('Ctrl Pts',(-67.5472469475061,3.20133531557612,-3.7431507213007));
#41935=CARTESIAN_POINT('Ctrl Pts',(-67.5867576472561,2.58205164511774,-4.2727940170719));
#41936=CARTESIAN_POINT('Ctrl Pts',(-67.6262683470061,1.828512987423,-4.64546011340169));
#41937=CARTESIAN_POINT('Ctrl Pts',(-67.6657790467562,1.03170742587757,-4.81615042461486));
#41938=CARTESIAN_POINT('Ctrl Pts',(-67.7052897465062,0.234901864332088,
-4.98684073582805));
#41939=CARTESIAN_POINT('Ctrl Pts',(-67.7448004462562,-0.605170601064078,
-4.95555526192458));
#41940=CARTESIAN_POINT('Ctrl Pts',(-67.7843111460062,-1.38707312596202,
-4.72607165290189));
#41941=CARTESIAN_POINT('Ctrl Pts',(-67.8238218457563,-2.16897565085989,
-4.49658804387921));
#41942=CARTESIAN_POINT('Ctrl Pts',(-67.8633325455063,-2.89270823525954,
-4.06890629973734));
#41943=CARTESIAN_POINT('Ctrl Pts',(-67.9028432452563,-3.47088181150553,
-3.49466802081241));
#41944=CARTESIAN_POINT('Ctrl Pts',(-67.9423539450063,-4.04905538775154,
-2.92042974188746));
#41945=CARTESIAN_POINT('Ctrl Pts',(-67.9818646447564,-4.48166995584387,
-2.19963492817945));
#41946=CARTESIAN_POINT('Ctrl Pts',(-68.0213753445064,-4.71648828814532,
-1.41931791819765));
#41947=CARTESIAN_POINT('Ctrl Pts',(-68.0446363877031,-4.85473234369457,
-0.959923683443132));
#41948=CARTESIAN_POINT('Ctrl Pts',(-68.0678974308997,-4.92442016477588,
-0.47989903766246));
#41949=CARTESIAN_POINT('Ctrl Pts',(-68.0911584740964,-4.92463956541989,
6.32542101904054E-5));
#41950=CARTESIAN_POINT('Ctrl Pts',(-68.3088415259036,-4.92463799521373,
6.23586074887003E-5));
#41951=CARTESIAN_POINT('Ctrl Pts',(-68.2856350622639,-4.92442229690989,
-0.47877419235977));
#41952=CARTESIAN_POINT('Ctrl Pts',(-68.2624285986241,-4.85506595209795,
-0.957671900476631));
#41953=CARTESIAN_POINT('Ctrl Pts',(-68.2392221349844,-4.71746064773569,
-1.41608270296097));
#41954=CARTESIAN_POINT('Ctrl Pts',(-68.1997114352344,-4.48317756397627,
-2.19656058448168));
#41955=CARTESIAN_POINT('Ctrl Pts',(-68.1602007354844,-4.05105746640354,
-2.91765194554378));
#41956=CARTESIAN_POINT('Ctrl Pts',(-68.1206900357343,-3.47327787646076,
-3.49228664021852));
#41957=CARTESIAN_POINT('Ctrl Pts',(-68.0811793359843,-2.89549828651797,
-4.06692133489327));
#41958=CARTESIAN_POINT('Ctrl Pts',(-68.0416686362342,-2.17205920420512,
-4.49509936318065));
#41959=CARTESIAN_POINT('Ctrl Pts',(-68.0021579364842,-1.3903142574668,-4.72511919955948));
#41960=CARTESIAN_POINT('Ctrl Pts',(-67.9626472367342,-0.608569310728499,
-4.95513903593829));
#41961=CARTESIAN_POINT('Ctrl Pts',(-67.9231365369842,0.231481500435274,
-4.98700068040857));
#41962=CARTESIAN_POINT('Ctrl Pts',(-67.8836258372341,1.02840394637516,-4.81685691168427));
#41963=CARTESIAN_POINT('Ctrl Pts',(-67.8441151374841,1.82532639231506,-4.64671314295996));
#41964=CARTESIAN_POINT('Ctrl Pts',(-67.8046044377341,2.57912047303106,-4.27456396104109));
#41965=CARTESIAN_POINT('Ctrl Pts',(-67.7650937379841,3.19876726338711,-3.74534553536036));
#41966=CARTESIAN_POINT('Ctrl Pts',(-67.725583038234,3.81841405374317,-3.21612710967962));
#41967=CARTESIAN_POINT('Ctrl Pts',(-67.686072338484,4.30391355373927,-2.52983944023701));
#41968=CARTESIAN_POINT('Ctrl Pts',(-67.646561638734,4.59664280018932,-1.76935020615716));
#41969=CARTESIAN_POINT('Ctrl Pts',(-67.6070509389839,4.88937204663936,-1.00886097207732));
#41970=CARTESIAN_POINT('Ctrl Pts',(-67.5675402392339,4.98933103954337,-0.174170173360232));
#41971=CARTESIAN_POINT('Ctrl Pts',(-67.5280295394839,4.8844499572822,0.63393516968748));
#41972=CARTESIAN_POINT('Ctrl Pts',(-67.4885188397338,4.77956887502102,1.44204051273519));
#41973=CARTESIAN_POINT('Ctrl Pts',(-67.4490081399838,4.46984771759466,2.22356040011353));
#41974=CARTESIAN_POINT('Ctrl Pts',(-67.4094974402338,3.99268461210709,2.88412807843272));
#41975=CARTESIAN_POINT('Ctrl Pts',(-67.3699867404838,3.5155215066195,3.54469575675192));
#41976=CARTESIAN_POINT('Ctrl Pts',(-67.3304760407338,2.87091645307069,4.08431122601196));
#41977=CARTESIAN_POINT('Ctrl Pts',(-67.2909653409837,2.13670404928016,4.43781714250942));
#41978=CARTESIAN_POINT('Ctrl Pts',(-67.2514546412337,1.40249164548963,4.79132305900688));
#41979=CARTESIAN_POINT('Ctrl Pts',(-67.2119439414836,0.578671891457383,
4.95871942274176));
#41980=CARTESIAN_POINT('Ctrl Pts',(-67.1724332417336,-0.235280846492803,
4.91979350256028));
#41981=CARTESIAN_POINT('Ctrl Pts',(-67.1329225419836,-1.04923358444297,
4.88086758237879));
#41982=CARTESIAN_POINT('Ctrl Pts',(-67.0934118422336,-1.85331930631107,
4.63561937828096));
#41983=CARTESIAN_POINT('Ctrl Pts',(-67.0539011424835,-2.55044648538715,
4.2136620545242));
#41984=CARTESIAN_POINT('Ctrl Pts',(-67.0143904427335,-3.24757366446323,
3.79170473076744));
#41985=CARTESIAN_POINT('Ctrl Pts',(-66.9748797429835,-3.83774230074728,
3.19303828735175));
#41986=CARTESIAN_POINT('Ctrl Pts',(-66.9353690432334,-4.24969087030623,
2.48995033914265));
#41987=CARTESIAN_POINT('Ctrl Pts',(-66.8958583434834,-4.66163943986517,
1.78686239093355));
#41988=CARTESIAN_POINT('Ctrl Pts',(-66.8563476437334,-4.895367942699,0.979352937931041));
#41989=CARTESIAN_POINT('Ctrl Pts',(-66.8168369439834,-4.92265419234351,
0.164926914612239));
#41990=CARTESIAN_POINT('Ctrl Pts',(-66.8141718046234,-4.92449474840484,
0.109990938681131));
#41991=CARTESIAN_POINT('Ctrl Pts',(-66.8115066652635,-4.92539599436154,
0.0550234924270285));
#41992=CARTESIAN_POINT('Ctrl Pts',(-66.8088415259036,-4.92536456956953,
5.50140474394305E-5));
#41993=CARTESIAN_POINT('Origin',(-74.75,0.,0.));
#41994=CARTESIAN_POINT('',(-65.0911584740964,-4.92488160240034,-0.000121459184743433));
#41995=CARTESIAN_POINT('',(-65.3088415259036,-4.92488488230248,-0.000121706157415094));
#41996=CARTESIAN_POINT('',(-74.75,-4.925,-6.03138548580071E-16));
#41997=CARTESIAN_POINT('Ctrl Pts',(-65.0911584740964,-4.92488160240034,
-0.000121459184743433));
#41998=CARTESIAN_POINT('Ctrl Pts',(-65.1196406368991,-4.9243274969235,0.587489219440107));
#41999=CARTESIAN_POINT('Ctrl Pts',(-65.1481227997017,-4.81907471229367,
1.17529310063035));
#42000=CARTESIAN_POINT('Ctrl Pts',(-65.1766049625043,-4.61328490383012,
1.72549341384484));
#42001=CARTESIAN_POINT('Ctrl Pts',(-65.2161156622544,-4.32781152211541,
2.48873599231131));
#42002=CARTESIAN_POINT('Ctrl Pts',(-65.2556263620044,-3.84886996389699,
3.17961623649651));
#42003=CARTESIAN_POINT('Ctrl Pts',(-65.2951370617544,-3.23429133576914,
3.71471192429474));
#42004=CARTESIAN_POINT('Ctrl Pts',(-65.3346477615044,-2.61971270764127,
4.24980761209299));
#42005=CARTESIAN_POINT('Ctrl Pts',(-65.3741584612545,-1.86949700960395,
4.62911874350427));
#42006=CARTESIAN_POINT('Ctrl Pts',(-65.4136691610045,-1.07423108520293,
4.80684435994266));
#42007=CARTESIAN_POINT('Ctrl Pts',(-65.4531798607546,-0.278965160801917,
4.98456997638105));
#42008=CARTESIAN_POINT('Ctrl Pts',(-65.4926905605046,0.561350989962814,
4.96071007784656));
#42009=CARTESIAN_POINT('Ctrl Pts',(-65.5322012602546,1.34525109828691,4.73814569295697));
#42010=CARTESIAN_POINT('Ctrl Pts',(-65.5717119600046,2.12915120661099,4.51558130806739));
#42011=CARTESIAN_POINT('Ctrl Pts',(-65.6112226597546,2.85663527249444,4.09431243682272));
#42012=CARTESIAN_POINT('Ctrl Pts',(-65.6507333595047,3.43986124540353,3.52520633970548));
#42013=CARTESIAN_POINT('Ctrl Pts',(-65.6902440592547,4.02308721831264,2.95610024258822));
#42014=CARTESIAN_POINT('Ctrl Pts',(-65.7297547590048,4.46205509824734,2.23915691959843));
#42015=CARTESIAN_POINT('Ctrl Pts',(-65.7692654587548,4.7037605095791,1.46094565047882));
#42016=CARTESIAN_POINT('Ctrl Pts',(-65.8087761585048,4.94546592091086,0.682734381359203));
#42017=CARTESIAN_POINT('Ctrl Pts',(-65.8482868582548,4.98990886363963,-0.156744833890189));
#42018=CARTESIAN_POINT('Ctrl Pts',(-65.8877975580048,4.83172295325732,-0.956126784529762));
#42019=CARTESIAN_POINT('Ctrl Pts',(-65.9273082577549,4.67353704287501,-1.75550873516929));
#42020=CARTESIAN_POINT('Ctrl Pts',(-65.9668189575049,4.31272227938163,-2.51479342119902));
#42021=CARTESIAN_POINT('Ctrl Pts',(-66.006329657255,3.79284622689918,-3.14229893934767));
#42022=CARTESIAN_POINT('Ctrl Pts',(-66.045840357005,3.27297017441671,-3.76980445749635));
#42023=CARTESIAN_POINT('Ctrl Pts',(-66.085351056755,2.59403283294513,-4.26553080776395));
#42024=CARTESIAN_POINT('Ctrl Pts',(-66.124861756505,1.83801434618199,-4.56962015799541));
#42025=CARTESIAN_POINT('Ctrl Pts',(-66.1643724562551,1.08199585941888,-4.87370950822687));
#42026=CARTESIAN_POINT('Ctrl Pts',(-66.2038831560051,0.248896227364141,
-4.98616185842222));
#42027=CARTESIAN_POINT('Ctrl Pts',(-66.2433938557551,-0.56068965944009,
-4.89339884241268));
#42028=CARTESIAN_POINT('Ctrl Pts',(-66.2829045555051,-1.37027554624432,
-4.80063582640315));
#42029=CARTESIAN_POINT('Ctrl Pts',(-66.3224152552551,-2.15634768779811,
-4.50265744418875));
#42030=CARTESIAN_POINT('Ctrl Pts',(-66.3619259550052,-2.82398965634758,
-4.03544390940708));
#42031=CARTESIAN_POINT('Ctrl Pts',(-66.4014366547552,-3.49163162489706,
-3.56823037462541));
#42032=CARTESIAN_POINT('Ctrl Pts',(-66.4409473545053,-4.04084342044216,
-2.93178168727652));
#42033=CARTESIAN_POINT('Ctrl Pts',(-66.4804580542553,-4.40530896465153,
-2.20294758246529));
#42034=CARTESIAN_POINT('Ctrl Pts',(-66.5173581942024,-4.74569345979552,
-1.5222691678622));
#42035=CARTESIAN_POINT('Ctrl Pts',(-66.5542583341494,-4.92493837806983,
-0.761010243661963));
#42036=CARTESIAN_POINT('Ctrl Pts',(-66.5911584740964,-4.92536651616557,
5.39754973401252E-5));
#42037=CARTESIAN_POINT('Ctrl Pts',(-66.8088415259036,-4.92536456956953,
5.50140474394305E-5));
#42038=CARTESIAN_POINT('Ctrl Pts',(-66.7719959655135,-4.92493012171699,
-0.759884379797087));
#42039=CARTESIAN_POINT('Ctrl Pts',(-66.7351504051234,-4.74623364618368,
-1.52002104452459));
#42040=CARTESIAN_POINT('Ctrl Pts',(-66.6983048447333,-4.40681886269117,
-2.19992561146736));
#42041=CARTESIAN_POINT('Ctrl Pts',(-66.6587941449832,-4.04285328693911,
-2.92900952059309));
#42042=CARTESIAN_POINT('Ctrl Pts',(-66.6192834452332,-3.4940781389798,-3.56583474520942));
#42043=CARTESIAN_POINT('Ctrl Pts',(-66.5797727454832,-2.82675677293931,
-4.03350608419058));
#42044=CARTESIAN_POINT('Ctrl Pts',(-66.5402620457332,-2.15943540689881,
-4.50117742317175));
#42045=CARTESIAN_POINT('Ctrl Pts',(-66.5007513459831,-1.37356782277715,
-4.79969487651773));
#42046=CARTESIAN_POINT('Ctrl Pts',(-66.4612406462331,-0.564045748482333,
-4.89301313897477));
#42047=CARTESIAN_POINT('Ctrl Pts',(-66.4217299464831,0.24547632581244,-4.9863314014318));
#42048=CARTESIAN_POINT('Ctrl Pts',(-66.382219246733,1.07865289028041,-4.8744504729999));
#42049=CARTESIAN_POINT('Ctrl Pts',(-66.342708546983,1.8348797649651,-4.57087972196626));
#42050=CARTESIAN_POINT('Ctrl Pts',(-66.303197847233,2.59110663964981,-4.26730897093261));
#42051=CARTESIAN_POINT('Ctrl Pts',(-66.2636871474829,3.2703838245513,-3.77204839729721));
#42052=CARTESIAN_POINT('Ctrl Pts',(-66.2241764477329,3.79069014064888,-3.14489959174344));
#42053=CARTESIAN_POINT('Ctrl Pts',(-66.1846657479829,4.31099645674646,-2.51775078618968));
#42054=CARTESIAN_POINT('Ctrl Pts',(-66.1451550482329,4.67233190404011,-1.75871374871756));
#42055=CARTESIAN_POINT('Ctrl Pts',(-66.1056443484829,4.83106604702023,-0.959440479596849));
#42056=CARTESIAN_POINT('Ctrl Pts',(-66.0661336487328,4.98980019000035,-0.160167210476135));
#42057=CARTESIAN_POINT('Ctrl Pts',(-66.0266229489828,4.94593302866694,0.679342290293157));
#42058=CARTESIAN_POINT('Ctrl Pts',(-65.9871122492328,4.70476142323086,1.45771915506364));
#42059=CARTESIAN_POINT('Ctrl Pts',(-65.9476015494827,4.46358981779478,2.23609601983415));
#42060=CARTESIAN_POINT('Ctrl Pts',(-65.9080908497327,4.02511376825602,2.95334024860583));
#42061=CARTESIAN_POINT('Ctrl Pts',(-65.8685801499827,3.44227826283868,3.52284622794538));
#42062=CARTESIAN_POINT('Ctrl Pts',(-65.8290694502326,2.85944275742136,4.09235220728492));
#42063=CARTESIAN_POINT('Ctrl Pts',(-65.7895587504826,2.13224779612549,4.51411993719233));
#42064=CARTESIAN_POINT('Ctrl Pts',(-65.7500480507326,1.34850052076172,4.73722192113332));
#42065=CARTESIAN_POINT('Ctrl Pts',(-65.7105373509825,0.564753245397947,
4.96032390507432));
#42066=CARTESIAN_POINT('Ctrl Pts',(-65.6710266512325,-0.275546344033775,
4.9847601430489));
#42067=CARTESIAN_POINT('Ctrl Pts',(-65.6315159514825,-1.0709339784724,4.8075800147594));
#42068=CARTESIAN_POINT('Ctrl Pts',(-65.5920052517325,-1.86632161291102,
4.6303998864699));
#42069=CARTESIAN_POINT('Ctrl Pts',(-65.5524945519824,-2.61679729235658,
4.25160339191634));
#42070=CARTESIAN_POINT('Ctrl Pts',(-65.5129838522324,-3.23174278109815,
3.71692934845159));
#42071=CARTESIAN_POINT('Ctrl Pts',(-65.4734731524824,-3.84668826983973,
3.18225530498682));
#42072=CARTESIAN_POINT('Ctrl Pts',(-65.4339624527323,-4.32610356787728,
2.49170371261087));
#42073=CARTESIAN_POINT('Ctrl Pts',(-65.3944517529823,-4.61210036560815,
1.72865710946905));
#42074=CARTESIAN_POINT('Ctrl Pts',(-65.3659150106227,-4.81866256228257,
1.17754400694317));
#42075=CARTESIAN_POINT('Ctrl Pts',(-65.3373782682632,-4.92432796707018,
0.588613870356569));
#42076=CARTESIAN_POINT('Ctrl Pts',(-65.3088415259036,-4.92488488230248,
-0.000121706157415094));
#42077=CARTESIAN_POINT('Origin',(-74.75,0.,0.));
#42078=CARTESIAN_POINT('',(-63.5911584740964,-4.92468790276689,8.47132295976605E-5));
#42079=CARTESIAN_POINT('',(-63.8088415259036,-4.92468576593835,8.39450088834838E-5));
#42080=CARTESIAN_POINT('',(-74.75,-4.925,-6.03138548580071E-16));
#42081=CARTESIAN_POINT('Ctrl Pts',(-63.5911584740964,-4.92468790276689,
8.47132295976605E-5));
#42082=CARTESIAN_POINT('Ctrl Pts',(-63.6060015401487,-4.92487782722442,
0.30634405253935));
#42083=CARTESIAN_POINT('Ctrl Pts',(-63.620844606201,-4.89675395020855,0.612568936338183));
#42084=CARTESIAN_POINT('Ctrl Pts',(-63.6356876722532,-4.8399842696057,0.913387866734746));
#42085=CARTESIAN_POINT('Ctrl Pts',(-63.6751983720033,-4.68886927777682,
1.71413660666273));
#42086=CARTESIAN_POINT('Ctrl Pts',(-63.7147090717532,-4.33477897649552,
2.47658043182792));
#42087=CARTESIAN_POINT('Ctrl Pts',(-63.7542197715033,-3.82046896632728,
3.10865598007547));
#42088=CARTESIAN_POINT('Ctrl Pts',(-63.7937304712533,-3.306158956159,3.74073152832308));
#42089=CARTESIAN_POINT('Ctrl Pts',(-63.8332411710034,-2.63162923710374,
4.24243879965303));
#42090=CARTESIAN_POINT('Ctrl Pts',(-63.8727518707534,-1.87832774245171,
4.55319777926076));
#42091=CARTESIAN_POINT('Ctrl Pts',(-63.9122625705035,-1.1250262477997,4.86395675886848));
#42092=CARTESIAN_POINT('Ctrl Pts',(-63.9517732702534,-0.292952977550855,
4.98376744675398));
#42093=CARTESIAN_POINT('Ctrl Pts',(-63.9912839700035,0.517421108612269,
4.89816297416606));
#42094=CARTESIAN_POINT('Ctrl Pts',(-64.0307946697535,1.32779519477542,4.81255850157814));
#42095=CARTESIAN_POINT('Ctrl Pts',(-64.0703053695035,2.11647009685286,4.52153886851682));
#42096=CARTESIAN_POINT('Ctrl Pts',(-64.1098160692536,2.78821510966239,4.06024403544654));
#42097=CARTESIAN_POINT('Ctrl Pts',(-64.1493267690036,3.45996012247191,3.59894920237627));
#42098=CARTESIAN_POINT('Ctrl Pts',(-64.1888374687536,4.01477524601345,2.96737916929708));
#42099=CARTESIAN_POINT('Ctrl Pts',(-64.2283481685037,4.38566781281213,2.24179458487893));
#42100=CARTESIAN_POINT('Ctrl Pts',(-64.2678588682537,4.75656037961082,1.51621000046075));
#42101=CARTESIAN_POINT('Ctrl Pts',(-64.3073695680038,4.94353038966664,0.696610864703609));
#42102=CARTESIAN_POINT('Ctrl Pts',(-64.3468802677538,4.92400163843868,-0.11803808615025));
#42103=CARTESIAN_POINT('Ctrl Pts',(-64.3863909675038,4.90447288721073,-0.932687037004086));
#42104=CARTESIAN_POINT('Ctrl Pts',(-64.4259016672538,4.67844537469903,-1.74238580295464));
#42105=CARTESIAN_POINT('Ctrl Pts',(-64.4654123670038,4.2732114102574,-2.44936509495314));
#42106=CARTESIAN_POINT('Ctrl Pts',(-64.5049230667538,3.86797744581578,-3.15634438695162));
#42107=CARTESIAN_POINT('Ctrl Pts',(-64.5444337665039,3.28353702944425,-3.76060420499805));
#42108=CARTESIAN_POINT('Ctrl Pts',(-64.5839444662539,2.59046001551689,-4.18918154692979));
#42109=CARTESIAN_POINT('Ctrl Pts',(-64.623455166004,1.89738300158948,-4.61775888886157));
#42110=CARTESIAN_POINT('Ctrl Pts',(-64.662965865754,1.09566939010621,-4.87065375467863));
#42111=CARTESIAN_POINT('Ctrl Pts',(-64.702476565504,0.282124280829646,-4.91732966306869));
#42112=CARTESIAN_POINT('Ctrl Pts',(-64.741987265254,-0.531420828446872,
-4.96400557145875));
#42113=CARTESIAN_POINT('Ctrl Pts',(-64.781497965004,-1.35679743551669,-4.80446252242183));
#42114=CARTESIAN_POINT('Ctrl Pts',(-64.8210086647541,-2.09434318758374,
-4.45796497717854));
#42115=CARTESIAN_POINT('Ctrl Pts',(-64.8605193645041,-2.83188893965079,
-4.11146743193524));
#42116=CARTESIAN_POINT('Ctrl Pts',(-64.9000300642541,-3.48160383671507,
-3.57801539048556));
#42117=CARTESIAN_POINT('Ctrl Pts',(-64.9395407640041,-3.96503627894513,
-2.9220219766076));
#42118=CARTESIAN_POINT('Ctrl Pts',(-64.9790514637542,-4.4484687211752,-2.26602856272963));
#42119=CARTESIAN_POINT('Ctrl Pts',(-65.0185621635042,-4.76561870857105,
-1.48749377642337));
#42120=CARTESIAN_POINT('Ctrl Pts',(-65.0580728632543,-4.87819109966346,
-0.680423926896355));
#42121=CARTESIAN_POINT('Ctrl Pts',(-65.0691014002016,-4.90961318993959,
-0.455148249397773));
#42122=CARTESIAN_POINT('Ctrl Pts',(-65.080129937149,-4.92509615677833,-0.227649337766092));
#42123=CARTESIAN_POINT('Ctrl Pts',(-65.0911584740964,-4.92488160240034,
-0.000121459184743433));
#42124=CARTESIAN_POINT('Ctrl Pts',(-65.3088415259036,-4.92488488230248,
-0.000121706157415094));
#42125=CARTESIAN_POINT('Ctrl Pts',(-65.2978675685131,-4.92509904704324,
-0.226523131011731));
#42126=CARTESIAN_POINT('Ctrl Pts',(-65.2868936111227,-4.90976947097626,
-0.452895783772063));
#42127=CARTESIAN_POINT('Ctrl Pts',(-65.2759196537322,-4.87865663849641,
-0.677077977943223));
#42128=CARTESIAN_POINT('Ctrl Pts',(-65.2364089539822,-4.76663781622961,
-1.48422484830604));
#42129=CARTESIAN_POINT('Ctrl Pts',(-65.1968982542322,-4.45002187427182,
-2.26297697512404));
#42130=CARTESIAN_POINT('Ctrl Pts',(-65.1573875544821,-3.96703946931719,
-2.91930180581596));
#42131=CARTESIAN_POINT('Ctrl Pts',(-65.1178768547321,-3.48405706436252,
-3.57562663650791));
#42132=CARTESIAN_POINT('Ctrl Pts',(-65.0783661549821,-2.83470819641105,
-4.10952417107375));
#42133=CARTESIAN_POINT('Ctrl Pts',(-65.0388554552321,-2.09740026810914,
-4.45652749345232));
#42134=CARTESIAN_POINT('Ctrl Pts',(-64.999344755482,-1.3600923398073,-4.80353081583086));
#42135=CARTESIAN_POINT('Ctrl Pts',(-64.959834055732,-0.534825351155019,
-4.96363992602214));
#42136=CARTESIAN_POINT('Ctrl Pts',(-64.920323355982,0.278751581226722,-4.91752201220536));
#42137=CARTESIAN_POINT('Ctrl Pts',(-64.8808126562319,1.09232851360851,-4.87140409838858));
#42138=CARTESIAN_POINT('Ctrl Pts',(-64.8413019564819,1.89421538971978,-4.61905916056376));
#42139=CARTESIAN_POINT('Ctrl Pts',(-64.8017912567319,2.58758618848735,-4.19095727748569));
#42140=CARTESIAN_POINT('Ctrl Pts',(-64.7622805569819,3.28095698725492,-3.76285539440761));
#42141=CARTESIAN_POINT('Ctrl Pts',(-64.7227698572319,3.86581170867873,-3.15899656607628));
#42142=CARTESIAN_POINT('Ctrl Pts',(-64.6832591574818,4.27153047198954,-2.45229537605597));
#42143=CARTESIAN_POINT('Ctrl Pts',(-64.6437484577318,4.67724923530035,-1.74559418603566));
#42144=CARTESIAN_POINT('Ctrl Pts',(-64.6042377579817,4.90383204049817,-0.936050634326364));
#42145=CARTESIAN_POINT('Ctrl Pts',(-64.5647270582317,4.9239195278971,-0.12141526820937));
#42146=CARTESIAN_POINT('Ctrl Pts',(-64.5252163584817,4.94400701529602,0.693220097907579));
#42147=CARTESIAN_POINT('Ctrl Pts',(-64.4857056587317,4.75759918489606,1.51294727843224));
#42148=CARTESIAN_POINT('Ctrl Pts',(-64.4461949589816,4.38720435932008,2.23878607600718));
#42149=CARTESIAN_POINT('Ctrl Pts',(-64.4066842592316,4.01680953374406,2.96462487358218));
#42150=CARTESIAN_POINT('Ctrl Pts',(-64.3671735594815,3.46242771299201,3.59657528820741));
#42151=CARTESIAN_POINT('Ctrl Pts',(-64.3276628597315,2.79099924420997,4.05833074100424));
#42152=CARTESIAN_POINT('Ctrl Pts',(-64.2881521599815,2.11957077542799,4.52008619380104));
#42153=CARTESIAN_POINT('Ctrl Pts',(-64.2486414602315,1.33109565861598,4.81164668476946));
#42154=CARTESIAN_POINT('Ctrl Pts',(-64.2091307604815,0.520780475338853,
4.8978069460797));
#42155=CARTESIAN_POINT('Ctrl Pts',(-64.1696200607315,-0.289534707938324,
4.98396720738995));
#42156=CARTESIAN_POINT('Ctrl Pts',(-64.1301093609814,-1.12168995768064,
4.86472723904205));
#42157=CARTESIAN_POINT('Ctrl Pts',(-64.0905986612314,-1.87520441536793,
4.55448499669779));
#42158=CARTESIAN_POINT('Ctrl Pts',(-64.0510879614814,-2.62871887305523,
4.24424275435354));
#42159=CARTESIAN_POINT('Ctrl Pts',(-64.0115772617313,-3.30359253868746,
3.74299823801292));
#42160=CARTESIAN_POINT('Ctrl Pts',(-63.9720665619813,-3.81833594820552,
3.11127558586541));
#42161=CARTESIAN_POINT('Ctrl Pts',(-63.9325558622312,-4.33307935772359,
2.47955293371789));
#42162=CARTESIAN_POINT('Ctrl Pts',(-63.8930451624812,-4.6876925111275,1.71735214576347));
#42163=CARTESIAN_POINT('Ctrl Pts',(-63.8535344627312,-4.83935667464416,
0.916707237965155));
#42164=CARTESIAN_POINT('Ctrl Pts',(-63.838636817122,-4.89654217057262,0.614821314135713));
#42165=CARTESIAN_POINT('Ctrl Pts',(-63.8237391715128,-4.92487454999785,
0.307469816571031));
#42166=CARTESIAN_POINT('Ctrl Pts',(-63.8088415259036,-4.92468576593835,
8.39450088834838E-5));
#42167=CARTESIAN_POINT('Origin',(-74.75,0.,0.));
#42168=CARTESIAN_POINT('',(-62.0911584740964,-4.92540487062078,2.56800769940328E-5));
#42169=CARTESIAN_POINT('',(-62.3088415259036,-4.92540385667628,2.68226834623546E-5));
#42170=CARTESIAN_POINT('',(-74.75,-4.925,-6.03138548580071E-16));
#42171=CARTESIAN_POINT('Ctrl Pts',(-62.0911584740964,-4.92540487062078,
2.56800769940328E-5));
#42172=CARTESIAN_POINT('Ctrl Pts',(-62.0923624433983,-4.92541209039183,
0.0248569463254631));
#42173=CARTESIAN_POINT('Ctrl Pts',(-62.0935664127002,-4.9252281978348,0.0496881052786896));
#42174=CARTESIAN_POINT('Ctrl Pts',(-62.0947703820021,-4.92485252944502,
0.074516362533359));
#42175=CARTESIAN_POINT('Ctrl Pts',(-62.1342810817521,-4.91252420767574,
0.889306088618798));
#42176=CARTESIAN_POINT('Ctrl Pts',(-62.1737917815022,-4.69366144066925,
1.70097080831941));
#42177=CARTESIAN_POINT('Ctrl Pts',(-62.2133024812522,-4.29469141098677,
2.41150384813135));
#42178=CARTESIAN_POINT('Ctrl Pts',(-62.2528131810022,-3.89572138130432,
3.12203688794325));
#42179=CARTESIAN_POINT('Ctrl Pts',(-62.2923238807522,-3.31664408894592,
3.73143824786648));
#42180=CARTESIAN_POINT('Ctrl Pts',(-62.3318345805023,-2.62738180324177,
4.16612409622118));
#42181=CARTESIAN_POINT('Ctrl Pts',(-62.3713452802523,-1.9381195175376,4.60080994457588));
#42182=CARTESIAN_POINT('Ctrl Pts',(-62.4108559800023,-1.13867223848768,
4.86078028136204));
#42183=CARTESIAN_POINT('Ctrl Pts',(-62.4503666797523,-0.325571411348048,
4.91464427819981));
#42184=CARTESIAN_POINT('Ctrl Pts',(-62.4898773795024,0.487529415791584,
4.96850827503758));
#42185=CARTESIAN_POINT('Ctrl Pts',(-62.5293880792524,1.31428379102092,4.81626593192696));
#42186=CARTESIAN_POINT('Ctrl Pts',(-62.5688987790024,2.05486299916099,4.47630016641082));
#42187=CARTESIAN_POINT('Ctrl Pts',(-62.6084094787525,2.7954422073011,4.13633440089467));
#42188=CARTESIAN_POINT('Ctrl Pts',(-62.6479201785025,3.44984624835192,3.60864521297299));
#42189=CARTESIAN_POINT('Ctrl Pts',(-62.6874308782526,3.93905731898545,2.95694987493439));
#42190=CARTESIAN_POINT('Ctrl Pts',(-62.7269415780026,4.42826838961897,2.3052545368958));
#42191=CARTESIAN_POINT('Ctrl Pts',(-62.7664522777526,4.75228648983517,1.52955304874031));
#42192=CARTESIAN_POINT('Ctrl Pts',(-62.8059629775026,4.87198716912245,0.723509605351551));
#42193=CARTESIAN_POINT('Ctrl Pts',(-62.8454736772526,4.99168784840973,-0.0825338380371624));
#42194=CARTESIAN_POINT('Ctrl Pts',(-62.8849843770027,4.9070711067681,-0.918919236659191));
#42195=CARTESIAN_POINT('Ctrl Pts',(-62.9244950767527,4.62835422378369,-1.68465495111375));
#42196=CARTESIAN_POINT('Ctrl Pts',(-62.9640057765027,4.34963734079928,-2.45039066556833));
#42197=CARTESIAN_POINT('Ctrl Pts',(-63.0035164762527,3.87682031647208,-3.14547669585548));
#42198=CARTESIAN_POINT('Ctrl Pts',(-63.0430271760028,3.26699473382334,-3.68598298073927));
#42199=CARTESIAN_POINT('Ctrl Pts',(-63.0825378757528,2.65716915117458,-4.22648926562307));
#42200=CARTESIAN_POINT('Ctrl Pts',(-63.1220485755028,1.91033501020428,-4.61241580510349));
#42201=CARTESIAN_POINT('Ctrl Pts',(-63.1615592752529,1.11667083911405,-4.79716284507845));
#42202=CARTESIAN_POINT('Ctrl Pts',(-63.2010699750029,0.323006668023829,
-4.9819098850534));
#42203=CARTESIAN_POINT('Ctrl Pts',(-63.2405806747529,-0.5174875331863,-4.96547742552289));
#42204=CARTESIAN_POINT('Ctrl Pts',(-63.280091374503,-1.30332399652472,-4.74984964869538));
#42205=CARTESIAN_POINT('Ctrl Pts',(-63.319602074253,-2.0891604598631,-4.53422187186789));
#42206=CARTESIAN_POINT('Ctrl Pts',(-63.359112774003,-2.82033918532976,-4.11939877774343));
#42207=CARTESIAN_POINT('Ctrl Pts',(-63.398623473753,-3.40857200062825,-3.55546931384058));
#42208=CARTESIAN_POINT('Ctrl Pts',(-63.4381341735031,-3.99680481592679,
-2.99153984993768));
#42209=CARTESIAN_POINT('Ctrl Pts',(-63.4776448732531,-4.44209172105713,
-2.27850401625637));
#42210=CARTESIAN_POINT('Ctrl Pts',(-63.5171555730031,-4.69066533243408,
-1.50245927207026));
#42211=CARTESIAN_POINT('Ctrl Pts',(-63.5418232067009,-4.8458567826278,-1.01795285725689));
#42212=CARTESIAN_POINT('Ctrl Pts',(-63.5664908403987,-4.92437226805018,
-0.508886490698715));
#42213=CARTESIAN_POINT('Ctrl Pts',(-63.5911584740964,-4.92468790276689,
8.47132295976605E-5));
#42214=CARTESIAN_POINT('Ctrl Pts',(-63.8088415259036,-4.92468576593835,
8.39450088834838E-5));
#42215=CARTESIAN_POINT('Ctrl Pts',(-63.7842284717628,-4.92437386750827,
-0.507761743991617));
#42216=CARTESIAN_POINT('Ctrl Pts',(-63.7596154176219,-4.84621118799329,
-1.01570125954844));
#42217=CARTESIAN_POINT('Ctrl Pts',(-63.7350023634811,-4.69169472196826,
-1.49924174849018));
#42218=CARTESIAN_POINT('Ctrl Pts',(-63.6954916637311,-4.4436534321463,-2.27545679950503));
#42219=CARTESIAN_POINT('Ctrl Pts',(-63.6559809639811,-3.99885567887296,
-2.98879787389256));
#42220=CARTESIAN_POINT('Ctrl Pts',(-63.616470264231,-3.41100978175644,-3.55313065525637));
#42221=CARTESIAN_POINT('Ctrl Pts',(-63.576959564481,-2.8231638846399,-4.1174634366202));
#42222=CARTESIAN_POINT('Ctrl Pts',(-63.537448864731,-2.09226984368017,-4.5327879249603));
#42223=CARTESIAN_POINT('Ctrl Pts',(-63.4979381649809,-1.30658145616534,
-4.74895463054403));
#42224=CARTESIAN_POINT('Ctrl Pts',(-63.4584274652309,-0.520893068650557,
-4.96512133612775));
#42225=CARTESIAN_POINT('Ctrl Pts',(-63.4189167654809,0.31958966541932,-4.98213025895514));
#42226=CARTESIAN_POINT('Ctrl Pts',(-63.3794060657308,1.11338036268379,-4.79792761018242));
#42227=CARTESIAN_POINT('Ctrl Pts',(-63.3398953659808,1.90717105994831,-4.6137249614097));
#42228=CARTESIAN_POINT('Ctrl Pts',(-63.3003846662308,2.65426972040742,-4.22831074103685));
#42229=CARTESIAN_POINT('Ctrl Pts',(-63.2608739664808,3.26446587573142,-3.68822284179601));
#42230=CARTESIAN_POINT('Ctrl Pts',(-63.2213632667307,3.87466203105542,-3.14813494255516));
#42231=CARTESIAN_POINT('Ctrl Pts',(-63.1818525669807,4.34795568124431,-2.45337336444632));
#42232=CARTESIAN_POINT('Ctrl Pts',(-63.1423418672306,4.62719769178514,-1.68782899184099));
#42233=CARTESIAN_POINT('Ctrl Pts',(-63.1028311674806,4.90643970232597,-0.922284619235678));
#42234=CARTESIAN_POINT('Ctrl Pts',(-63.0633204677306,4.99163007321876,-0.0859574521338825));
#42235=CARTESIAN_POINT('Ctrl Pts',(-63.0238097679806,4.87248226044709,0.720167901387682));
#42236=CARTESIAN_POINT('Ctrl Pts',(-62.9842990682306,4.75333444767542,1.52629325490925));
#42237=CARTESIAN_POINT('Ctrl Pts',(-62.9447883684805,4.4298484512393,2.30221679485058));
#42238=CARTESIAN_POINT('Ctrl Pts',(-62.9052776687305,3.94108447132522,2.95424751407866));
#42239=CARTESIAN_POINT('Ctrl Pts',(-62.8657669689805,3.45232049141112,3.60627823330677));
#42240=CARTESIAN_POINT('Ctrl Pts',(-62.8262562692304,2.79827852801906,4.13441613182161));
#42241=CARTESIAN_POINT('Ctrl Pts',(-62.7867455694804,2.05793266442289,4.47488975654842));
#42242=CARTESIAN_POINT('Ctrl Pts',(-62.7472348697304,1.31758680082672,4.81536338127524));
#42243=CARTESIAN_POINT('Ctrl Pts',(-62.7077241699804,0.490937037026456,
4.96817273221402));
#42244=CARTESIAN_POINT('Ctrl Pts',(-62.6682134702303,-0.322200543395056,
4.91486642691301));
#42245=CARTESIAN_POINT('Ctrl Pts',(-62.6287027704803,-1.13533812381655,
4.86156012161199));
#42246=CARTESIAN_POINT('Ctrl Pts',(-62.5891920707303,-1.93496352085928,
4.60213816007118));
#42247=CARTESIAN_POINT('Ctrl Pts',(-62.5496813709802,-2.62452378191686,
4.16792515560365));
#42248=CARTESIAN_POINT('Ctrl Pts',(-62.5101706712302,-3.31408404297441,
3.73371215113613));
#42249=CARTESIAN_POINT('Ctrl Pts',(-62.4706599714801,-3.89357916804681,
3.1247081037419));
#42250=CARTESIAN_POINT('Ctrl Pts',(-62.4311492717301,-4.2930364354653,2.41444887051428));
#42251=CARTESIAN_POINT('Ctrl Pts',(-62.3916385719801,-4.69249370288381,
1.70418963728662));
#42252=CARTESIAN_POINT('Ctrl Pts',(-62.3521278722301,-4.91191311264837,
0.89267521822563));
#42253=CARTESIAN_POINT('Ctrl Pts',(-62.3126171724801,-4.92480026881991,
0.0778941383738648));
#42254=CARTESIAN_POINT('Ctrl Pts',(-62.3113586236212,-4.92521076814783,
0.0519406168031391));
#42255=CARTESIAN_POINT('Ctrl Pts',(-62.3101000747624,-4.92541171219871,
0.0259837807572669));
#42256=CARTESIAN_POINT('Ctrl Pts',(-62.3088415259036,-4.92540385667628,
2.68226834623546E-5));
#42257=CARTESIAN_POINT('Origin',(-74.75,0.,0.));
#42258=CARTESIAN_POINT('',(-60.5911584740964,-4.92480136718117,-0.000112186803593595));
#42259=CARTESIAN_POINT('',(-60.8088415259036,-4.92480425490107,-0.00011264726956837));
#42260=CARTESIAN_POINT('',(-74.75,-4.925,-6.03138548580071E-16));
#42261=CARTESIAN_POINT('Ctrl Pts',(-60.5911584740964,-4.92480136718117,
-0.000112186803593595));
#42262=CARTESIAN_POINT('Ctrl Pts',(-60.618234046398,-4.92432726268177,0.558505514510406));
#42263=CARTESIAN_POINT('Ctrl Pts',(-60.6453096186995,-4.82941391746452,
1.11728024600357));
#42264=CARTESIAN_POINT('Ctrl Pts',(-60.672385191001,-4.64306200662679,1.64368490447722));
#42265=CARTESIAN_POINT('Ctrl Pts',(-60.7118958907511,-4.37112336337482,
2.41185394542412));
#42266=CARTESIAN_POINT('Ctrl Pts',(-60.7514065905011,-3.90446786036597,
3.11109147015909));
#42267=CARTESIAN_POINT('Ctrl Pts',(-60.7909172902511,-3.29944296942331,
3.6569661345086));
#42268=CARTESIAN_POINT('Ctrl Pts',(-60.8304279900011,-2.69441807848069,
4.20284079885807));
#42269=CARTESIAN_POINT('Ctrl Pts',(-60.8699386897512,-1.9510237996043,4.59535260282208));
#42270=CARTESIAN_POINT('Ctrl Pts',(-60.9094493895012,-1.15902336576893,
4.78710663625474));
#42271=CARTESIAN_POINT('Ctrl Pts',(-60.9489600892512,-0.36702293193357,
4.97886066968739));
#42272=CARTESIAN_POINT('Ctrl Pts',(-60.9884707890012,0.473583656860748,
4.96985693258868));
#42273=CARTESIAN_POINT('Ctrl Pts',(-61.0279814887513,1.26129509202582,4.76118260593435));
#42274=CARTESIAN_POINT('Ctrl Pts',(-61.0674921885013,2.04900652719094,4.55250827928001));
#42275=CARTESIAN_POINT('Ctrl Pts',(-61.1070028882514,2.7838228087268,4.14416336307003));
#42276=CARTESIAN_POINT('Ctrl Pts',(-61.1465135880014,3.37701652282332,3.58545457946338));
#42277=CARTESIAN_POINT('Ctrl Pts',(-61.1860242877514,3.97021023691983,3.02674579585673));
#42278=CARTESIAN_POINT('Ctrl Pts',(-61.2255349875014,4.421781383577,2.31767314485344));
#42279=CARTESIAN_POINT('Ctrl Pts',(-61.2650456872515,4.67720377868587,1.54385554044626));
#42280=CARTESIAN_POINT('Ctrl Pts',(-61.3045563870015,4.93262617379475,0.770037936039061));
#42281=CARTESIAN_POINT('Ctrl Pts',(-61.3440670867516,4.99189981735533,-0.0685246217720721));
#42282=CARTESIAN_POINT('Ctrl Pts',(-61.3835777865016,4.84786754771377,-0.870577606571574));
#42283=CARTESIAN_POINT('Ctrl Pts',(-61.4230884862516,4.70383527807222,-1.67263059137105));
#42284=CARTESIAN_POINT('Ctrl Pts',(-61.4625991860016,4.35649709522856,-2.43817400315895));
#42285=CARTESIAN_POINT('Ctrl Pts',(-61.5021098857517,3.84779329858565,-3.07477021171873));
#42286=CARTESIAN_POINT('Ctrl Pts',(-61.5416205855017,3.3390895019428,-3.71136642027844));
#42287=CARTESIAN_POINT('Ctrl Pts',(-61.5811312852517,2.66902009150075,-4.21901542561004));
#42288=CARTESIAN_POINT('Ctrl Pts',(-61.6206419850017,1.91849442749971,-4.53641976201257));
#42289=CARTESIAN_POINT('Ctrl Pts',(-61.6601526847518,1.16796876349859,-4.85382409841514));
#42290=CARTESIAN_POINT('Ctrl Pts',(-61.6996633845018,0.336986845938493,
-4.98098376588859));
#42291=CARTESIAN_POINT('Ctrl Pts',(-61.7391740842518,-0.474112143410631,
-4.90254452306669));
#42292=CARTESIAN_POINT('Ctrl Pts',(-61.7786847840019,-1.28521113275975,
-4.82410528024479));
#42293=CARTESIAN_POINT('Ctrl Pts',(-61.8181954837519,-2.07642719389789,
-4.54006712712753));
#42294=CARTESIAN_POINT('Ctrl Pts',(-61.8577061835019,-2.75222278267403,
-4.08472702631593));
#42295=CARTESIAN_POINT('Ctrl Pts',(-61.8972168832519,-3.42801837145014,
-3.62938692550436));
#42296=CARTESIAN_POINT('Ctrl Pts',(-61.936727583002,-3.98839348786427,-3.00274487699847));
#42297=CARTESIAN_POINT('Ctrl Pts',(-61.976238282752,-4.3656841078053,-2.28046648651042));
#42298=CARTESIAN_POINT('Ctrl Pts',(-62.0145450132002,-4.73147793505032,
-1.58019734959341));
#42299=CARTESIAN_POINT('Ctrl Pts',(-62.0528517436483,-4.92517515893018,
-0.790031526007394));
#42300=CARTESIAN_POINT('Ctrl Pts',(-62.0911584740964,-4.92540487062078,
2.56800769940328E-5));
#42301=CARTESIAN_POINT('Ctrl Pts',(-62.3088415259036,-4.92540385667628,
2.68226834623546E-5));
#42302=CARTESIAN_POINT('Ctrl Pts',(-62.2705893750124,-4.92516509707053,
-0.788905184172106));
#42303=CARTESIAN_POINT('Ctrl Pts',(-62.2323372241212,-4.73204013316386,
-1.57794991883566));
#42304=CARTESIAN_POINT('Ctrl Pts',(-62.19408507323,-4.36724718275288,-2.27747167475169));
#42305=CARTESIAN_POINT('Ctrl Pts',(-62.15457437348,-3.99045203793583,-3.00000866738299));
#42306=CARTESIAN_POINT('Ctrl Pts',(-62.1150636737299,-3.43050684572326,
-3.62703491200312));
#42307=CARTESIAN_POINT('Ctrl Pts',(-62.0755529739799,-2.75502371774203,
-4.08283841209044));
#42308=CARTESIAN_POINT('Ctrl Pts',(-62.0360422742299,-2.0795405897608,-4.53864191217776));
#42309=CARTESIAN_POINT('Ctrl Pts',(-61.9965315744799,-1.28851952601091,
-4.82322266773226));
#42310=CARTESIAN_POINT('Ctrl Pts',(-61.9570208747298,-0.477474525377241,
-4.9022181981402));
#42311=CARTESIAN_POINT('Ctrl Pts',(-61.9175101749798,0.3335704752564,-4.98121372854814));
#42312=CARTESIAN_POINT('Ctrl Pts',(-61.8779994752297,1.16463941277381,-4.85462403380952));
#42313=CARTESIAN_POINT('Ctrl Pts',(-61.8384887754797,1.91538259839802,-4.53773453237479));
#42314=CARTESIAN_POINT('Ctrl Pts',(-61.7989780757297,2.66612578402223,-4.22084503094005));
#42315=CARTESIAN_POINT('Ctrl Pts',(-61.7594673759797,3.33654321775324,-3.71365572280919));
#42316=CARTESIAN_POINT('Ctrl Pts',(-61.7199566762296,3.84568351541099,-3.07740856629143));
#42317=CARTESIAN_POINT('Ctrl Pts',(-61.6804459764796,4.35482381306875,-2.44116140977365));
#42318=CARTESIAN_POINT('Ctrl Pts',(-61.6409352767296,4.70268697465325,-1.67585640486897));
#42319=CARTESIAN_POINT('Ctrl Pts',(-61.6014245769795,4.84726931261692,-0.873902394698959));
#42320=CARTESIAN_POINT('Ctrl Pts',(-61.5619138772295,4.99185165058058,-0.0719483845289988));
#42321=CARTESIAN_POINT('Ctrl Pts',(-61.5224031774795,4.93315316492343,0.76665463090628));
#42322=CARTESIAN_POINT('Ctrl Pts',(-61.4828924777295,4.67826156456697,1.54064724001566));
#42323=CARTESIAN_POINT('Ctrl Pts',(-61.4433817779794,4.42336996421049,2.3146398491251));
#42324=CARTESIAN_POINT('Ctrl Pts',(-61.4038710782294,3.97228524915466,3.02402205190863));
#42325=CARTESIAN_POINT('Ctrl Pts',(-61.3643603784794,3.37947487548879,3.5831375567173));
#42326=CARTESIAN_POINT('Ctrl Pts',(-61.3248496787293,2.78666450182296,4.14225306152595));
#42327=CARTESIAN_POINT('Ctrl Pts',(-61.2853389789793,2.05212846954711,4.55110186835976));
#42328=CARTESIAN_POINT('Ctrl Pts',(-61.2458282792293,1.26456033791886,4.76031641137174));
#42329=CARTESIAN_POINT('Ctrl Pts',(-61.2063175794793,0.476992206290612,
4.96953095438371));
#42330=CARTESIAN_POINT('Ctrl Pts',(-61.1668068797292,-0.363608024690031,
4.97911123357385));
#42331=CARTESIAN_POINT('Ctrl Pts',(-61.1272961799792,-1.15573978373521,
4.78790045189409));
#42332=CARTESIAN_POINT('Ctrl Pts',(-61.0877854802292,-1.94787154278039,
4.59668967021432));
#42333=CARTESIAN_POINT('Ctrl Pts',(-61.0482747804792,-2.6915348298901,4.20468782766466));
#42334=CARTESIAN_POINT('Ctrl Pts',(-61.0087640807291,-3.29693399116305,
3.65922825755163));
#42335=CARTESIAN_POINT('Ctrl Pts',(-60.9692533809791,-3.90233315243601,
3.11376868743858));
#42336=CARTESIAN_POINT('Ctrl Pts',(-60.9297426812291,-4.36946818787219,
2.41485138976216));
#42337=CARTESIAN_POINT('Ctrl Pts',(-60.890231981479,-4.64193359992515,1.64686904231828));
#42338=CARTESIAN_POINT('Ctrl Pts',(-60.8631018296205,-4.82902287072889,
1.11953143902096));
#42339=CARTESIAN_POINT('Ctrl Pts',(-60.8359716777621,-4.9243268280576,0.559630166400692));
#42340=CARTESIAN_POINT('Ctrl Pts',(-60.8088415259036,-4.92480425490107,
-0.00011264726956837));
#42341=CARTESIAN_POINT('Origin',(-74.75,0.,0.));
#42342=CARTESIAN_POINT('',(-59.25,-4.925,-6.03138548580071E-16));
#42343=CARTESIAN_POINT('',(-59.3088415259036,-4.92475008045824,0.000102229393649578));
#42344=CARTESIAN_POINT('',(-74.75,-4.925,-6.03138548580071E-16));
#42345=CARTESIAN_POINT('',(-59.25,-3.87448963569914,3.04038732119116));
#42346=CARTESIAN_POINT('Origin',(-59.25,0.,0.));
#42347=CARTESIAN_POINT('Ctrl Pts',(-59.25,-3.87448963569905,3.04038732119127));
#42348=CARTESIAN_POINT('Ctrl Pts',(-59.2895106997501,-3.37129935567942,
3.68162322923889));
#42349=CARTESIAN_POINT('Ctrl Pts',(-59.3290213995001,-2.70610538505704,
4.19521969019135));
#42350=CARTESIAN_POINT('Ctrl Pts',(-59.3685320992501,-1.95853021177386,
4.51926688453211));
#42351=CARTESIAN_POINT('Ctrl Pts',(-59.4080427990001,-1.21095503849063,
4.84331407887289));
#42352=CARTESIAN_POINT('Ctrl Pts',(-59.4475534987502,-0.38099866254657,
4.97781200660196));
#42353=CARTESIAN_POINT('Ctrl Pts',(-59.4870641985002,0.430795782907827,
4.90654364883144));
#42354=CARTESIAN_POINT('Ctrl Pts',(-59.5265748982502,1.24259022836218,4.83527529106094));
#42355=CARTESIAN_POINT('Ctrl Pts',(-59.5660855980002,2.03622274332688,4.55824064779087));
#42356=CARTESIAN_POINT('Ctrl Pts',(-59.6055962977503,2.71600019639951,4.10889083869069));
#42357=CARTESIAN_POINT('Ctrl Pts',(-59.6451069975003,3.39577764947222,3.65954102959046));
#42358=CARTESIAN_POINT('Ctrl Pts',(-59.6846176972503,3.96170004065284,3.03787605466006));
#42359=CARTESIAN_POINT('Ctrl Pts',(-59.7241283970004,4.3453670671339,2.31896030760023));
#42360=CARTESIAN_POINT('Ctrl Pts',(-59.7636390967504,4.72903409361491,1.60004456054048));
#42361=CARTESIAN_POINT('Ctrl Pts',(-59.8031497965004,4.93044575539642,0.783878041351297));
#42362=CARTESIAN_POINT('Ctrl Pts',(-59.8426604962504,4.9253149473138,-0.0309888376303113));
#42363=CARTESIAN_POINT('Ctrl Pts',(-59.8821711960004,4.92018413923118,-0.845855716611944));
#42364=CARTESIAN_POINT('Ctrl Pts',(-59.9216818957505,4.70851086128444,-1.65942295538596));
#42365=CARTESIAN_POINT('Ctrl Pts',(-59.9611925955005,4.31583785436935,-2.37345423564581));
#42366=CARTESIAN_POINT('Ctrl Pts',(-60.0007032952506,3.92316484745423,-3.08748551590572));
#42367=CARTESIAN_POINT('Ctrl Pts',(-60.0402139950006,3.34949211157074,-3.7019808376514));
#42368=CARTESIAN_POINT('Ctrl Pts',(-60.0797246947506,2.66409743455116,-4.14274124495021));
#42369=CARTESIAN_POINT('Ctrl Pts',(-60.1192353945006,1.97870275753165,-4.58350165224898));
#42370=CARTESIAN_POINT('Ctrl Pts',(-60.1587460942507,1.18158613937606,-4.85052714510093));
#42371=CARTESIAN_POINT('Ctrl Pts',(-60.1982567940007,0.36899357827524,-4.91157502086969));
#42372=CARTESIAN_POINT('Ctrl Pts',(-60.2377674937508,-0.443598982825585,
-4.97262289663845));
#42373=CARTESIAN_POINT('Ctrl Pts',(-60.2772781935008,-1.27166748687167,
-4.82769315532402));
#42374=CARTESIAN_POINT('Ctrl Pts',(-60.3167888932508,-2.01522254205752,
-4.49428572454397));
#42375=CARTESIAN_POINT('Ctrl Pts',(-60.3562995930008,-2.75877759724342,
-4.16087829376391));
#42376=CARTESIAN_POINT('Ctrl Pts',(-60.3958102927509,-3.41781920356909,
-3.63899317351821));
#42377=CARTESIAN_POINT('Ctrl Pts',(-60.4353209925009,-3.91277057456095,
-2.99164681298116));
#42378=CARTESIAN_POINT('Ctrl Pts',(-60.4748316922509,-4.40772194555281,
-2.34430045244411));
#42379=CARTESIAN_POINT('Ctrl Pts',(-60.5143423920009,-4.73858308121087,
-1.57149285161571));
#42380=CARTESIAN_POINT('Ctrl Pts',(-60.553853091751,-4.86540275729235,-0.766538772622105));
#42381=CARTESIAN_POINT('Ctrl Pts',(-60.5662882191994,-4.90531647294471,
-0.51319710502857));
#42382=CARTESIAN_POINT('Ctrl Pts',(-60.5787233466479,-4.92501911141971,
-0.256671207364706));
#42383=CARTESIAN_POINT('Ctrl Pts',(-60.5911584740964,-4.92480136718117,
-0.000112186803593595));
#42384=CARTESIAN_POINT('Ctrl Pts',(-60.8088415259036,-4.92480425490107,
-0.00011264726956837));
#42385=CARTESIAN_POINT('Ctrl Pts',(-60.7964609780121,-4.92502212341619,
-0.255545154531168));
#42386=CARTESIAN_POINT('Ctrl Pts',(-60.7840804301205,-4.90549280940482,
-0.510944663455777));
#42387=CARTESIAN_POINT('Ctrl Pts',(-60.771699882229,-4.86592730455705,-0.763201574512367));
#42388=CARTESIAN_POINT('Ctrl Pts',(-60.7321891824789,-4.73965980846626,
-1.5682424466878));
#42389=CARTESIAN_POINT('Ctrl Pts',(-60.6926784827289,-4.40932902761496,
-2.34127679382733));
#42390=CARTESIAN_POINT('Ctrl Pts',(-60.6531677829788,-3.9148216471047,-2.98896247343204));
#42391=CARTESIAN_POINT('Ctrl Pts',(-60.6136570832288,-3.42031426659448,
-3.63664815303671));
#42392=CARTESIAN_POINT('Ctrl Pts',(-60.5741463834788,-2.76163028642532,
-4.15898516510658));
#42393=CARTESIAN_POINT('Ctrl Pts',(-60.5346356837288,-2.01830431751824,
-4.49290249811251));
#42394=CARTESIAN_POINT('Ctrl Pts',(-60.4951249839787,-1.27497834861111,
-4.82681983111845));
#42395=CARTESIAN_POINT('Ctrl Pts',(-60.4556142842287,-0.447010390966045,
-4.97231748506042));
#42396=CARTESIAN_POINT('Ctrl Pts',(-60.4161035844787,0.365624332431433,
-4.91182695300899));
#42397=CARTESIAN_POINT('Ctrl Pts',(-60.3765928847287,1.17825905582891,-4.85133642095756));
#42398=CARTESIAN_POINT('Ctrl Pts',(-60.3370821849786,1.9755605449788,-4.58485770291274));
#42399=CARTESIAN_POINT('Ctrl Pts',(-60.2975714852286,2.6612563944335,-4.14456749006351));
#42400=CARTESIAN_POINT('Ctrl Pts',(-60.2580607854786,3.34695224388815,-3.7042772772143));
#42401=CARTESIAN_POINT('Ctrl Pts',(-60.2185500857286,3.92104245364762,-3.09017556956071));
#42402=CARTESIAN_POINT('Ctrl Pts',(-60.1790393859785,4.31420705304533,-2.37641377416709));
#42403=CARTESIAN_POINT('Ctrl Pts',(-60.1395286862285,4.70737165244309,-1.66265197877339));
#42404=CARTESIAN_POINT('Ctrl Pts',(-60.1000179864784,4.91961064147904,-0.849230095639638));
#42405=CARTESIAN_POINT('Ctrl Pts',(-60.0605072867284,4.92529640254283,-0.0343669333774221));
#42406=CARTESIAN_POINT('Ctrl Pts',(-60.0209965869784,4.93098216360662,0.780496228884701));
#42407=CARTESIAN_POINT('Ctrl Pts',(-59.9814858872283,4.7301146966983,1.59680067027529));
#42408=CARTESIAN_POINT('Ctrl Pts',(-59.9419751874783,4.34694877854636,2.31597940409487));
#42409=CARTESIAN_POINT('Ctrl Pts',(-59.9024644877283,3.96378286039443,3.03515813791445));
#42410=CARTESIAN_POINT('Ctrl Pts',(-59.8629537879783,3.39831849099889,3.65721116416303));
#42411=CARTESIAN_POINT('Ctrl Pts',(-59.8234430882283,2.71883323159572,4.10702714690975));
#42412=CARTESIAN_POINT('Ctrl Pts',(-59.7839323884782,2.03934797219251,4.55684312965649));
#42413=CARTESIAN_POINT('Ctrl Pts',(-59.7444216887282,1.24584182278165,4.83442206890134));
#42414=CARTESIAN_POINT('Ctrl Pts',(-59.7049109889781,0.43413082165801,4.90624662373847));
#42415=CARTESIAN_POINT('Ctrl Pts',(-59.6654002892281,-0.37758017946563,
4.97807117857561));
#42416=CARTESIAN_POINT('Ctrl Pts',(-59.6258895894781,-1.20749603230206,
4.84414134900504));
#42417=CARTESIAN_POINT('Ctrl Pts',(-59.5863788897281,-1.95541025039442,
4.52062949002602));
#42418=CARTESIAN_POINT('Ctrl Pts',(-59.5468681899781,-2.70332446848675,
4.19711763104702));
#42419=CARTESIAN_POINT('Ctrl Pts',(-59.507357490228,-3.36923705183502,3.6840237426596));
#42420=CARTESIAN_POINT('Ctrl Pts',(-59.467846790478,-3.87273257024307,3.0433014749766));
#42421=CARTESIAN_POINT('Ctrl Pts',(-59.428336090728,-4.37622808865111,2.40257920729359));
#42422=CARTESIAN_POINT('Ctrl Pts',(-59.3888253909779,-4.71730654211892,
1.634228560315));
#42423=CARTESIAN_POINT('Ctrl Pts',(-59.3493146912279,-4.85479958887199,
0.831028695869623));
#42424=CARTESIAN_POINT('Ctrl Pts',(-59.3358236361198,-4.90174703051343,
0.556773526950549));
#42425=CARTESIAN_POINT('Ctrl Pts',(-59.3223325810117,-4.92495839013675,
0.278455277590655));
#42426=CARTESIAN_POINT('Ctrl Pts',(-59.3088415259036,-4.92475008045824,
0.000102229393649578));
#42427=CARTESIAN_POINT('Origin',(-92.3478126690739,0.,0.));
#42428=CARTESIAN_POINT('',(-60.0978126690739,-4.07033583047938,-9.27221085090139E-5));
#42429=CARTESIAN_POINT('',(-59.8021873309261,-4.07029344213305,8.44923339615722E-5));
#42430=CARTESIAN_POINT('',(-92.3478126690739,-4.0705,-4.39132641279065E-13));
#42431=CARTESIAN_POINT('',(-59.25,3.73370339826928,1.62162243917742));
#42432=CARTESIAN_POINT('Ctrl Pts',(-60.0978126690739,-4.07033583047938,
-9.27221085087783E-5));
#42433=CARTESIAN_POINT('Ctrl Pts',(-60.0853775416254,-4.07051579553988,
-0.212138101437242));
#42434=CARTESIAN_POINT('Ctrl Pts',(-60.0334317144269,-4.00249114200519,
-1.09781061344082));
#42435=CARTESIAN_POINT('Ctrl Pts',(-59.9419751874784,-3.36951511201551,
-2.57628189458803));
#42436=CARTESIAN_POINT('Ctrl Pts',(-59.8234430882282,-1.73542646721431,
-3.87029207649262));
#42437=CARTESIAN_POINT('Ctrl Pts',(-59.7049109889782,0.317763083477844,
-4.22964426655577));
#42438=CARTESIAN_POINT('Ctrl Pts',(-59.586378889728,2.29420766877876,-3.56755659021834));
#42439=CARTESIAN_POINT('Ctrl Pts',(-59.4678467904781,3.71662484933523,-2.04392011884845));
#42440=CARTESIAN_POINT('Ctrl Pts',(-59.3557204939019,4.21310320094652,-0.135703240697654));
#42441=CARTESIAN_POINT('Ctrl Pts',(-59.283104897076,3.95802532033354,1.10373061144362));
#42442=CARTESIAN_POINT('Ctrl Pts',(-59.25,3.73370339826928,1.62162243917742));
#42443=CARTESIAN_POINT('',(-59.25,2.75129702511905,-2.99988915288066));
#42444=CARTESIAN_POINT('Origin',(-59.25,0.,0.));
#42445=CARTESIAN_POINT('Ctrl Pts',(-59.8021873309261,-4.07029344213305,
8.44923339619191E-5));
#42446=CARTESIAN_POINT('Ctrl Pts',(-59.7761676862842,-4.0699613898905,-0.443619105718286));
#42447=CARTESIAN_POINT('Ctrl Pts',(-59.7106373418922,-3.88779319744078,
-1.56135382729816));
#42448=CARTESIAN_POINT('Ctrl Pts',(-59.6055962977503,-2.88282865866802,
-3.11125693021052));
#42449=CARTESIAN_POINT('Ctrl Pts',(-59.4870641985001,-1.05281798849905,
-4.10883397176923));
#42450=CARTESIAN_POINT('Ctrl Pts',(-59.3685320992501,1.03189169588001,-4.11422147186713));
#42451=CARTESIAN_POINT('Ctrl Pts',(-59.28951069975,2.25480927425104,-3.45523440144076));
#42452=CARTESIAN_POINT('Ctrl Pts',(-59.25,2.75129702511905,-2.99988915288066));
#42453=CARTESIAN_POINT('Origin',(-92.3478126690739,0.,0.));
#42454=CARTESIAN_POINT('',(-61.5978126690739,-4.07083462454048,2.1224518266207E-5));
#42455=CARTESIAN_POINT('',(-61.3021873309261,-4.07033821717255,-9.31026831621495E-5));
#42456=CARTESIAN_POINT('',(-92.3478126690739,-4.0705,-4.39132641279065E-13));
#42457=CARTESIAN_POINT('Ctrl Pts',(-61.5978126690739,-4.07083462454048,
2.12245182661715E-5));
#42458=CARTESIAN_POINT('Ctrl Pts',(-61.5595059386257,-4.0706447684112,-0.652959051089105));
#42459=CARTESIAN_POINT('Ctrl Pts',(-61.4816885084275,-3.74543265053492,
-1.97962494652396));
#42460=CARTESIAN_POINT('Ctrl Pts',(-61.3643603784794,-2.3700998720048,-3.51759714491556));
#42461=CARTESIAN_POINT('Ctrl Pts',(-61.2458282792293,-0.408285672900589,
-4.22186758284269));
#42462=CARTESIAN_POINT('Ctrl Pts',(-61.1272961799792,1.65212766441617,-3.90657615556305));
#42463=CARTESIAN_POINT('Ctrl Pts',(-61.0087640807291,3.31355966555602,-2.64786431219091));
#42464=CARTESIAN_POINT('Ctrl Pts',(-60.8902319814791,4.1747820452098,-0.749705251673546));
#42465=CARTESIAN_POINT('Ctrl Pts',(-60.7716998822289,4.02781349732346,1.32950422542484));
#42466=CARTESIAN_POINT('Ctrl Pts',(-60.6531677829789,2.90814627754596,3.08764446455717));
#42467=CARTESIAN_POINT('Ctrl Pts',(-60.5346356837287,1.08617490252564,4.10013257507453));
#42468=CARTESIAN_POINT('Ctrl Pts',(-60.4161035844787,-0.998102733832139,
4.12245727265436));
#42469=CARTESIAN_POINT('Ctrl Pts',(-60.2975714852285,-2.84134318794365,
3.14922724339409));
#42470=CARTESIAN_POINT('Ctrl Pts',(-60.191474513427,-3.87702460308865,1.59736017128054));
#42471=CARTESIAN_POINT('Ctrl Pts',(-60.1248882413754,-4.06994398431395,
0.461603390216087));
#42472=CARTESIAN_POINT('Ctrl Pts',(-60.0978126690739,-4.07033583047938,
-9.27221085087783E-5));
#42473=CARTESIAN_POINT('Ctrl Pts',(-61.3021873309261,-4.07033821717255,
-9.31026831620455E-5));
#42474=CARTESIAN_POINT('Ctrl Pts',(-61.2898067830346,-4.07051828494729,
-0.211207421628787));
#42475=CARTESIAN_POINT('Ctrl Pts',(-61.237915535393,-4.0028659545813,-1.09594776340383));
#42476=CARTESIAN_POINT('Ctrl Pts',(-61.1465135880014,-3.3712816981627,-2.57397025366613));
#42477=CARTESIAN_POINT('Ctrl Pts',(-61.0279814887513,-1.73807978469344,
-3.86910089790803));
#42478=CARTESIAN_POINT('Ctrl Pts',(-60.9094493895012,0.314860461962913,
-4.22986122300694));
#42479=CARTESIAN_POINT('Ctrl Pts',(-60.7909172902512,2.29176343348649,-3.56912927064055));
#42480=CARTESIAN_POINT('Ctrl Pts',(-60.672385191001,3.71521573733988,-2.04646876241471));
#42481=CARTESIAN_POINT('Ctrl Pts',(-60.553853091751,4.24146069462157,-0.0295953967523683));
#42482=CARTESIAN_POINT('Ctrl Pts',(-60.4353209925008,3.74341133987005,1.99442525015962));
#42483=CARTESIAN_POINT('Ctrl Pts',(-60.3167888932508,2.34134674152,3.53680099229865));
#42484=CARTESIAN_POINT('Ctrl Pts',(-60.1982567940007,0.373854285980798,
4.22505585861098));
#42485=CARTESIAN_POINT('Ctrl Pts',(-60.0797246947506,-1.68391575197083,
3.89297786596098));
#42486=CARTESIAN_POINT('Ctrl Pts',(-59.9611925955005,-3.33504093198254,
2.62076547651056));
#42487=CARTESIAN_POINT('Ctrl Pts',(-59.8686801408924,-3.99509770559378,
1.13384936119896));
#42488=CARTESIAN_POINT('Ctrl Pts',(-59.8156783860342,-4.07046560955365,
0.230142580189046));
#42489=CARTESIAN_POINT('Ctrl Pts',(-59.8021873309261,-4.07029344213305,
8.44923339619191E-5));
#42490=CARTESIAN_POINT('Origin',(-92.3478126690739,0.,0.));
#42491=CARTESIAN_POINT('',(-63.0978126690739,-4.07024205242896,7.0015268888928E-5));
#42492=CARTESIAN_POINT('',(-62.8021873309261,-4.07083378651793,2.21688792080826E-5));
#42493=CARTESIAN_POINT('',(-92.3478126690739,-4.0705,-4.39132641279065E-13));
#42494=CARTESIAN_POINT('Ctrl Pts',(-63.0978126690739,-4.07024205242896,
7.00152688889316E-5));
#42495=CARTESIAN_POINT('Ctrl Pts',(-63.0731450353761,-4.06998118113666,
-0.420593392972697));
#42496=CARTESIAN_POINT('Ctrl Pts',(-63.0089667019283,-3.90114800565978,
-1.51524740589905));
#42497=CARTESIAN_POINT('Ctrl Pts',(-62.9052776687305,-2.93532053926837,
-3.06182240003477));
#42498=CARTESIAN_POINT('Ctrl Pts',(-62.7867455694804,-1.12236845682437,
-4.09037310336489));
#42499=CARTESIAN_POINT('Ctrl Pts',(-62.6682134702303,0.961630515374074,
-4.13111726165049));
#42500=CARTESIAN_POINT('Ctrl Pts',(-62.5496813709802,2.81340008135553,-3.17421534553572));
#42501=CARTESIAN_POINT('Ctrl Pts',(-62.4311492717302,3.98574629304517,-1.4507548259719));
#42502=CARTESIAN_POINT('Ctrl Pts',(-62.31261717248,4.19555285965564,0.623056401494609));
#42503=CARTESIAN_POINT('Ctrl Pts',(-62.19408507323,3.39215244731244,2.5464023350196));
#42504=CARTESIAN_POINT('Ctrl Pts',(-62.0755529739799,1.7695626102988,3.85480365853339));
#42505=CARTESIAN_POINT('Ctrl Pts',(-61.9570208747298,-0.280368567998288,
4.23228738907051));
#42506=CARTESIAN_POINT('Ctrl Pts',(-61.8384887754797,-2.26259200924054,
3.58769291847877));
#42507=CARTESIAN_POINT('Ctrl Pts',(-61.7199566762296,-3.69840974642527,
2.07668688666092));
#42508=CARTESIAN_POINT('Ctrl Pts',(-61.6397313074277,-4.06570085141387,
0.714567436849348));
#42509=CARTESIAN_POINT('Ctrl Pts',(-61.5990166383758,-4.07084059166293,
0.0205442030491459));
#42510=CARTESIAN_POINT('Ctrl Pts',(-61.5978126690739,-4.07083462454048,
2.12245182661715E-5));
#42511=CARTESIAN_POINT('Ctrl Pts',(-62.8021873309261,-4.07083378651793,
2.21688792079568E-5));
#42512=CARTESIAN_POINT('Ctrl Pts',(-62.7639351800349,-4.07063645230967,
-0.652028132421247));
#42513=CARTESIAN_POINT('Ctrl Pts',(-62.6861723293937,-3.74615023682731,
-1.97777149888163));
#42514=CARTESIAN_POINT('Ctrl Pts',(-62.5688987790024,-2.37251192093704,
-3.51597074883963));
#42515=CARTESIAN_POINT('Ctrl Pts',(-62.4503666797524,-0.411181216372217,
-4.22158656537844));
#42516=CARTESIAN_POINT('Ctrl Pts',(-62.3318345805023,1.64944788626615,-3.90770838115492));
#42517=CARTESIAN_POINT('Ctrl Pts',(-62.2133024812522,3.3117428085009,-2.65013635349193));
#42518=CARTESIAN_POINT('Ctrl Pts',(-62.0947703820021,4.17426686894535,-0.752568421026256));
#42519=CARTESIAN_POINT('Ctrl Pts',(-61.976238282752,4.02872442070117,1.32674137044345));
#42520=CARTESIAN_POINT('Ctrl Pts',(-61.8577061835019,2.91026330437545,3.08564914085777));
#42521=CARTESIAN_POINT('Ctrl Pts',(-61.7391740842519,1.08898680526139,4.09938664434021));
#42522=CARTESIAN_POINT('Ctrl Pts',(-61.6206419850017,-0.995275066945756,
4.12314087364582));
#42523=CARTESIAN_POINT('Ctrl Pts',(-61.5021098857517,-2.83918252492348,
3.15117528982951));
#42524=CARTESIAN_POINT('Ctrl Pts',(-61.3959583343931,-3.87646153412254,
1.5992209574618));
#42525=CARTESIAN_POINT('Ctrl Pts',(-61.3293174827846,-4.06994362509825,
0.4625329121485));
#42526=CARTESIAN_POINT('Ctrl Pts',(-61.3021873309261,-4.07033821717255,
-9.31026831620455E-5));
#42527=CARTESIAN_POINT('Origin',(-92.3478126690739,0.,0.));
#42528=CARTESIAN_POINT('',(-64.5978126690739,-4.07040214468438,-0.000100385708283945));
#42529=CARTESIAN_POINT('',(-64.3021873309261,-4.0702402863456,6.93803360128642E-5));
#42530=CARTESIAN_POINT('',(-92.3478126690739,-4.0705,-4.39132641279065E-13));
#42531=CARTESIAN_POINT('Ctrl Pts',(-64.5978126690739,-4.07040214468438,
-0.000100385708283902));
#42532=CARTESIAN_POINT('Ctrl Pts',(-64.5867841321265,-4.07057947333322,
-0.188151599873747));
#42533=CARTESIAN_POINT('Ctrl Pts',(-64.536244895429,-4.01193778252147,-1.04980305045492));
#42534=CARTESIAN_POINT('Ctrl Pts',(-64.4461949589816,-3.41452444788805,
-2.51632388066006));
#42535=CARTESIAN_POINT('Ctrl Pts',(-64.3276628597316,-1.80356130768488,
-3.83901415561695));
#42536=CARTESIAN_POINT('Ctrl Pts',(-64.2091307604814,0.242953704951307,
-4.23459993090915));
#42537=CARTESIAN_POINT('Ctrl Pts',(-64.0905986612314,2.23079650020559,-3.60754903671119));
#42538=CARTESIAN_POINT('Ctrl Pts',(-63.9720665619813,3.67991206254491,-2.10929141882807));
#42539=CARTESIAN_POINT('Ctrl Pts',(-63.8535344627312,4.24034555879598,-0.101649493872672));
#42540=CARTESIAN_POINT('Ctrl Pts',(-63.7350023634811,3.77675484249208,1.93054032263455));
#42541=CARTESIAN_POINT('Ctrl Pts',(-63.6164702642311,2.40109496815141,3.49651341074552));
#42542=CARTESIAN_POINT('Ctrl Pts',(-63.4979381649809,0.445581553589111,
4.21809437503554));
#42543=CARTESIAN_POINT('Ctrl Pts',(-63.3794060657309,-1.61753778440945,
3.92102468668754));
#42544=CARTESIAN_POINT('Ctrl Pts',(-63.2608739664807,-3.29002908679384,
2.67704532753104));
#42545=CARTESIAN_POINT('Ctrl Pts',(-63.1670095009284,-3.98528076530966,
1.17999684215322));
#42546=CARTESIAN_POINT('Ctrl Pts',(-63.1126557351261,-4.07039902451109,
0.253192581900508));
#42547=CARTESIAN_POINT('Ctrl Pts',(-63.0978126690739,-4.07024205242896,
7.00152688889316E-5));
#42548=CARTESIAN_POINT('Ctrl Pts',(-64.3021873309261,-4.0702402863456,6.93803360126907E-5));
#42549=CARTESIAN_POINT('Ctrl Pts',(-64.2775742767853,-4.06998250308468,
-0.419663792674221));
#42550=CARTESIAN_POINT('Ctrl Pts',(-64.2134505228944,-3.90167851966751,
-1.51338581363879));
#42551=CARTESIAN_POINT('Ctrl Pts',(-64.1098160692536,-2.93741985505644,
-3.05980844446182));
#42552=CARTESIAN_POINT('Ctrl Pts',(-63.9912839700035,-1.12517364567985,
-4.08960235093184));
#42553=CARTESIAN_POINT('Ctrl Pts',(-63.8727518707534,0.95879689383177,-4.13177584557272));
#42554=CARTESIAN_POINT('Ctrl Pts',(-63.7542197715033,2.81122233387158,-3.17614422078426));
#42555=CARTESIAN_POINT('Ctrl Pts',(-63.6356876722533,3.98475033575612,-1.45348817792618));
#42556=CARTESIAN_POINT('Ctrl Pts',(-63.5171555730031,4.1959792117271,0.620178664929396));
#42557=CARTESIAN_POINT('Ctrl Pts',(-63.3986234737531,3.39389814665504,2.54407517416668));
#42558=CARTESIAN_POINT('Ctrl Pts',(-63.2800913745029,1.77220607843935,3.85358907217963));
#42559=CARTESIAN_POINT('Ctrl Pts',(-63.1615592752529,-0.277465716615854,
4.23247869430933));
#42560=CARTESIAN_POINT('Ctrl Pts',(-63.0430271760028,-2.26013080006508,
3.58924391596298));
#42561=CARTESIAN_POINT('Ctrl Pts',(-62.9244950767527,-3.69698455028266,
2.07922301753555));
#42562=CARTESIAN_POINT('Ctrl Pts',(-62.8442151283938,-4.06546031589444,
0.716429282973149));
#42563=CARTESIAN_POINT('Ctrl Pts',(-62.803445879785,-4.07084027908729,0.0214755288467767));
#42564=CARTESIAN_POINT('Ctrl Pts',(-62.8021873309261,-4.07083378651793,
2.21688792079568E-5));
#42565=CARTESIAN_POINT('Origin',(-92.3478126690739,0.,0.));
#42566=CARTESIAN_POINT('',(-66.0978126690738,-4.0708029246806,4.46106111926773E-5));
#42567=CARTESIAN_POINT('',(-65.8021873309261,-4.07040485551518,-0.000100589830685782));
#42568=CARTESIAN_POINT('',(-92.3478126690739,-4.0705,-4.39132641279065E-13));
#42569=CARTESIAN_POINT('Ctrl Pts',(-66.0978126690738,-4.0708029246806,4.46106111927618E-5));
#42570=CARTESIAN_POINT('Ctrl Pts',(-66.0609125291268,-4.07044906963106,
-0.628973034888802));
#42571=CARTESIAN_POINT('Ctrl Pts',(-65.9845016894298,-3.76367733983292,
-1.93184242303918));
#42572=CARTESIAN_POINT('Ctrl Pts',(-65.8685801499826,-2.43190252088865,
-3.47515657294758));
#42573=CARTESIAN_POINT('Ctrl Pts',(-65.7500480507326,-0.482842631226866,
-4.21399170277722));
#42574=CARTESIAN_POINT('Ctrl Pts',(-65.6315159514825,1.58282156305449,-3.93516695670401));
#42575=CARTESIAN_POINT('Ctrl Pts',(-65.5129838522324,3.26624153165954,-2.70601724578163));
#42576=CARTESIAN_POINT('Ctrl Pts',(-65.3944517529823,4.16087899042085,-0.823376648126326));
#42577=CARTESIAN_POINT('Ctrl Pts',(-65.2759196537323,4.05068305232286,1.25810567411077));
#42578=CARTESIAN_POINT('Ctrl Pts',(-65.1573875544821,2.96226553641969,3.03576118450472));
#42579=CARTESIAN_POINT('Ctrl Pts',(-65.0388554552321,1.1584743342804,4.08029414312485));
#42580=CARTESIAN_POINT('Ctrl Pts',(-64.9203233559819,-0.925083163194395,
4.13945457986673));
#42581=CARTESIAN_POINT('Ctrl Pts',(-64.8017912567319,-2.78523727417561,
3.19895551768826));
#42582=CARTESIAN_POINT('Ctrl Pts',(-64.6942876944292,-3.8622781385591,1.64530822478956));
#42583=CARTESIAN_POINT('Ctrl Pts',(-64.6262948318765,-4.06994417791418,
0.485558348777591));
#42584=CARTESIAN_POINT('Ctrl Pts',(-64.5978126690739,-4.07040214468438,
-0.000100385708283902));
#42585=CARTESIAN_POINT('Ctrl Pts',(-65.8021873309261,-4.07040485551518,
-0.000100589830685713));
#42586=CARTESIAN_POINT('Ctrl Pts',(-65.7912133735357,-4.07058186212983,
-0.187220792849738));
#42587=CARTESIAN_POINT('Ctrl Pts',(-65.7407287163952,-4.01229538452908,
-1.04794026068607));
#42588=CARTESIAN_POINT('Ctrl Pts',(-65.6507333595047,-3.41624951217949,
-2.51398138263055));
#42589=CARTESIAN_POINT('Ctrl Pts',(-65.5322012602546,-1.80619393837446,
-3.83777625437688));
#42590=CARTESIAN_POINT('Ctrl Pts',(-65.4136691610045,0.240049276229987,
-4.23476557399121));
#42591=CARTESIAN_POINT('Ctrl Pts',(-65.2951370617545,2.22832167981034,-3.60907822206265));
#42592=CARTESIAN_POINT('Ctrl Pts',(-65.1766049625043,3.6784645083721,-2.11181485512497));
#42593=CARTESIAN_POINT('Ctrl Pts',(-65.0580728632543,4.24027484861026,-0.104557782698988));
#42594=CARTESIAN_POINT('Ctrl Pts',(-64.9395407640041,3.77807805248247,1.92794951983446));
#42595=CARTESIAN_POINT('Ctrl Pts',(-64.8210086647541,2.4034925491091,3.4948657610925));
#42596=CARTESIAN_POINT('Ctrl Pts',(-64.7024765655039,0.448474500591471,
4.21778777844487));
#42597=CARTESIAN_POINT('Ctrl Pts',(-64.583944466254,-1.61484810493722,3.92213318484474));
#42598=CARTESIAN_POINT('Ctrl Pts',(-64.4654123670038,-3.2881922202403,2.67930122316078));
#42599=CARTESIAN_POINT('Ctrl Pts',(-64.3714933218946,-3.98487537838422,
1.18185972389678));
#42600=CARTESIAN_POINT('Ctrl Pts',(-64.3170849765353,-4.07039631589167,
0.254123023015174));
#42601=CARTESIAN_POINT('Ctrl Pts',(-64.3021873309261,-4.0702402863456,6.93803360126907E-5));
#42602=CARTESIAN_POINT('Origin',(-92.3478126690739,0.,0.));
#42603=CARTESIAN_POINT('',(-67.5978126690739,-4.07020210173435,5.22794437556925E-5));
#42604=CARTESIAN_POINT('',(-67.3021873309261,-4.07080131582391,4.54689699823894E-5));
#42605=CARTESIAN_POINT('',(-92.3478126690739,-4.0705,-4.39132641279065E-13));
#42606=CARTESIAN_POINT('Ctrl Pts',(-67.5978126690739,-4.07020210173435,
5.22794437558469E-5));
#42607=CARTESIAN_POINT('Ctrl Pts',(-67.5745516258772,-4.07002076765889,
-0.396635336610467));
#42608=CARTESIAN_POINT('Ctrl Pts',(-67.5117798829305,-3.91459128202717,
-1.46726694234189));
#42609=CARTESIAN_POINT('Ctrl Pts',(-67.4094974402338,-2.98897915866447,
-3.00946285351303));
#42610=CARTESIAN_POINT('Ctrl Pts',(-67.2909653409837,-1.19448972629963,
-4.06989648165282));
#42611=CARTESIAN_POINT('Ctrl Pts',(-67.1724332417337,0.888463555159219,
-4.14746857598213));
#42612=CARTESIAN_POINT('Ctrl Pts',(-67.0539011424835,2.75685691930934,-3.22344582769147));
#42613=CARTESIAN_POINT('Ctrl Pts',(-66.9353690432335,3.95948184624652,-1.52097553788664));
#42614=CARTESIAN_POINT('Ctrl Pts',(-66.8168369439834,4.20590987283498,0.548803443132984));
#42615=CARTESIAN_POINT('Ctrl Pts',(-66.6983048447332,3.43662974878158,2.48604888274442));
#42616=CARTESIAN_POINT('Ctrl Pts',(-66.5797727454832,1.83741913355893,3.82292479722488));
#42617=CARTESIAN_POINT('Ctrl Pts',(-66.4612406462331,-0.205519865420819,
4.23658171908943));
#42618=CARTESIAN_POINT('Ctrl Pts',(-66.3427085469829,-2.19882674941518,
3.62712337861033));
#42619=CARTESIAN_POINT('Ctrl Pts',(-66.224176447733,-3.66112695025279,2.1417311996929));
#42620=CARTESIAN_POINT('Ctrl Pts',(-66.1425444884298,-4.059296707607,0.762551858271784));
#42621=CARTESIAN_POINT('Ctrl Pts',(-66.1004232288768,-4.07082795872572,
0.0445454765449013));
#42622=CARTESIAN_POINT('Ctrl Pts',(-66.0978126690738,-4.0708029246806,4.46106111927618E-5));
#42623=CARTESIAN_POINT('Ctrl Pts',(-67.3021873309261,-4.07080131582391,
4.54689699825889E-5));
#42624=CARTESIAN_POINT('Ctrl Pts',(-67.265341770536,-4.07044224577636,-0.628042511262155));
#42625=CARTESIAN_POINT('Ctrl Pts',(-67.1889855103959,-3.76437490242843,
-1.92998766076815));
#42626=CARTESIAN_POINT('Ctrl Pts',(-67.0731185505057,-2.43428544669007,
-3.47348779841137));
#42627=CARTESIAN_POINT('Ctrl Pts',(-66.9545864512557,-0.485732755623718,
-4.21365955100716));
#42628=CARTESIAN_POINT('Ctrl Pts',(-66.8360543520056,1.58012219199054,-3.93625164084547));
#42629=CARTESIAN_POINT('Ctrl Pts',(-66.7175222527555,3.26438479979246,-2.70825681953606));
#42630=CARTESIAN_POINT('Ctrl Pts',(-66.5989901535054,4.16031329007191,-0.826230264593738));
#42631=CARTESIAN_POINT('Ctrl Pts',(-66.4804580542553,4.05154499755959,1.25532715035943));
#42632=CARTESIAN_POINT('Ctrl Pts',(-66.3619259550052,2.96434697137833,3.03372875434832));
#42633=CARTESIAN_POINT('Ctrl Pts',(-66.2433938557551,1.16127260186261,4.07949862922429));
#42634=CARTESIAN_POINT('Ctrl Pts',(-66.124861756505,-0.922243831912986,
4.14008809521949));
#42635=CARTESIAN_POINT('Ctrl Pts',(-66.006329657255,-2.78304256481646,3.20086507121113));
#42636=CARTESIAN_POINT('Ctrl Pts',(-65.8987715153953,-3.86169612693019,
1.64716843702214));
#42637=CARTESIAN_POINT('Ctrl Pts',(-65.8307240732857,-4.06994456648923,
0.486487869905523));
#42638=CARTESIAN_POINT('Ctrl Pts',(-65.8021873309261,-4.07040485551518,
-0.000100589830685713));
#42639=CARTESIAN_POINT('Origin',(-92.3478126690739,0.,0.));
#42640=CARTESIAN_POINT('',(-69.0978126690739,-4.07047413145155,-0.000103298102520897));
#42641=CARTESIAN_POINT('',(-68.8021873309261,-4.07020080396294,5.15392301635165E-5));
#42642=CARTESIAN_POINT('',(-92.3478126690739,-4.0705,-4.39132641279065E-13));
#42643=CARTESIAN_POINT('Ctrl Pts',(-69.0978126690739,-4.07047413145155,
-0.000103298102520806));
#42644=CARTESIAN_POINT('Ctrl Pts',(-69.0881907226276,-4.07063840498987,
-0.16416193285465));
#42645=CARTESIAN_POINT('Ctrl Pts',(-69.0390580764313,-4.0209408203763,-1.00179737554187));
#42646=CARTESIAN_POINT('Ctrl Pts',(-68.9504147304849,-3.45846662340299,
-2.45557970596334));
#42647=CARTESIAN_POINT('Ctrl Pts',(-68.8318826312348,-1.87113344337377,
-3.8065368400609));
#42648=CARTESIAN_POINT('Ctrl Pts',(-68.7133505319848,0.168069973265368,
-4.23823259881627));
#42649=CARTESIAN_POINT('Ctrl Pts',(-68.5948184327347,2.16668525394882,-3.64641441527627));
#42650=CARTESIAN_POINT('Ctrl Pts',(-68.4762863334845,3.64205587679515,-2.17400369546731));
#42651=CARTESIAN_POINT('Ctrl Pts',(-68.3577542342345,4.23788653064464,-0.176580947402252));
#42652=CARTESIAN_POINT('Ctrl Pts',(-68.2392221349844,3.81028681608063,1.86348529825389));
#42653=CARTESIAN_POINT('Ctrl Pts',(-68.1206900357343,2.46252012400403,3.45352829964948));
#42654=CARTESIAN_POINT('Ctrl Pts',(-68.0021579364842,0.520065995274375,
4.20955988651605));
#42655=CARTESIAN_POINT('Ctrl Pts',(-67.8836258372342,-1.54798171159727,
3.94900186099799));
#42656=CARTESIAN_POINT('Ctrl Pts',(-67.7650937379841,-3.24219885883922,
2.73477780401754));
#42657=CARTESIAN_POINT('Ctrl Pts',(-67.6698226819306,-3.97461545403881,
1.22800549874083));
#42658=CARTESIAN_POINT('Ctrl Pts',(-67.6140623256272,-4.07032877775755,
0.277169580906076));
#42659=CARTESIAN_POINT('Ctrl Pts',(-67.5978126690739,-4.07020210173435,
5.22794437558469E-5));
#42660=CARTESIAN_POINT('Ctrl Pts',(-68.8021873309261,-4.07020080396294,
5.15392301636899E-5));
#42661=CARTESIAN_POINT('Ctrl Pts',(-68.7789808672864,-4.07002252986222,
-0.395705654822888));
#42662=CARTESIAN_POINT('Ctrl Pts',(-68.7162637038966,-3.91510335891766,
-1.46540498961079));
#42663=CARTESIAN_POINT('Ctrl Pts',(-68.6140358407569,-2.99104255021837,
-3.00741210752073));
#42664=CARTESIAN_POINT('Ctrl Pts',(-68.4955037415068,-1.19728085404309,
-4.06907626842045));
#42665=CARTESIAN_POINT('Ctrl Pts',(-68.3769716422567,0.885618735911535,
-4.14807697328309));
#42666=CARTESIAN_POINT('Ctrl Pts',(-68.2584395430066,2.75464541949803,-3.22533591033841));
#42667=CARTESIAN_POINT('Ctrl Pts',(-68.1399074437565,3.9584377330416,-1.52369085949611));
#42668=CARTESIAN_POINT('Ctrl Pts',(-68.0213753445065,4.20628529483797,0.54591862040923));
#42669=CARTESIAN_POINT('Ctrl Pts',(-67.9028432452563,3.43833404328219,2.48369123050478));
#42670=CARTESIAN_POINT('Ctrl Pts',(-67.7843111460063,1.84004072116821,3.82166367778779));
#42671=CARTESIAN_POINT('Ctrl Pts',(-67.6657790467562,-0.202614086215485,
4.23672168707678));
#42672=CARTESIAN_POINT('Ctrl Pts',(-67.5472469475061,-2.19633851110734,
3.62863063238826));
#42673=CARTESIAN_POINT('Ctrl Pts',(-67.428714848256,-3.65965715110381,2.14424174431298));
#42674=CARTESIAN_POINT('Ctrl Pts',(-67.347028309396,-4.05903959952155,0.764413873298388));
#42675=CARTESIAN_POINT('Ctrl Pts',(-67.3048524702861,-4.07082728833475,
0.045476776836982));
#42676=CARTESIAN_POINT('Ctrl Pts',(-67.3021873309261,-4.07080131582391,
4.54689699825889E-5));
#42677=CARTESIAN_POINT('Origin',(-92.3478126690739,0.,0.));
#42678=CARTESIAN_POINT('',(-70.5978126690739,-4.07075375686348,6.52392274777287E-5));
#42679=CARTESIAN_POINT('',(-70.3021873309261,-4.07047700469628,-0.000103310864021655));
#42680=CARTESIAN_POINT('',(-92.3478126690739,-4.0705,-4.39132641279065E-13));
#42681=CARTESIAN_POINT('Ctrl Pts',(-70.5978126690739,-4.07075375686348,
6.52392274777796E-5));
#42682=CARTESIAN_POINT('Ctrl Pts',(-70.5623191196279,-4.07029028939964,
-0.604996165359999));
#42683=CARTESIAN_POINT('Ctrl Pts',(-70.4873148704319,-3.78140816801703,
-1.88402768221452));
#42684=CARTESIAN_POINT('Ctrl Pts',(-70.372799921486,-2.49294537375558,-3.43163023054535));
#42685=CARTESIAN_POINT('Ctrl Pts',(-70.2542678222358,-0.557248744408297,
-4.20479929705468));
#42686=CARTESIAN_POINT('Ctrl Pts',(-70.1357357229858,1.51302095431612,-3.96252830672392));
#42687=CARTESIAN_POINT('Ctrl Pts',(-70.0172036237356,3.21790294474063,-2.7633247619019));
#42688=CARTESIAN_POINT('Ctrl Pts',(-69.8986715244856,4.14567598115117,-0.896790799288985));
#42689=CARTESIAN_POINT('Ctrl Pts',(-69.7801394252355,4.07228707527332,1.18631405942714));
#42690=CARTESIAN_POINT('Ctrl Pts',(-69.6616073259855,3.01545931965475,2.98292946189813));
#42691=CARTESIAN_POINT('Ctrl Pts',(-69.5430752267353,1.23041181972154,4.05918093071395));
#42692=CARTESIAN_POINT('Ctrl Pts',(-69.4245431274853,-0.851774551486206,
4.15515862422754));
#42693=CARTESIAN_POINT('Ctrl Pts',(-69.3060110282352,-2.72826123349541,
3.24768436257942));
#42694=CARTESIAN_POINT('Ctrl Pts',(-69.1971008754314,-3.84704351951115,
1.69324039772707));
#42695=CARTESIAN_POINT('Ctrl Pts',(-69.1277014223776,-4.06996384683415,
0.509513762107668));
#42696=CARTESIAN_POINT('Ctrl Pts',(-69.0978126690739,-4.07047413145155,
-0.000103298102520806));
#42697=CARTESIAN_POINT('Ctrl Pts',(-70.3021873309261,-4.07047700469628,
-0.000103310864021447));
#42698=CARTESIAN_POINT('Ctrl Pts',(-70.2926199640367,-4.0706405847988,-0.163231007798239));
#42699=CARTESIAN_POINT('Ctrl Pts',(-70.2435418973974,-4.02128126826631,
-0.999934669155785));
#42700=CARTESIAN_POINT('Ctrl Pts',(-70.154953131008,-3.46015001328113,-2.45320708625443));
#42701=CARTESIAN_POINT('Ctrl Pts',(-70.0364210317579,-1.87374378398806,
-3.80525259964336));
#42702=CARTESIAN_POINT('Ctrl Pts',(-69.9178889325078,0.165163070961228,
-4.23834688141492));
#42703=CARTESIAN_POINT('Ctrl Pts',(-69.7993568332577,2.16418379186852,-3.64789961943599));
#42704=CARTESIAN_POINT('Ctrl Pts',(-69.6808247340076,3.64056394757633,-2.17650115247581));
#42705=CARTESIAN_POINT('Ctrl Pts',(-69.5622926347575,4.2377644279798,-0.179487532051847));
#42706=CARTESIAN_POINT('Ctrl Pts',(-69.4437605355075,3.81156402742994,1.8608715126343));
#42707=CARTESIAN_POINT('Ctrl Pts',(-69.3252284362573,2.46488820851225,3.45183853059299));
#42708=CARTESIAN_POINT('Ctrl Pts',(-69.2066963370073,0.522953071331976,
4.20920220550053));
#42709=CARTESIAN_POINT('Ctrl Pts',(-69.0881642377572,-1.54527285978556,
3.95006264640662));
#42710=CARTESIAN_POINT('Ctrl Pts',(-68.9696321385071,-3.24032240668157,
2.737000880967));
#42711=CARTESIAN_POINT('Ctrl Pts',(-68.8743065028967,-3.97419245969456,
1.22986834614377));
#42712=CARTESIAN_POINT('Ctrl Pts',(-68.8184915670364,-4.07032605454294,
0.278099881035541));
#42713=CARTESIAN_POINT('Ctrl Pts',(-68.8021873309261,-4.07020080396294,
5.15392301636899E-5));
#42714=CARTESIAN_POINT('Origin',(-92.3478126690739,0.,0.));
#42715=CARTESIAN_POINT('',(-72.0978126690739,-4.07028079851592,-0.000396239704358614));
#42716=CARTESIAN_POINT('',(-71.8021873309261,-4.07074215327807,5.17293523791262E-5));
#42717=CARTESIAN_POINT('',(-92.3478126690739,-4.0705,-4.39132641279065E-13));
#42718=CARTESIAN_POINT('Ctrl Pts',(-72.0978126690739,-4.07028079851592,
-0.000396239704358523));
#42719=CARTESIAN_POINT('Ctrl Pts',(-72.0759582163783,-4.07012861038251,
-0.3729091594408));
#42720=CARTESIAN_POINT('Ctrl Pts',(-72.0145930639327,-3.92738889203425,
-1.41858141393639));
#42721=CARTESIAN_POINT('Ctrl Pts',(-71.9137172117371,-3.04181408411095,
-2.95660822043184));
#42722=CARTESIAN_POINT('Ctrl Pts',(-71.7951851124869,-1.26618312449043,
-4.04792730165813));
#42723=CARTESIAN_POINT('Ctrl Pts',(-71.676653013237,0.814991865508356,-4.1626338697688));
#42724=CARTESIAN_POINT('Ctrl Pts',(-71.5581209139868,2.69946593220966,-3.27161473710967));
#42725=CARTESIAN_POINT('Ctrl Pts',(-71.4395888147368,3.93197366980717,-1.59074811823812));
#42726=CARTESIAN_POINT('Ctrl Pts',(-71.3210567154866,4.21495618453984,0.474392460257583));
#42727=CARTESIAN_POINT('Ctrl Pts',(-71.2025246162366,3.48003171573737,2.42491205953816));
#42728=CARTESIAN_POINT('Ctrl Pts',(-71.0839925169865,1.90470242326041,3.78985487631873));
#42729=CARTESIAN_POINT('Ctrl Pts',(-70.9654604177364,-0.130607360489598,
4.2395507965525));
#42730=CARTESIAN_POINT('Ctrl Pts',(-70.8469283184863,-2.13437432226263,
3.6654214565239));
#42731=CARTESIAN_POINT('Ctrl Pts',(-70.7283962192362,-3.62270043207957,
2.20610597997014));
#42732=CARTESIAN_POINT('Ctrl Pts',(-70.6453576694321,-4.05246440445107,
0.810540587465255));
#42733=CARTESIAN_POINT('Ctrl Pts',(-70.601829819378,-4.07080621198539,0.068545924968227));
#42734=CARTESIAN_POINT('Ctrl Pts',(-70.5978126690739,-4.07075375686348,
6.52392274777796E-5));
#42735=CARTESIAN_POINT('Ctrl Pts',(-71.8021873309261,-4.07074215327807,
5.17293523791609E-5));
#42736=CARTESIAN_POINT('Ctrl Pts',(-71.7667483610371,-4.07027236134414,
-0.6040848204387));
#42737=CARTESIAN_POINT('Ctrl Pts',(-71.6917986913982,-3.78210048234303,
-1.88214965493016));
#42738=CARTESIAN_POINT('Ctrl Pts',(-71.5773383220089,-2.49529078987354,
-3.42993115267771));
#42739=CARTESIAN_POINT('Ctrl Pts',(-71.458806222759,-0.560136340693826,
-4.20441037867915));
#42740=CARTESIAN_POINT('Ctrl Pts',(-71.3402741235088,1.5103047169698,-3.96356795830934));
#42741=CARTESIAN_POINT('Ctrl Pts',(-71.2217420242588,3.21600598369556,-2.76552975458416));
#42742=CARTESIAN_POINT('Ctrl Pts',(-71.1032099250086,4.14506039630085,-0.899634673257719));
#42743=CARTESIAN_POINT('Ctrl Pts',(-70.9846778257586,4.07309954546553,1.18352108347017));
#42744=CARTESIAN_POINT('Ctrl Pts',(-70.8661457265085,3.01750462107274,2.98086038723955));
#42745=CARTESIAN_POINT('Ctrl Pts',(-70.7476136272584,1.23319553280523,4.0583361681078));
#42746=CARTESIAN_POINT('Ctrl Pts',(-70.6290815280083,-0.848924438267781,
4.15574181331312));
#42747=CARTESIAN_POINT('Ctrl Pts',(-70.5105494287582,-2.72603312996977,
3.24955484789199));
#42748=CARTESIAN_POINT('Ctrl Pts',(-70.4015846963975,-3.84644248062139,
1.69509993942009));
#42749=CARTESIAN_POINT('Ctrl Pts',(-70.3321306637868,-4.0699650421557,0.51044331963423));
#42750=CARTESIAN_POINT('Ctrl Pts',(-70.3021873309261,-4.07047700469628,
-0.000103310864021447));
#42751=CARTESIAN_POINT('Origin',(-92.3478126690739,0.,0.));
#42752=CARTESIAN_POINT('',(-73.5978126690739,-4.06507175003265,0.00203090272800402));
#42753=CARTESIAN_POINT('',(-73.3021873309261,-4.06969892170118,-0.00325965976725018));
#42754=CARTESIAN_POINT('',(-92.3478126690739,-4.0705,-4.39132641279065E-13));
#42755=CARTESIAN_POINT('Ctrl Pts',(-73.5978126690739,-4.06507175003265,
0.00203090272800382));
#42756=CARTESIAN_POINT('Ctrl Pts',(-73.5500866133787,-4.06112590042124,
-0.814333197936782));
#42757=CARTESIAN_POINT('Ctrl Pts',(-73.4233391581834,-3.42780995393646,
-2.98789524608297));
#42758=CARTESIAN_POINT('Ctrl Pts',(-73.217570303488,0.104851279587011,-4.80118117413053));
#42759=CARTESIAN_POINT('Ctrl Pts',(-72.9805061049878,4.0818527109764,-2.5374258400941));
#42760=CARTESIAN_POINT('Ctrl Pts',(-72.7434419064878,4.34947338571156,2.0393426803231));
#42761=CARTESIAN_POINT('Ctrl Pts',(-72.5458884077375,1.29059508521834,4.29352941894811));
#42762=CARTESIAN_POINT('Ctrl Pts',(-72.3878456087375,-1.47975600101921,
3.96853832825987));
#42763=CARTESIAN_POINT('Ctrl Pts',(-72.2693135094873,-3.19245598996507,
2.7952829416349));
#42764=CARTESIAN_POINT('Ctrl Pts',(-72.1726358629329,-3.96369324348151,
1.2752093510444));
#42765=CARTESIAN_POINT('Ctrl Pts',(-72.1154689161283,-4.0704037515507,0.300557539988409));
#42766=CARTESIAN_POINT('Ctrl Pts',(-72.0978126690739,-4.07028079851592,
-0.000396239704358523));
#42767=CARTESIAN_POINT('Ctrl Pts',(-73.3021873309261,-4.06969892170118,
-0.00325965976725035));
#42768=CARTESIAN_POINT('Ctrl Pts',(-73.2803874577875,-4.072936090382,-0.375222354381865));
#42769=CARTESIAN_POINT('Ctrl Pts',(-73.1795661851488,-3.85606008990605,
-2.09201308027041));
#42770=CARTESIAN_POINT('Ctrl Pts',(-72.9997235130101,-1.43150958571139,
-4.58558645780951));
#42771=CARTESIAN_POINT('Ctrl Pts',(-72.8021700142599,2.29645120176649,-3.85049572963833));
#42772=CARTESIAN_POINT('Ctrl Pts',(-72.6441272152598,3.92679810234926,-1.58721605638371));
#42773=CARTESIAN_POINT('Ctrl Pts',(-72.5255951160097,4.21734429791554,0.468377299721421));
#42774=CARTESIAN_POINT('Ctrl Pts',(-72.4070630167596,3.4806665638518,2.42407836288371));
#42775=CARTESIAN_POINT('Ctrl Pts',(-72.2885309175095,1.90781163232082,3.78777607431905));
#42776=CARTESIAN_POINT('Ctrl Pts',(-72.1699988182595,-0.127952933172336,
4.24002244278688));
#42777=CARTESIAN_POINT('Ctrl Pts',(-72.0514667190093,-2.13173404035006,
3.66669431825119));
#42778=CARTESIAN_POINT('Ctrl Pts',(-71.9329346197594,-3.62124894073959,
2.20868457101181));
#42779=CARTESIAN_POINT('Ctrl Pts',(-71.8498414903981,-4.05218757424346,
0.812398134823304));
#42780=CARTESIAN_POINT('Ctrl Pts',(-71.8062590607871,-4.07079612961688,
0.0694634768615688));
#42781=CARTESIAN_POINT('Ctrl Pts',(-71.8021873309261,-4.07074215327807,
5.17293523791609E-5));
#42782=CARTESIAN_POINT('Origin',(-92.3478126690739,0.,0.));
#42783=CARTESIAN_POINT('',(-75.0978126690739,-4.07583767183017,0.00141285829539006));
#42784=CARTESIAN_POINT('',(-74.8021873309261,-4.06510912917479,0.00214260453011594));
#42785=CARTESIAN_POINT('',(-92.3478126690739,-4.0705,-4.39132641279065E-13));
#42786=CARTESIAN_POINT('Ctrl Pts',(-75.0978126690739,-4.07583767183017,
0.00141285829539012));
#42787=CARTESIAN_POINT('Ctrl Pts',(-75.024215010379,-4.06930339312292,-1.24860930367453));
#42788=CARTESIAN_POINT('Ctrl Pts',(-74.8715959521841,-2.78876718547004,
-3.85121310504378));
#42789=CARTESIAN_POINT('Ctrl Pts',(-74.639955494489,1.63433374823429,-4.51748027493275));
#42790=CARTESIAN_POINT('Ctrl Pts',(-74.402891295989,4.6763033020638,-1.09843764222045));
#42791=CARTESIAN_POINT('Ctrl Pts',(-74.1658270974887,3.47436957665643,3.31745869645859));
#42792=CARTESIAN_POINT('Ctrl Pts',(-73.9287628989886,-0.881308697829502,
4.72204116943823));
#42793=CARTESIAN_POINT('Ctrl Pts',(-73.7394247561836,-3.72131169761533,
2.42118440488785));
#42794=CARTESIAN_POINT('Ctrl Pts',(-73.6291080128787,-4.0676591568148,0.537344262025627));
#42795=CARTESIAN_POINT('Ctrl Pts',(-73.5978126690739,-4.06507175003265,
0.00203090272800382));
#42796=CARTESIAN_POINT('Ctrl Pts',(-74.8021873309261,-4.06510912917479,
0.00214260453011594));
#42797=CARTESIAN_POINT('Ctrl Pts',(-74.7545158547878,-4.06124659588267,
-0.813195354839492));
#42798=CARTESIAN_POINT('Ctrl Pts',(-74.6278229791496,-3.42914710515804,
-2.98561629200826));
#42799=CARTESIAN_POINT('Ctrl Pts',(-74.422108704011,0.102291553945791,-4.80267280759255));
#42800=CARTESIAN_POINT('Ctrl Pts',(-74.185044505511,4.07867853910156,-2.53741907084073));
#42801=CARTESIAN_POINT('Ctrl Pts',(-73.9479803070107,4.35373227228281,2.03076696083007));
#42802=CARTESIAN_POINT('Ctrl Pts',(-73.7109161085106,0.675669024164784,
4.75614017541162));
#42803=CARTESIAN_POINT('Ctrl Pts',(-73.4956517831491,-3.21859608763278,
3.31010339667926));
#42804=CARTESIAN_POINT('Ctrl Pts',(-73.3594088572876,-4.06120182028099,
0.973088826299921));
#42805=CARTESIAN_POINT('Ctrl Pts',(-73.3021873309261,-4.06969892170118,
-0.00325965976725035));
#42806=CARTESIAN_POINT('Origin',(-92.3478126690739,0.,0.));
#42807=CARTESIAN_POINT('',(-76.5978126690739,-4.07011789117663,1.93561709038092E-5));
#42808=CARTESIAN_POINT('',(-76.3021873309261,-4.07616962263128,0.0032098901687027));
#42809=CARTESIAN_POINT('',(-92.3478126690739,-4.0705,-4.39132641279065E-13));
#42810=CARTESIAN_POINT('Ctrl Pts',(-76.5978126690739,-4.07011789117663,
1.93561709039766E-5));
#42811=CARTESIAN_POINT('Ctrl Pts',(-76.5773648068794,-4.07005952701129,
-0.348697968315602));
#42812=CARTESIAN_POINT('Ctrl Pts',(-76.5174062449349,-3.93994663469226,
-1.3712594731013));
#42813=CARTESIAN_POINT('Ctrl Pts',(-76.4179369832404,-3.09392819414575,
-2.90202919022035));
#42814=CARTESIAN_POINT('Ctrl Pts',(-76.2994048839903,-1.33668453718049,
-4.02495526764412));
#42815=CARTESIAN_POINT('Ctrl Pts',(-76.1808727847402,0.739496217920181,
-4.17664208939481));
#42816=CARTESIAN_POINT('Ctrl Pts',(-76.0623406854901,2.64486935815373,-3.3181392451129));
#42817=CARTESIAN_POINT('Ctrl Pts',(-75.9438085862401,3.89596740984592,-1.66144883365045));
#42818=CARTESIAN_POINT('Ctrl Pts',(-75.7857657872398,4.3485497237372,1.09093805761265));
#42819=CARTESIAN_POINT('Ctrl Pts',(-75.5882122884899,2.2380304938709,4.25065369199898));
#42820=CARTESIAN_POINT('Ctrl Pts',(-75.3511480899896,-2.34621401747439,
4.19467891885534));
#42821=CARTESIAN_POINT('Ctrl Pts',(-75.1876815501843,-4.03215439766421,
1.5273685129187));
#42822=CARTESIAN_POINT('Ctrl Pts',(-75.1032364098791,-4.0763192120678,0.0935325850297277));
#42823=CARTESIAN_POINT('Ctrl Pts',(-75.0978126690739,-4.07583767183017,
0.00141285829539012));
#42824=CARTESIAN_POINT('Ctrl Pts',(-76.3021873309261,-4.07616962263128,
0.00320989016870294));
#42825=CARTESIAN_POINT('Ctrl Pts',(-76.2286442517882,-4.0696862238209,-1.24479614250474));
#42826=CARTESIAN_POINT('Ctrl Pts',(-76.0760797731501,-2.78983322256644,
-3.85270151269288));
#42827=CARTESIAN_POINT('Ctrl Pts',(-75.8444938950122,1.63095801340486,-4.51688897627564));
#42828=CARTESIAN_POINT('Ctrl Pts',(-75.607429696512,4.67567242759371,-1.10249052069397));
#42829=CARTESIAN_POINT('Ctrl Pts',(-75.3703654980118,3.47661902182452,3.31543652103366));
#42830=CARTESIAN_POINT('Ctrl Pts',(-75.1333012995117,-0.878131813745364,
4.72260507390595));
#42831=CARTESIAN_POINT('Ctrl Pts',(-74.9439085771497,-3.72034050812532,
2.4228541118301));
#42832=CARTESIAN_POINT('Ctrl Pts',(-74.8335372542879,-4.06764922510844,
0.538328697573246));
#42833=CARTESIAN_POINT('Ctrl Pts',(-74.8021873309261,-4.06510912917479,
0.00214260453011594));
#42834=CARTESIAN_POINT('Origin',(-92.3478126690739,0.,0.));
#42835=CARTESIAN_POINT('',(-78.0978126690738,-4.07062303909154,-9.39073287783277E-5));
#42836=CARTESIAN_POINT('',(-77.8021873309261,-4.07016223393827,1.2136666346918E-5));
#42837=CARTESIAN_POINT('',(-92.3478126690739,-4.0705,-4.39132641279065E-13));
#42838=CARTESIAN_POINT('Ctrl Pts',(-78.0978126690738,-4.07062303909154,
-9.39073287782588E-5));
#42839=CARTESIAN_POINT('Ctrl Pts',(-78.0910039036297,-4.07073767756003,
-0.116174268661055));
#42840=CARTESIAN_POINT('Ctrl Pts',(-78.0446844384356,-4.03762736234282,
-0.905794127161616));
#42841=CARTESIAN_POINT('Ctrl Pts',(-77.9588542734915,-3.54309601390001,
-2.33180902134115));
#42842=CARTESIAN_POINT('Ctrl Pts',(-77.8403221742414,-2.00450312872445,
-3.73802499184148));
#42843=CARTESIAN_POINT('Ctrl Pts',(-77.7217900749913,0.0181685980883059,
-4.2415248017455));
#42844=CARTESIAN_POINT('Ctrl Pts',(-77.6032579757413,2.03645182254301,-3.72071578999402));
#42845=CARTESIAN_POINT('Ctrl Pts',(-77.4847258764911,3.56294292078298,-2.30137044925895));
#42846=CARTESIAN_POINT('Ctrl Pts',(-77.3661937772411,4.22899594778787,-0.326255287706977));
#42847=CARTESIAN_POINT('Ctrl Pts',(-77.247661677991,3.87377273534343,1.72765045644101));
#42848=CARTESIAN_POINT('Ctrl Pts',(-77.1291295787409,2.58303669769032,3.36433361268123));
#42849=CARTESIAN_POINT('Ctrl Pts',(-77.0105974794908,0.668537789879148,
4.18855118954554));
#42850=CARTESIAN_POINT('Ctrl Pts',(-76.8920653802408,-1.40746790745146,
4.00124113310223));
#42851=CARTESIAN_POINT('Ctrl Pts',(-76.7735332809906,-3.14345978794428,
2.84767271097138));
#42852=CARTESIAN_POINT('Ctrl Pts',(-76.6754490439351,-3.95199757018475,
1.32400107408212));
#42853=CARTESIAN_POINT('Ctrl Pts',(-76.6168755066295,-4.07017230207751,
0.325116505509737));
#42854=CARTESIAN_POINT('Ctrl Pts',(-76.5978126690739,-4.07011789117663,
1.93561709039766E-5));
#42855=CARTESIAN_POINT('Ctrl Pts',(-77.8021873309261,-4.07016223393827,
1.21366663470221E-5));
#42856=CARTESIAN_POINT('Ctrl Pts',(-77.7817940482886,-4.07013329270246,
-0.347778280513504));
#42857=CARTESIAN_POINT('Ctrl Pts',(-77.721890065901,-3.94054142339228,-1.36941406884846));
#42858=CARTESIAN_POINT('Ctrl Pts',(-77.6224753837634,-3.09545209551088,
-2.89984013449786));
#42859=CARTESIAN_POINT('Ctrl Pts',(-77.5039432845133,-1.34038284556851,
-4.02417116971747));
#42860=CARTESIAN_POINT('Ctrl Pts',(-77.3854111852633,0.738520086648723,
-4.17687915873197));
#42861=CARTESIAN_POINT('Ctrl Pts',(-77.2668790860131,2.63879720128349,-3.32049492888954));
#42862=CARTESIAN_POINT('Ctrl Pts',(-77.1483469867632,3.90237383473824,-1.66302156401962));
#42863=CARTESIAN_POINT('Ctrl Pts',(-77.0298148875129,4.22242284177216,0.397665888508434));
#42864=CARTESIAN_POINT('Ctrl Pts',(-76.911282788263,3.52503575024894,2.35909274883029));
#42865=CARTESIAN_POINT('Ctrl Pts',(-76.7927506890127,1.97181984252191,3.75729912712469));
#42866=CARTESIAN_POINT('Ctrl Pts',(-76.6742185897627,-0.0484579238967644,
4.23516823465935));
#42867=CARTESIAN_POINT('Ctrl Pts',(-76.5161757907627,-2.75000559908163,
3.54082966140385));
#42868=CARTESIAN_POINT('Ctrl Pts',(-76.3921653711505,-4.03185271297995,
1.52933182071804));
#42869=CARTESIAN_POINT('Ctrl Pts',(-76.3076656512883,-4.07665257950683,
0.0961754953757293));
#42870=CARTESIAN_POINT('Ctrl Pts',(-76.3021873309261,-4.07616962263128,
0.00320989016870294));
#42871=CARTESIAN_POINT('Origin',(-92.3478126690739,0.,0.));
#42872=CARTESIAN_POINT('',(-79.5978126690739,-4.07062191593116,9.40553201711143E-5));
#42873=CARTESIAN_POINT('',(-79.3021873309261,-4.07062585394818,-9.35223854153788E-5));
#42874=CARTESIAN_POINT('',(-92.3478126690739,-4.0705,-4.39132641279065E-13));
#42875=CARTESIAN_POINT('Ctrl Pts',(-79.5978126690739,-4.07062191593116,
9.40553201713226E-5));
#42876=CARTESIAN_POINT('Ctrl Pts',(-79.5651323006301,-4.07007120518726,
-0.557063040139934));
#42877=CARTESIAN_POINT('Ctrl Pts',(-79.4929412324364,-3.81534586386885,
-1.78831340922059));
#42878=CARTESIAN_POINT('Ctrl Pts',(-79.3812394644925,-2.61267572378093,
-3.34137526175934));
#42879=CARTESIAN_POINT('Ctrl Pts',(-79.2627073652425,-0.705515467763387,
-4.18247665892133));
#42880=CARTESIAN_POINT('Ctrl Pts',(-79.1441752659924,1.3720235726515,-4.01352892025788));
#42881=CARTESIAN_POINT('Ctrl Pts',(-79.0256431667423,3.11822514541502,-2.87533215814075));
#42882=CARTESIAN_POINT('Ctrl Pts',(-78.9071110674922,4.11138949440471,-1.04275572611736));
#42883=CARTESIAN_POINT('Ctrl Pts',(-78.7885789682421,4.11167193448134,1.04164148226761));
#42884=CARTESIAN_POINT('Ctrl Pts',(-78.670046868992,3.11900426003185,2.87448699928452));
#42885=CARTESIAN_POINT('Ctrl Pts',(-78.551514769742,1.37311120556277,4.01315694786418));
#42886=CARTESIAN_POINT('Ctrl Pts',(-78.4329826704918,-0.704381968314586,
4.18266770388186));
#42887=CARTESIAN_POINT('Ctrl Pts',(-78.3144505712418,-2.61177010587796,
3.34208318501393));
#42888=CARTESIAN_POINT('Ctrl Pts',(-78.2027272374358,-3.81509334776075,
1.78904754094927));
#42889=CARTESIAN_POINT('Ctrl Pts',(-78.1305146033798,-4.0700724400591,0.557430416525206));
#42890=CARTESIAN_POINT('Ctrl Pts',(-78.0978126690738,-4.07062303909154,
-9.39073287782588E-5));
#42891=CARTESIAN_POINT('Ctrl Pts',(-79.3021873309261,-4.07062585394818,
-9.35223854152401E-5));
#42892=CARTESIAN_POINT('Ctrl Pts',(-79.295433145039,-4.0707393191523,-0.115243145155149));
#42893=CARTESIAN_POINT('Ctrl Pts',(-79.2491682594018,-4.03793381614542,
-0.903931660617922));
#42894=CARTESIAN_POINT('Ctrl Pts',(-79.1633926740146,-3.54469454740893,
-2.32937839090772));
#42895=CARTESIAN_POINT('Ctrl Pts',(-79.0448605747645,-2.00706634268101,
-3.73664927998142));
#42896=CARTESIAN_POINT('Ctrl Pts',(-78.9263284755144,0.0152592617744791,
-4.24153630056935));
#42897=CARTESIAN_POINT('Ctrl Pts',(-78.8077963762643,2.03389985453592,-3.72211159382277));
#42898=CARTESIAN_POINT('Ctrl Pts',(-78.6892642770142,3.56136279891019,-2.30381373712066));
#42899=CARTESIAN_POINT('Ctrl Pts',(-78.5707321777641,4.22877291137641,-0.329155494427314));
#42900=CARTESIAN_POINT('Ctrl Pts',(-78.4522000785141,3.87495330153115,1.72499266588648));
#42901=CARTESIAN_POINT('Ctrl Pts',(-78.333667979264,2.58535055813011,3.36256220074308));
#42902=CARTESIAN_POINT('Ctrl Pts',(-78.2151358800139,0.671396364788188,
4.18808967855972));
#42903=CARTESIAN_POINT('Ctrl Pts',(-78.0966037807638,-1.40469494822981,
4.00220956636128));
#42904=CARTESIAN_POINT('Ctrl Pts',(-77.9780716815137,-3.14156294622147,
2.84981991591854));
#42905=CARTESIAN_POINT('Ctrl Pts',(-77.8799328649011,-3.95145378701792,
1.32587590907784));
#42906=CARTESIAN_POINT('Ctrl Pts',(-77.8213047480386,-4.07018936452272,
0.326043732027068));
#42907=CARTESIAN_POINT('Ctrl Pts',(-77.8021873309261,-4.07016223393827,
1.21366663470221E-5));
#42908=CARTESIAN_POINT('Origin',(-92.3478126690739,0.,0.));
#42909=CARTESIAN_POINT('',(-81.0978126690739,-4.07016105732122,-1.11263490865075E-5));
#42910=CARTESIAN_POINT('',(-80.8021873309261,-4.07061909410162,9.44285938865585E-5));
#42911=CARTESIAN_POINT('',(-92.3478126690739,-4.0705,-4.39132641279065E-13));
#42912=CARTESIAN_POINT('Ctrl Pts',(-81.0978126690739,-4.07016105732122,
-1.11263490864752E-5));
#42913=CARTESIAN_POINT('Ctrl Pts',(-81.0787713973805,-4.07019225222942,
-0.324745259963735));
#42914=CARTESIAN_POINT('Ctrl Pts',(-81.020219425937,-3.95209632995797,-1.3232814526723));
#42915=CARTESIAN_POINT('Ctrl Pts',(-80.9221567547438,-3.14428645876529,
-2.84680974826745));
#42916=CARTESIAN_POINT('Ctrl Pts',(-80.8036246554935,-1.40852487473531,
-4.00086500082885));
#42917=CARTESIAN_POINT('Ctrl Pts',(-80.6850925562435,0.667389075585396,
-4.18872950897938));
#42918=CARTESIAN_POINT('Ctrl Pts',(-80.5665604569934,2.58213159232414,-3.36503484640604));
#42919=CARTESIAN_POINT('Ctrl Pts',(-80.4480283577433,3.87330104552845,-1.72869953673665));
#42920=CARTESIAN_POINT('Ctrl Pts',(-80.3294962584933,4.22908587072581,0.325108867355182));
#42921=CARTESIAN_POINT('Ctrl Pts',(-80.2109641592431,3.56356564694796,2.30040495511053));
#42922=CARTESIAN_POINT('Ctrl Pts',(-80.0924320599931,2.03746048854546,3.72016368392876));
#42923=CARTESIAN_POINT('Ctrl Pts',(-79.9738999607429,0.0193178668117769,
4.2415197627297));
#42924=CARTESIAN_POINT('Ctrl Pts',(-79.855367861493,-2.00348993210374,3.73856806405375));
#42925=CARTESIAN_POINT('Ctrl Pts',(-79.7368357622428,-3.54246400293638,
2.33276914106685));
#42926=CARTESIAN_POINT('Ctrl Pts',(-79.6509840314364,-4.03750608952868,
0.906530038982288));
#42927=CARTESIAN_POINT('Ctrl Pts',(-79.6046430003801,-4.07073701673981,
0.116542177935112));
#42928=CARTESIAN_POINT('Ctrl Pts',(-79.5978126690739,-4.07062191593116,
9.40553201713226E-5));
#42929=CARTESIAN_POINT('Ctrl Pts',(-80.8021873309261,-4.07061909410162,
9.44285938865412E-5));
#42930=CARTESIAN_POINT('Ctrl Pts',(-80.7695615420393,-4.07006813553142,
-0.556133273234639));
#42931=CARTESIAN_POINT('Ctrl Pts',(-80.6974250534025,-3.81598438975405,
-1.78645542910972));
#42932=CARTESIAN_POINT('Ctrl Pts',(-80.5857778650156,-2.61496685112479,
-3.33958253217321));
#42933=CARTESIAN_POINT('Ctrl Pts',(-80.4672457657655,-0.708383924910281,
-4.18199179059653));
#42934=CARTESIAN_POINT('Ctrl Pts',(-80.3487136665154,1.36927050498713,-4.01446900670923));
#42935=CARTESIAN_POINT('Ctrl Pts',(-80.2301815672654,3.11625232078442,-2.87747017272681));
#42936=CARTESIAN_POINT('Ctrl Pts',(-80.1116494680153,4.11067334059816,-1.04557534807476));
#42937=CARTESIAN_POINT('Ctrl Pts',(-79.9931173687652,4.11238540021266,1.03882117896535));
#42938=CARTESIAN_POINT('Ctrl Pts',(-79.8745852695151,3.12097504491475,2.87234710485192));
#42939=CARTESIAN_POINT('Ctrl Pts',(-79.756053170265,1.37586337731199,4.01221423757314));
#42940=CARTESIAN_POINT('Ctrl Pts',(-79.6375210710149,-0.701513053379031,
4.18314983703188));
#42941=CARTESIAN_POINT('Ctrl Pts',(-79.5189889717648,-2.60947726422201,
3.343873730567));
#42942=CARTESIAN_POINT('Ctrl Pts',(-79.4072110584019,-3.81445379114245,
1.79090547468083));
#42943=CARTESIAN_POINT('Ctrl Pts',(-79.334943844789,-4.07007556934039,0.558360194698833));
#42944=CARTESIAN_POINT('Ctrl Pts',(-79.3021873309261,-4.07062585394818,
-9.35223854152401E-5));
#42945=CARTESIAN_POINT('Origin',(-92.3478126690739,0.,0.));
#42946=CARTESIAN_POINT('',(-82.5978126690739,-4.07069297892822,-8.16732152922881E-5));
#42947=CARTESIAN_POINT('',(-82.3021873309261,-4.07016134870022,-1.19732118704363E-5));
#42948=CARTESIAN_POINT('',(-92.3478126690739,-4.0705,-4.39132641279065E-13));
#42949=CARTESIAN_POINT('Ctrl Pts',(-82.5978126690739,-4.07069297892822,
-8.16732152923022E-5));
#42950=CARTESIAN_POINT('Ctrl Pts',(-82.5924104941309,-4.07077627717628,
-0.0921769713394929));
#42951=CARTESIAN_POINT('Ctrl Pts',(-82.5474976194379,-4.04531628661873,
-0.857797526681112));
#42952=CARTESIAN_POINT('Ctrl Pts',(-82.4630740449948,-3.58375688894285,
-2.26882120021829));
#42953=CARTESIAN_POINT('Ctrl Pts',(-82.3445419457447,-2.0702588085909,-3.70201182373276));
#42954=CARTESIAN_POINT('Ctrl Pts',(-82.2260098464947,-0.0568026194346637,
-4.24118338910624));
#42955=CARTESIAN_POINT('Ctrl Pts',(-82.1074777472446,1.97037114458219,-3.75612840970636));
#42956=CARTESIAN_POINT('Ctrl Pts',(-81.9889456479944,3.52170921742845,-2.36398546219828));
#42957=CARTESIAN_POINT('Ctrl Pts',(-81.8704135487444,4.2225704934618,-0.40095075177776));
#42958=CARTESIAN_POINT('Ctrl Pts',(-81.7518814494942,3.90370015456685,1.65891174594675));
#42959=CARTESIAN_POINT('Ctrl Pts',(-81.6333493502442,2.64210394076326,3.31815458407359));
#42960=CARTESIAN_POINT('Ctrl Pts',(-81.514817250994,0.742451613392211,4.17607814574591));
#42961=CARTESIAN_POINT('Ctrl Pts',(-81.3962851517442,-1.33649940985683,
4.02549778351171));
#42962=CARTESIAN_POINT('Ctrl Pts',(-81.2777530524938,-3.09269188977919,
2.90277797161605));
#42963=CARTESIAN_POINT('Ctrl Pts',(-81.1782622249373,-3.93987357385575,
1.37201827475063));
#42964=CARTESIAN_POINT('Ctrl Pts',(-81.1182820971305,-4.07012752269499,
0.349079107360558));
#42965=CARTESIAN_POINT('Ctrl Pts',(-81.0978126690739,-4.07016105732122,
-1.11263490864752E-5));
#42966=CARTESIAN_POINT('Ctrl Pts',(-82.3021873309261,-4.07016134870022,
-1.1973211870471E-5));
#42967=CARTESIAN_POINT('Ctrl Pts',(-82.2832006387897,-4.07019482461848,
-0.323815229975626));
#42968=CARTESIAN_POINT('Ctrl Pts',(-82.2247032469032,-3.95255397240321,
-1.3214188020348));
#42969=CARTESIAN_POINT('Ctrl Pts',(-82.1266951552668,-3.14623825560085,
-2.84465252019879));
#42970=CARTESIAN_POINT('Ctrl Pts',(-82.0081630560165,-1.41126860599162,
-3.99989800412737));
#42971=CARTESIAN_POINT('Ctrl Pts',(-81.8896309567667,0.664516008557521,
-4.18918626896089));
#42972=CARTESIAN_POINT('Ctrl Pts',(-81.7710988575164,2.57982302217583,-3.36680505760746));
#42973=CARTESIAN_POINT('Ctrl Pts',(-81.6525667582664,3.87211448147575,-1.73135570118489));
#42974=CARTESIAN_POINT('Ctrl Pts',(-81.5340346590163,4.22930786260355,0.322208201322427));
#42975=CARTESIAN_POINT('Ctrl Pts',(-81.4155025597663,3.56514258472508,2.29796028517889));
#42976=CARTESIAN_POINT('Ctrl Pts',(-81.2969704605161,2.04001154890355,3.71876538679436));
#42977=CARTESIAN_POINT('Ctrl Pts',(-81.178438361266,0.0222269802501248,
4.24150552080608));
#42978=CARTESIAN_POINT('Ctrl Pts',(-81.0599062620159,-2.00092530328236,
3.73994131670062));
#42979=CARTESIAN_POINT('Ctrl Pts',(-80.9413741627659,-3.54086320495273,
2.33519825400134));
#42980=CARTESIAN_POINT('Ctrl Pts',(-80.8554678524026,-4.03719872678699,
0.908392514475943));
#42981=CARTESIAN_POINT('Ctrl Pts',(-80.8090722417893,-4.07073536104181,
0.117473295968627));
#42982=CARTESIAN_POINT('Ctrl Pts',(-80.8021873309261,-4.07061909410162,
9.44285938865412E-5));
#42983=CARTESIAN_POINT('Origin',(-92.3478126690739,0.,0.));
#42984=CARTESIAN_POINT('',(-84.0978126690739,-4.07054770473266,0.000101237284119069));
#42985=CARTESIAN_POINT('',(-83.8021873309262,-4.07069555842019,-8.11031842548604E-5));
#42986=CARTESIAN_POINT('',(-92.3478126690739,-4.0705,-4.39132641279065E-13));
#42987=CARTESIAN_POINT('Ctrl Pts',(-84.0978126690739,-4.07054770473266,
0.000101237284118993));
#42988=CARTESIAN_POINT('Ctrl Pts',(-84.0665388911312,-4.07000484049112,
-0.533103383895171));
#42989=CARTESIAN_POINT('Ctrl Pts',(-83.9957544134385,-3.83156152900343,
-1.74041987047235));
#42990=CARTESIAN_POINT('Ctrl Pts',(-83.8854592359959,-2.67132578982276,
-3.29467473390518));
#42991=CARTESIAN_POINT('Ctrl Pts',(-83.7669271367457,-0.779329768066677,
-4.16935344990209));
#42992=CARTESIAN_POINT('Ctrl Pts',(-83.6483950374957,1.3008708565925,-4.03715222552651));
#42993=CARTESIAN_POINT('Ctrl Pts',(-83.5298629382456,3.06691707187941,-2.92999705662308));
#42994=CARTESIAN_POINT('Ctrl Pts',(-83.4113308389955,4.0923167299564,-1.11526089294132));
#42995=CARTESIAN_POINT('Ctrl Pts',(-83.2927987397454,4.12944046598591,0.968805716066663));
#42996=CARTESIAN_POINT('Ctrl Pts',(-83.1742666404953,3.16932306615985,2.81891014044657));
#42997=CARTESIAN_POINT('Ctrl Pts',(-83.0557345412452,1.44382852615606,3.98826055626553));
#42998=CARTESIAN_POINT('Ctrl Pts',(-82.9372024419952,-0.630344051771873,
4.19446414384497));
#42999=CARTESIAN_POINT('Ctrl Pts',(-82.818670342745,-2.55229140128288,3.38772367240052));
#43000=CARTESIAN_POINT('Ctrl Pts',(-82.7055404184379,-3.79836930332596,
1.83691733808824));
#43001=CARTESIAN_POINT('Ctrl Pts',(-82.6319211938809,-4.07016704624553,
0.581394268202383));
#43002=CARTESIAN_POINT('Ctrl Pts',(-82.5978126690739,-4.07069297892822,
-8.16732152923022E-5));
#43003=CARTESIAN_POINT('Ctrl Pts',(-83.8021873309262,-4.07069555842019,
-8.11031842551206E-5));
#43004=CARTESIAN_POINT('Ctrl Pts',(-83.7968397355401,-4.07077761748435,
-0.0912457722533375));
#43005=CARTESIAN_POINT('Ctrl Pts',(-83.751981440404,-4.04560590414255,-0.855935203987643));
#43006=CARTESIAN_POINT('Ctrl Pts',(-83.6676124455178,-3.58531215974383,
-2.26636268917237));
#43007=CARTESIAN_POINT('Ctrl Pts',(-83.5490803462679,-2.07279741151507,
-3.70059103556392));
#43008=CARTESIAN_POINT('Ctrl Pts',(-83.4305482470176,-0.0597114933943472,
-4.24114343771067));
#43009=CARTESIAN_POINT('Ctrl Pts',(-83.3120161477677,1.96779447944969,-3.75747894316481));
#43010=CARTESIAN_POINT('Ctrl Pts',(-83.1934840485175,3.52008701406145,-2.36640033280838));
#43011=CARTESIAN_POINT('Ctrl Pts',(-83.0749519492674,4.22229450661292,-0.403846779244268));
#43012=CARTESIAN_POINT('Ctrl Pts',(-82.9564198500173,3.90483703380788,1.65623393911674));
#43013=CARTESIAN_POINT('Ctrl Pts',(-82.8378877507673,2.64437913491587,3.31634167607942));
#43014=CARTESIAN_POINT('Ctrl Pts',(-82.7193556515171,0.745315673391867,
4.17556794564238));
#43015=CARTESIAN_POINT('Ctrl Pts',(-82.6008235522671,-1.33373814150481,
4.02641350230884));
#43016=CARTESIAN_POINT('Ctrl Pts',(-82.482291453017,-3.09070024685299,2.90489846737928));
#43017=CARTESIAN_POINT('Ctrl Pts',(-82.3827460459034,-3.93939696035747,
1.37388074382986));
#43018=CARTESIAN_POINT('Ctrl Pts',(-82.3227113385397,-4.07012516230206,
0.350009002499383));
#43019=CARTESIAN_POINT('Ctrl Pts',(-82.3021873309261,-4.07016134870022,
-1.1973211870471E-5));
#43020=CARTESIAN_POINT('Origin',(-92.3478126690739,0.,0.));
#43021=CARTESIAN_POINT('',(-85.5978126690739,-4.07017509531035,-3.25600794716127E-5));
#43022=CARTESIAN_POINT('',(-85.3021873309261,-4.07054479772079,0.000101412767817208));
#43023=CARTESIAN_POINT('',(-92.3478126690739,-4.0705,-4.39132641279065E-13));
#43024=CARTESIAN_POINT('Ctrl Pts',(-85.5978126690739,-4.07017509531035,
-3.25600794716038E-5));
#43025=CARTESIAN_POINT('Ctrl Pts',(-85.5801779878816,-4.07026000090821,
-0.300775414177721));
#43026=CARTESIAN_POINT('Ctrl Pts',(-85.5230326069393,-3.96366872821567,
-1.27527671801632));
#43027=CARTESIAN_POINT('Ctrl Pts',(-85.426376526247,-3.19411212591926,-2.79079035483874));
#43028=CARTESIAN_POINT('Ctrl Pts',(-85.3078444269969,-1.47901940386148,
-3.97534459897585));
#43029=CARTESIAN_POINT('Ctrl Pts',(-85.1893123277468,0.593249793413271,
-4.19987115995485));
#43030=CARTESIAN_POINT('Ctrl Pts',(-85.0707802284967,2.52225185735541,-3.41014789205285));
#43031=CARTESIAN_POINT('Ctrl Pts',(-84.9522481292466,3.84214154206329,-1.79688938122436));
#43032=CARTESIAN_POINT('Ctrl Pts',(-84.8337160299966,4.23417147746969,0.250309762069736));
#43033=CARTESIAN_POINT('Ctrl Pts',(-84.7151839307464,3.60366821294754,2.23706023356476));
#43034=CARTESIAN_POINT('Ctrl Pts',(-84.5966518314964,2.10289542607052,3.6835708089593));
#43035=CARTESIAN_POINT('Ctrl Pts',(-84.4781197322463,0.094282935351365,
4.24051574760746));
#43036=CARTESIAN_POINT('Ctrl Pts',(-84.3595876329963,-1.9370984564613,3.77339537387491));
#43037=CARTESIAN_POINT('Ctrl Pts',(-84.241055533746,-3.50067936031506,2.39501713853357));
#43038=CARTESIAN_POINT('Ctrl Pts',(-84.1537972124387,-4.02937512391122,
0.954530185624109));
#43039=CARTESIAN_POINT('Ctrl Pts',(-84.1060495908813,-4.07069068490978,
0.140537253042811));
#43040=CARTESIAN_POINT('Ctrl Pts',(-84.0978126690739,-4.07054770473266,
0.000101237284118993));
#43041=CARTESIAN_POINT('Ctrl Pts',(-85.3021873309262,-4.07054479772079,
0.000101412767817364));
#43042=CARTESIAN_POINT('Ctrl Pts',(-85.2709681325404,-4.07000279076567,
-0.53217374801187));
#43043=CARTESIAN_POINT('Ctrl Pts',(-85.2002382344046,-3.83218071396426,
-1.73856103852625));
#43044=CARTESIAN_POINT('Ctrl Pts',(-85.089997636519,-2.67358487308622,-3.29284178910621));
#43045=CARTESIAN_POINT('Ctrl Pts',(-84.9714655372688,-0.782189207191325,
-4.16881795786684));
#43046=CARTESIAN_POINT('Ctrl Pts',(-84.8529334380188,1.29810160318103,-4.03804350515179));
#43047=CARTESIAN_POINT('Ctrl Pts',(-84.7344013387685,3.06490676631494,-2.93209986792342));
#43048=CARTESIAN_POINT('Ctrl Pts',(-84.6158692395186,4.09155085191131,-1.11806741652885));
#43049=CARTESIAN_POINT('Ctrl Pts',(-84.4973371402684,4.13010397153302,0.965973242904165));
#43050=CARTESIAN_POINT('Ctrl Pts',(-84.3788050410185,3.17125572172011,2.81673574712594));
#43051=CARTESIAN_POINT('Ctrl Pts',(-84.2602729417682,1.44656360418077,3.98726934890774));
#43052=CARTESIAN_POINT('Ctrl Pts',(-84.1417408425183,-0.627467060215684,
4.19489549452951));
#43053=CARTESIAN_POINT('Ctrl Pts',(-84.0232087432681,-2.54996727660215,
3.38947341189422));
#43054=CARTESIAN_POINT('Ctrl Pts',(-83.9100242394041,-3.79771021737389,
1.83877430965476));
#43055=CARTESIAN_POINT('Ctrl Pts',(-83.8363504352901,-4.07017132422319,
0.582324235826637));
#43056=CARTESIAN_POINT('Ctrl Pts',(-83.8021873309262,-4.07069555842019,
-8.11031842551206E-5));
#43057=CARTESIAN_POINT('Origin',(-92.3478126690739,0.,0.));
#43058=CARTESIAN_POINT('',(-87.0978126690739,-4.07075463294496,-6.48897006623938E-5));
#43059=CARTESIAN_POINT('',(-86.8021873309262,-4.0701759211548,-3.33690431755795E-5));
#43060=CARTESIAN_POINT('',(-92.3478126690739,-4.0705,-4.39132641279065E-13));
#43061=CARTESIAN_POINT('Ctrl Pts',(-87.0978126690739,-4.07075463294496,
-6.48897006625716E-5));
#43062=CARTESIAN_POINT('Ctrl Pts',(-87.093817084632,-4.07080662684575,-0.0681779009651227));
#43063=CARTESIAN_POINT('Ctrl Pts',(-87.05031080044,-4.05257240534199,-0.809804772914534));
#43064=CARTESIAN_POINT('Ctrl Pts',(-86.9672938164981,-3.62329806373565,
-2.2051245358312));
#43065=CARTESIAN_POINT('Ctrl Pts',(-86.848761717248,-2.1353677918245,-3.66484208003093));
#43066=CARTESIAN_POINT('Ctrl Pts',(-86.730229617998,-0.131755887070526,
-4.23951689036003));
#43067=CARTESIAN_POINT('Ctrl Pts',(-86.6116975187478,1.90367446658495,-3.7903676078918));
#43068=CARTESIAN_POINT('Ctrl Pts',(-86.4931654194978,3.47937607418291,-2.42586174626368));
#43069=CARTESIAN_POINT('Ctrl Pts',(-86.3746333202476,4.21482414698068,-0.475521279897397));
#43070=CARTESIAN_POINT('Ctrl Pts',(-86.2561012209977,3.93241131237811,1.58965541797289));
#43071=CARTESIAN_POINT('Ctrl Pts',(-86.1375691217474,2.70033898852751,3.27093754520615));
#43072=CARTESIAN_POINT('Ctrl Pts',(-86.0190370224974,0.816147051306786,
4.16230309663427));
#43073=CARTESIAN_POINT('Ctrl Pts',(-85.9005049232474,-1.26514069566702,
4.04849133601287));
#43074=CARTESIAN_POINT('Ctrl Pts',(-85.7819728239972,-3.04090270501211,
2.95698728713125));
#43075=CARTESIAN_POINT('Ctrl Pts',(-85.6810754059395,-3.92736595192102,
1.42001385856659));
#43076=CARTESIAN_POINT('Ctrl Pts',(-85.6196886876317,-4.07006976896994,
0.373042302212225));
#43077=CARTESIAN_POINT('Ctrl Pts',(-85.5978126690739,-4.07017509531035,
-3.25600794716038E-5));
#43078=CARTESIAN_POINT('Ctrl Pts',(-86.8021873309262,-4.0701759211548,-3.33690431757877E-5));
#43079=CARTESIAN_POINT('Ctrl Pts',(-86.7846072292908,-4.07026268870466,
-0.299845247585942));
#43080=CARTESIAN_POINT('Ctrl Pts',(-86.7275164279055,-3.96410850627354,
-1.27341394546106));
#43081=CARTESIAN_POINT('Ctrl Pts',(-86.63091492677,-3.19602548924936,-2.78859896610174));
#43082=CARTESIAN_POINT('Ctrl Pts',(-86.51238282752,-1.48174561502481,-3.97432925838274));
#43083=CARTESIAN_POINT('Ctrl Pts',(-86.3938507282698,0.590369102043211,
-4.20027706765055));
#43084=CARTESIAN_POINT('Ctrl Pts',(-86.2753186290198,2.51991235967365,-3.41187702317127));
#43085=CARTESIAN_POINT('Ctrl Pts',(-86.1567865297697,3.84090821614495,-1.79952415844573));
#43086=CARTESIAN_POINT('Ctrl Pts',(-86.0382544305196,4.234342165928,0.247405625489327));
#43087=CARTESIAN_POINT('Ctrl Pts',(-85.9197223312695,3.6052016952943,2.23458807343251));
#43088=CARTESIAN_POINT('Ctrl Pts',(-85.8011902320195,2.10542137327692,3.68212764073006));
#43089=CARTESIAN_POINT('Ctrl Pts',(-85.6826581327693,0.0971913426281407,
4.24045008986049));
#43090=CARTESIAN_POINT('Ctrl Pts',(-85.5641260335193,-1.93450995627506,
3.77472308265816));
#43091=CARTESIAN_POINT('Ctrl Pts',(-85.4455939342692,-3.49903587826941,
2.39741757820016));
#43092=CARTESIAN_POINT('Ctrl Pts',(-85.3582810334048,-4.0290508143939,0.956392788326129));
#43093=CARTESIAN_POINT('Ctrl Pts',(-85.3104788322905,-4.07068874925191,
0.141468278350529));
#43094=CARTESIAN_POINT('Ctrl Pts',(-85.3021873309262,-4.07054479772079,
0.000101412767817364));
#43095=CARTESIAN_POINT('Origin',(-92.3478126690739,0.,0.));
#43096=CARTESIAN_POINT('',(-88.5978126690739,-4.07047297420895,0.00010377974335732));
#43097=CARTESIAN_POINT('',(-88.3021873309261,-4.07075680315938,-6.41537658660485E-5));
#43098=CARTESIAN_POINT('',(-92.3478126690739,-4.0705,-4.39132641279065E-13));
#43099=CARTESIAN_POINT('Ctrl Pts',(-88.5978126690739,-4.07047297420895,
0.000103779743357239));
#43100=CARTESIAN_POINT('Ctrl Pts',(-88.5679454816323,-4.0699633629615,-0.509146035156339));
#43101=CARTESIAN_POINT('Ctrl Pts',(-88.4985675944407,-3.84728083634177,
-1.69250630808891));
#43102=CARTESIAN_POINT('Ctrl Pts',(-88.3896790074992,-2.72914125118652,
-3.24694449006369));
#43103=CARTESIAN_POINT('Ctrl Pts',(-88.271146908249,-0.852900597114338,
-4.15492782628333));
#43104=CARTESIAN_POINT('Ctrl Pts',(-88.152614808999,1.22931172268961,-4.05951413513238));
#43105=CARTESIAN_POINT('Ctrl Pts',(-88.0340827097489,3.01465081869963,-2.98374660176146));
#43106=CARTESIAN_POINT('Ctrl Pts',(-87.9155506104989,4.07196543070694,-1.18741760272948));
#43107=CARTESIAN_POINT('Ctrl Pts',(-87.7970185112487,4.1459188620231,0.895667260529816));
#43108=CARTESIAN_POINT('Ctrl Pts',(-87.6784864119986,3.21865170212703,2.76245259353163));
#43109=CARTESIAN_POINT('Ctrl Pts',(-87.5599543127485,1.51409475903765,3.96211813494982));
#43110=CARTESIAN_POINT('Ctrl Pts',(-87.4414222134985,-0.556109197774073,
4.20495013639211));
#43111=CARTESIAN_POINT('Ctrl Pts',(-87.3228901142483,-2.49201530688875,
3.43230575316451));
#43112=CARTESIAN_POINT('Ctrl Pts',(-87.2083535994403,-3.78114015235693,
1.88476091323141));
#43113=CARTESIAN_POINT('Ctrl Pts',(-87.133327784382,-4.07029248043415,0.605363798947223));
#43114=CARTESIAN_POINT('Ctrl Pts',(-87.0978126690739,-4.07075463294496,
-6.48897006625716E-5));
#43115=CARTESIAN_POINT('Ctrl Pts',(-88.3021873309261,-4.07075680315937,
-6.4153765865849E-5));
#43116=CARTESIAN_POINT('Ctrl Pts',(-88.2982463260412,-4.07080763529163,
-0.0672466394881131));
#43117=CARTESIAN_POINT('Ctrl Pts',(-88.2547946214061,-4.05284527665673,
-0.807942598938564));
#43118=CARTESIAN_POINT('Ctrl Pts',(-88.1718322170211,-3.62480963907511,
-2.20263892537862));
#43119=CARTESIAN_POINT('Ctrl Pts',(-88.0533001177711,-2.13788088541058,
-3.6633766416475));
#43120=CARTESIAN_POINT('Ctrl Pts',(-87.9347680185209,-0.134663600797729,
-4.23942553278804));
#43121=CARTESIAN_POINT('Ctrl Pts',(-87.8162359192709,1.9010743336757,-3.79167238760187));
#43122=CARTESIAN_POINT('Ctrl Pts',(-87.6977038200208,3.47771144175241,-2.42824756783923));
#43123=CARTESIAN_POINT('Ctrl Pts',(-87.5791717207707,4.2144970165252,-0.478411976782104));
#43124=CARTESIAN_POINT('Ctrl Pts',(-87.4606396215207,3.93350068426081,1.58695793523026));
#43125=CARTESIAN_POINT('Ctrl Pts',(-87.3421075222705,2.70258178445977,3.26908470681113));
#43126=CARTESIAN_POINT('Ctrl Pts',(-87.2235754230204,0.819001646208479,
4.16174235447228));
#43127=CARTESIAN_POINT('Ctrl Pts',(-87.1050433237704,-1.2623636734931,4.04935810686113));
#43128=CARTESIAN_POINT('Ctrl Pts',(-86.9865112245203,-3.03887389383025,
2.95907224971836));
#43129=CARTESIAN_POINT('Ctrl Pts',(-86.8855592269055,-3.92687118700315,
1.42187609361087));
#43130=CARTESIAN_POINT('Ctrl Pts',(-86.8241179290408,-4.07006768149243,
0.373972080681628));
#43131=CARTESIAN_POINT('Ctrl Pts',(-86.8021873309262,-4.0701759211548,-3.33690431757877E-5));
#43132=CARTESIAN_POINT('Origin',(-59.25,4.52129938221115E-16,0.));
#43133=CARTESIAN_POINT('Ctrl Pts',(-59.25,3.73370339826923,1.62162243917753));
#43134=CARTESIAN_POINT('Ctrl Pts',(-59.25,3.70030638409769,1.72678322255912));
#43135=CARTESIAN_POINT('Ctrl Pts',(-59.25,3.66264502024489,1.83042819249524));
#43136=CARTESIAN_POINT('Ctrl Pts',(-59.25,3.62080294009585,1.93228746156618));
#43137=CARTESIAN_POINT('Ctrl Pts',(-59.25,3.57306535757599,2.04849858790993));
#43138=CARTESIAN_POINT('Ctrl Pts',(-59.25,3.51988717582558,2.16238619955646));
#43139=CARTESIAN_POINT('Ctrl Pts',(-59.25,3.46157351130409,2.27367045215858));
#43140=CARTESIAN_POINT('Ctrl Pts',(-59.25,3.42831099083415,2.33714776507546));
#43141=CARTESIAN_POINT('Ctrl Pts',(-59.25,3.3933765912802,2.39977793900337));
#43142=CARTESIAN_POINT('Ctrl Pts',(-59.25,3.35681960546461,2.46150741409173));
#43143=CARTESIAN_POINT('Ctrl Pts',(-59.25,3.33178364519508,2.50378269065766));
#43144=CARTESIAN_POINT('Ctrl Pts',(-59.25,3.30598655682051,2.54563549772312));
#43145=CARTESIAN_POINT('Ctrl Pts',(-59.25,3.27944283224882,2.58704812709493));
#43146=CARTESIAN_POINT('Ctrl Pts',(-59.25,3.26794189314794,2.60499150678627));
#43147=CARTESIAN_POINT('Ctrl Pts',(-59.25,3.25630353761244,2.62284785295622));
#43148=CARTESIAN_POINT('Ctrl Pts',(-59.25,3.24453365056515,2.64060915444784));
#43149=CARTESIAN_POINT('Ctrl Pts',(-59.25,3.17311768024368,2.74837914196769));
#43150=CARTESIAN_POINT('Ctrl Pts',(-59.25,3.09681512798329,2.85272629165589));
#43151=CARTESIAN_POINT('Ctrl Pts',(-59.25,3.01594945594691,2.95335783811544));
#43152=CARTESIAN_POINT('Ctrl Pts',(-59.25,2.93456493547749,3.05463505434908));
#43153=CARTESIAN_POINT('Ctrl Pts',(-59.25,2.84855818714407,3.15214957100135));
#43154=CARTESIAN_POINT('Ctrl Pts',(-59.25,2.7582089599964,3.24558571221565));
#43155=CARTESIAN_POINT('Ctrl Pts',(-59.25,2.72369285823248,3.28128110729978));
#43156=CARTESIAN_POINT('Ctrl Pts',(-59.25,2.68854249786815,3.31638103986582));
#43157=CARTESIAN_POINT('Ctrl Pts',(-59.25,2.65277174372166,3.35086689904567));
#43158=CARTESIAN_POINT('Ctrl Pts',(-59.25,2.63289346302342,3.37003114663433));
#43159=CARTESIAN_POINT('Ctrl Pts',(-59.25,2.61282357777559,3.38900574658438));
#43160=CARTESIAN_POINT('Ctrl Pts',(-59.25,2.59256434889638,3.40778741403533));
#43161=CARTESIAN_POINT('Ctrl Pts',(-59.25,2.57182031456538,3.4270185287396));
#43162=CARTESIAN_POINT('Ctrl Pts',(-59.25,2.55087325423301,3.44605124301962));
#43163=CARTESIAN_POINT('Ctrl Pts',(-59.25,2.52975088546925,3.46485978106417));
#43164=CARTESIAN_POINT('Ctrl Pts',(-59.25,2.47960903746643,3.50950888582762));
#43165=CARTESIAN_POINT('Ctrl Pts',(-59.25,2.42845837805422,3.5529152668294));
#43166=CARTESIAN_POINT('Ctrl Pts',(-59.25,2.37634253095915,3.59504099741696));
#43167=CARTESIAN_POINT('Ctrl Pts',(-59.25,2.27551221171727,3.67654309515114));
#43168=CARTESIAN_POINT('Ctrl Pts',(-59.25,2.17107182552093,3.75325338346143));
#43169=CARTESIAN_POINT('Ctrl Pts',(-59.25,2.06344354535521,3.82509569453245));
#43170=CARTESIAN_POINT('Ctrl Pts',(-59.25,1.95411483048912,3.89807305262374));
#43171=CARTESIAN_POINT('Ctrl Pts',(-59.25,1.84149617014203,3.96602787167803));
#43172=CARTESIAN_POINT('Ctrl Pts',(-59.25,1.72598702798438,4.02884810767464));
#43173=CARTESIAN_POINT('Ctrl Pts',(-59.25,1.6224562778767,4.08515383407155));
#43174=CARTESIAN_POINT('Ctrl Pts',(-59.25,1.51660255473828,4.13733445853516));
#43175=CARTESIAN_POINT('Ctrl Pts',(-59.25,1.40869034106602,4.18528315122508));
#43176=CARTESIAN_POINT('Ctrl Pts',(-59.25,1.32775618081182,4.22124467074251));
#43177=CARTESIAN_POINT('Ctrl Pts',(-59.25,1.24566363779897,4.25482524316704));
#43178=CARTESIAN_POINT('Ctrl Pts',(-59.25,1.1625182592197,4.2859693893738));
#43179=CARTESIAN_POINT('Ctrl Pts',(-59.25,1.14549561314186,4.29234564007268));
#43180=CARTESIAN_POINT('Ctrl Pts',(-59.25,1.12842677920724,4.29862046901966));
#43181=CARTESIAN_POINT('Ctrl Pts',(-59.25,1.11131922234629,4.30479098303606));
#43182=CARTESIAN_POINT('Ctrl Pts',(-59.25,0.98320067627071,4.35100198152908));
#43183=CARTESIAN_POINT('Ctrl Pts',(-59.25,0.85324085305285,4.39124906607606));
#43184=CARTESIAN_POINT('Ctrl Pts',(-59.25,0.721878465181344,4.42543828020427));
#43185=CARTESIAN_POINT('Ctrl Pts',(-59.25,0.613754215266846,4.4535793881171));
#43186=CARTESIAN_POINT('Ctrl Pts',(-59.25,0.504678753627349,4.47761582662026));
#43187=CARTESIAN_POINT('Ctrl Pts',(-59.25,0.39487946495906,4.49747515579454));
#43188=CARTESIAN_POINT('Ctrl Pts',(-59.25,0.262138836200427,4.52148387090821));
#43189=CARTESIAN_POINT('Ctrl Pts',(-59.25,0.128340414767412,4.53938931245444));
#43190=CARTESIAN_POINT('Ctrl Pts',(-59.25,-0.0061098054212493,4.55128614781597));
#43191=CARTESIAN_POINT('Ctrl Pts',(-59.25,-0.141656910697344,4.56328004111668));
#43192=CARTESIAN_POINT('Ctrl Pts',(-59.25,-0.27786725021061,4.56916700363061));
#43193=CARTESIAN_POINT('Ctrl Pts',(-59.25,-0.414338511577332,4.56899300375995));
#43194=CARTESIAN_POINT('Ctrl Pts',(-59.25,-0.46130902680036,4.56893311669294));
#43195=CARTESIAN_POINT('Ctrl Pts',(-59.25,-0.508310516274796,4.56815480456615));
#43196=CARTESIAN_POINT('Ctrl Pts',(-59.25,-0.555326693203861,4.56665852086362));
#43197=CARTESIAN_POINT('Ctrl Pts',(-59.25,-0.574417009651001,4.56605097403099));
#43198=CARTESIAN_POINT('Ctrl Pts',(-59.25,-0.593511702466989,4.56532496172441));
#43199=CARTESIAN_POINT('Ctrl Pts',(-59.25,-0.612603479656446,4.56448075813901));
#43200=CARTESIAN_POINT('Ctrl Pts',(-59.25,-0.751213987889701,4.55835165413454));
#43201=CARTESIAN_POINT('Ctrl Pts',(-59.25,-0.889274990910051,4.54601536277982));
#43202=CARTESIAN_POINT('Ctrl Pts',(-59.25,-1.02635580814156,4.52760979279899));
#43203=CARTESIAN_POINT('Ctrl Pts',(-59.25,-1.17093917736832,4.50819687001292));
#43204=CARTESIAN_POINT('Ctrl Pts',(-59.25,-1.31443290670101,4.48203265993226));
#43205=CARTESIAN_POINT('Ctrl Pts',(-59.25,-1.45634950900623,4.44921976842928));
#43206=CARTESIAN_POINT('Ctrl Pts',(-59.25,-1.59826611131146,4.41640687692631));
#43207=CARTESIAN_POINT('Ctrl Pts',(-59.25,-1.73860660530752,4.37694532748719));
#43208=CARTESIAN_POINT('Ctrl Pts',(-59.25,-1.87688689423306,4.33087666257546));
#43209=CARTESIAN_POINT('Ctrl Pts',(-59.25,-1.97170999958983,4.29928594273741));
#43210=CARTESIAN_POINT('Ctrl Pts',(-59.25,-2.06556440611198,4.26458709411248));
#43211=CARTESIAN_POINT('Ctrl Pts',(-59.25,-2.15833273047387,4.22686765274433));
#43212=CARTESIAN_POINT('Ctrl Pts',(-59.25,-2.19891887238219,4.21036539714576));
#43213=CARTESIAN_POINT('Ctrl Pts',(-59.25,-2.2392970843243,4.19328480879033));
#43214=CARTESIAN_POINT('Ctrl Pts',(-59.25,-2.27945727353288,4.17563243334272));
#43215=CARTESIAN_POINT('Ctrl Pts',(-59.25,-2.30456458384424,4.16459653742614));
#43216=CARTESIAN_POINT('Ctrl Pts',(-59.25,-2.32958667668184,4.15333714984871));
#43217=CARTESIAN_POINT('Ctrl Pts',(-59.25,-2.35452104605308,4.14185577889582));
#43218=CARTESIAN_POINT('Ctrl Pts',(-59.25,-2.37061736322258,4.13444400979725));
#43219=CARTESIAN_POINT('Ctrl Pts',(-59.25,-2.38667325540531,4.12694148008939));
#43220=CARTESIAN_POINT('Ctrl Pts',(-59.25,-2.40268097740313,4.11935218483388));
#43221=CARTESIAN_POINT('Ctrl Pts',(-59.25,-2.52978167954032,4.05909346995659));
#43222=CARTESIAN_POINT('Ctrl Pts',(-59.25,-2.65398157892713,3.99330674132034));
#43223=CARTESIAN_POINT('Ctrl Pts',(-59.25,-2.77498221207584,3.92231859342991));
#43224=CARTESIAN_POINT('Ctrl Pts',(-59.25,-2.89853629781064,3.84983239660291));
#43225=CARTESIAN_POINT('Ctrl Pts',(-59.25,-3.01875535833896,3.77192276608097));
#43226=CARTESIAN_POINT('Ctrl Pts',(-59.25,-3.13531440596932,3.68888383868272));
#43227=CARTESIAN_POINT('Ctrl Pts',(-59.25,-3.25228861614668,3.60554914142963));
#43228=CARTESIAN_POINT('Ctrl Pts',(-59.25,-3.36557741397246,3.51704820512911));
#43229=CARTESIAN_POINT('Ctrl Pts',(-59.25,-3.47483444492779,3.42362900180858));
#43230=CARTESIAN_POINT('Ctrl Pts',(-59.25,-3.58315056993114,3.33101431132959));
#43231=CARTESIAN_POINT('Ctrl Pts',(-59.25,-3.68750474245897,3.2335652796617));
#43232=CARTESIAN_POINT('Ctrl Pts',(-59.25,-3.78753162267819,3.13148094463183));
#43233=CARTESIAN_POINT('Ctrl Pts',(-59.25,-3.8168940019152,3.10151461005521));
#43234=CARTESIAN_POINT('Ctrl Pts',(-59.25,-3.84588328389748,3.07114859897418));
#43235=CARTESIAN_POINT('Ctrl Pts',(-59.25,-3.87448963569914,3.04038732119116));
#43236=CARTESIAN_POINT('',(-59.25,-4.77631074058413,-1.20178265305869));
#43237=CARTESIAN_POINT('Origin',(-59.25,0.,0.));
#43238=CARTESIAN_POINT('Ctrl Pts',(-59.25,-4.77631074058413,-1.20178265305869));
#43239=CARTESIAN_POINT('Ctrl Pts',(-59.25,-4.73353179200075,-1.32696589596601));
#43240=CARTESIAN_POINT('Ctrl Pts',(-59.25,-4.6857353234603,-1.45022519891399));
#43241=CARTESIAN_POINT('Ctrl Pts',(-59.25,-4.63294581112938,-1.57123974166275));
#43242=CARTESIAN_POINT('Ctrl Pts',(-59.25,-4.57511560091207,-1.70380956732513));
#43243=CARTESIAN_POINT('Ctrl Pts',(-59.25,-4.51129338536423,-1.83368642289548));
#43244=CARTESIAN_POINT('Ctrl Pts',(-59.25,-4.44173477384968,-1.96050991602634));
#43245=CARTESIAN_POINT('Ctrl Pts',(-59.25,-4.40262471266493,-2.03181775941211));
#43246=CARTESIAN_POINT('Ctrl Pts',(-59.25,-4.3617004223149,-2.10215974213619));
#43247=CARTESIAN_POINT('Ctrl Pts',(-59.25,-4.31900226670184,-2.17146662848551));
#43248=CARTESIAN_POINT('Ctrl Pts',(-59.25,-4.28594231940442,-2.22512894661517));
#43249=CARTESIAN_POINT('Ctrl Pts',(-59.25,-4.25181887239913,-2.27817065668745));
#43250=CARTESIAN_POINT('Ctrl Pts',(-59.25,-4.21664938444057,-2.33055784224177));
#43251=CARTESIAN_POINT('Ctrl Pts',(-59.25,-4.20538410111805,-2.34733819708897));
#43252=CARTESIAN_POINT('Ctrl Pts',(-59.25,-4.19401242684272,-2.36404991219832));
#43253=CARTESIAN_POINT('Ctrl Pts',(-59.25,-4.18254029751914,-2.3806843491385));
#43254=CARTESIAN_POINT('Ctrl Pts',(-59.25,-4.10178449304619,-2.4977792056528));
#43255=CARTESIAN_POINT('Ctrl Pts',(-59.25,-4.01598249499716,-2.61115479677391));
#43256=CARTESIAN_POINT('Ctrl Pts',(-59.25,-3.92538451237541,-2.72046840686664));
#43257=CARTESIAN_POINT('Ctrl Pts',(-59.25,-3.83550276971064,-2.82891781697254));
#43258=CARTESIAN_POINT('Ctrl Pts',(-59.25,-3.74089999144967,-2.93336972028254));
#43259=CARTESIAN_POINT('Ctrl Pts',(-59.25,-3.64178917502125,-3.03344935010836));
#43260=CARTESIAN_POINT('Ctrl Pts',(-59.25,-3.57026391056714,-3.10567377775125));
#43261=CARTESIAN_POINT('Ctrl Pts',(-59.25,-3.49639015724155,-3.17562028805039));
#43262=CARTESIAN_POINT('Ctrl Pts',(-59.25,-3.42024023020396,-3.24313265702998));
#43263=CARTESIAN_POINT('Ctrl Pts',(-59.25,-3.40538944723384,-3.25629894068275));
#43264=CARTESIAN_POINT('Ctrl Pts',(-59.25,-3.39045018710911,-3.26937423378017));
#43265=CARTESIAN_POINT('Ctrl Pts',(-59.25,-3.37542919856903,-3.28235193981733));
#43266=CARTESIAN_POINT('Ctrl Pts',(-59.25,-3.31342750193073,-3.33591963881594));
#43267=CARTESIAN_POINT('Ctrl Pts',(-59.25,-3.25009665988727,-3.38777142952235));
#43268=CARTESIAN_POINT('Ctrl Pts',(-59.25,-3.18548516409361,-3.43784341538071));
#43269=CARTESIAN_POINT('Ctrl Pts',(-59.25,-3.07590904070656,-3.52276164909831));
#43270=CARTESIAN_POINT('Ctrl Pts',(-59.25,-2.96265082171774,-3.60256350100977));
#43271=CARTESIAN_POINT('Ctrl Pts',(-59.25,-2.84610495743846,-3.67709913006717));
#43272=CARTESIAN_POINT('Ctrl Pts',(-59.25,-2.72927364023283,-3.75181731741237));
#43273=CARTESIAN_POINT('Ctrl Pts',(-59.25,-2.60913776602312,-3.8212437224481));
#43274=CARTESIAN_POINT('Ctrl Pts',(-59.25,-2.48607529075415,-3.88517902227304));
#43275=CARTESIAN_POINT('Ctrl Pts',(-59.25,-2.3787050182169,-3.94096166886738));
#43276=CARTESIAN_POINT('Ctrl Pts',(-59.25,-2.26910631512645,-3.99256368168234));
#43277=CARTESIAN_POINT('Ctrl Pts',(-59.25,-2.15752519659779,-4.03982030716511));
#43278=CARTESIAN_POINT('Ctrl Pts',(-59.25,-2.0738393577013,-4.07526277627718));
#43279=CARTESIAN_POINT('Ctrl Pts',(-59.25,-1.98903828425897,-4.10826035675606));
#43280=CARTESIAN_POINT('Ctrl Pts',(-59.25,-1.90322614380203,-4.13873171989141));
#43281=CARTESIAN_POINT('Ctrl Pts',(-59.25,-1.8843717581363,-4.14542679624371));
#43282=CARTESIAN_POINT('Ctrl Pts',(-59.25,-1.86546856747819,-4.1519998780532));
#43283=CARTESIAN_POINT('Ctrl Pts',(-59.25,-1.8465176865997,-4.15845003453348));
#43284=CARTESIAN_POINT('Ctrl Pts',(-59.25,-1.83130602442166,-4.16362750369719));
#43285=CARTESIAN_POINT('Ctrl Pts',(-59.25,-1.81606476693151,-4.16872534849972));
#43286=CARTESIAN_POINT('Ctrl Pts',(-59.25,-1.80080388427029,-4.17374013987465));
#43287=CARTESIAN_POINT('Ctrl Pts',(-59.25,-1.67249942992059,-4.21590153285044));
#43288=CARTESIAN_POINT('Ctrl Pts',(-59.25,-1.5426287282479,-4.25225822040849));
#43289=CARTESIAN_POINT('Ctrl Pts',(-59.25,-1.41154865683054,-4.28264911633847));
#43290=CARTESIAN_POINT('Ctrl Pts',(-59.25,-1.3124362801824,-4.30562830677922));
#43291=CARTESIAN_POINT('Ctrl Pts',(-59.25,-1.21263206758244,-4.32519576401433));
#43292=CARTESIAN_POINT('Ctrl Pts',(-59.25,-1.11228793538546,-4.34126217629354));
#43293=CARTESIAN_POINT('Ctrl Pts',(-59.25,-0.979035358188069,-4.36259766244154));
#43294=CARTESIAN_POINT('Ctrl Pts',(-59.25,-0.844829892568941,-4.37776087849656));
#43295=CARTESIAN_POINT('Ctrl Pts',(-59.25,-0.710100950691535,-4.38675752439951));
#43296=CARTESIAN_POINT('Ctrl Pts',(-59.25,-0.576496800019825,-4.39567906136112));
#43297=CARTESIAN_POINT('Ctrl Pts',(-59.25,-0.442377092384796,-4.3985363451751));
#43298=CARTESIAN_POINT('Ctrl Pts',(-59.25,-0.308176480047048,-4.39528647850796));
#43299=CARTESIAN_POINT('Ctrl Pts',(-59.25,-0.261458280238702,-4.39415512807922));
#43300=CARTESIAN_POINT('Ctrl Pts',(-59.25,-0.214730472181454,-4.39228324020791));
#43301=CARTESIAN_POINT('Ctrl Pts',(-59.25,-0.168012117042926,-4.38966768275966));
#43302=CARTESIAN_POINT('Ctrl Pts',(-59.25,-0.142145356406747,-4.38821951536928));
#43303=CARTESIAN_POINT('Ctrl Pts',(-59.25,-0.116275424988109,-4.38654282160773));
#43304=CARTESIAN_POINT('Ctrl Pts',(-59.25,-0.0904392486155291,-4.38463973183507));
#43305=CARTESIAN_POINT('Ctrl Pts',(-59.25,0.0410133206382076,-4.37495695074047));
#43306=CARTESIAN_POINT('Ctrl Pts',(-59.25,0.171725828963868,-4.35941295456871));
#43307=CARTESIAN_POINT('Ctrl Pts',(-59.25,0.301301898250337,-4.33804997480716));
#43308=CARTESIAN_POINT('Ctrl Pts',(-59.25,0.429447519281489,-4.31692283054592));
#43309=CARTESIAN_POINT('Ctrl Pts',(-59.25,0.556482392005791,-4.29010420308145));
#43310=CARTESIAN_POINT('Ctrl Pts',(-59.25,0.682008049033365,-4.25758697212456));
#43311=CARTESIAN_POINT('Ctrl Pts',(-59.25,0.802901216297604,-4.22626978061066));
#43312=CARTESIAN_POINT('Ctrl Pts',(-59.25,0.922395005914746,-4.18966643744355));
#43313=CARTESIAN_POINT('Ctrl Pts',(-59.25,1.04011060800678,-4.14773097044074));
#43314=CARTESIAN_POINT('Ctrl Pts',(-59.25,1.12177492014559,-4.11863855612911));
#43315=CARTESIAN_POINT('Ctrl Pts',(-59.25,1.2025829258255,-4.08697895456957));
#43316=CARTESIAN_POINT('Ctrl Pts',(-59.25,1.2824204934428,-4.05280356580097));
#43317=CARTESIAN_POINT('Ctrl Pts',(-59.25,1.32283749131235,-4.03550260515957));
#43318=CARTESIAN_POINT('Ctrl Pts',(-59.25,1.36300566803296,-4.01755679371646));
#43319=CARTESIAN_POINT('Ctrl Pts',(-59.25,1.40290943437871,-3.99897218974183));
#43320=CARTESIAN_POINT('Ctrl Pts',(-59.25,1.42483837727862,-3.98875910068537));
#43321=CARTESIAN_POINT('Ctrl Pts',(-59.25,1.44668745843242,-3.97835308915049));
#43322=CARTESIAN_POINT('Ctrl Pts',(-59.25,1.46845401683104,-3.96775511286795));
#43323=CARTESIAN_POINT('Ctrl Pts',(-59.25,1.48305813660077,-3.96064447497506));
#43324=CARTESIAN_POINT('Ctrl Pts',(-59.25,1.49762227703197,-3.95344876155404));
#43325=CARTESIAN_POINT('Ctrl Pts',(-59.25,1.51213804695255,-3.94617228279005));
#43326=CARTESIAN_POINT('Ctrl Pts',(-59.25,1.62935001463851,-3.88741615766419));
#43327=CARTESIAN_POINT('Ctrl Pts',(-59.25,1.74355939590811,-3.82332582185838));
#43328=CARTESIAN_POINT('Ctrl Pts',(-59.25,1.85442498273839,-3.75415630054696));
#43329=CARTESIAN_POINT('Ctrl Pts',(-59.25,1.96237767301167,-3.68680414805339));
#43330=CARTESIAN_POINT('Ctrl Pts',(-59.25,2.06716045912934,-3.61463545217675));
#43331=CARTESIAN_POINT('Ctrl Pts',(-59.25,2.16842427848398,-3.53784621807521));
#43332=CARTESIAN_POINT('Ctrl Pts',(-59.25,2.27378671312092,-3.45794896839208));
#43333=CARTESIAN_POINT('Ctrl Pts',(-59.25,2.37534057096294,-3.37304919561452));
#43334=CARTESIAN_POINT('Ctrl Pts',(-59.25,2.47264335148199,-3.2833325165496));
#43335=CARTESIAN_POINT('Ctrl Pts',(-59.25,2.56305105159527,-3.19997335072932));
#43336=CARTESIAN_POINT('Ctrl Pts',(-59.25,2.64978877207528,-3.11245500767447));
#43337=CARTESIAN_POINT('Ctrl Pts',(-59.25,2.73245446931944,-3.02090586202492));
#43338=CARTESIAN_POINT('Ctrl Pts',(-59.25,2.73875909413107,-3.01392372754366));
#43339=CARTESIAN_POINT('Ctrl Pts',(-59.25,2.74504000957142,-3.00691814002619));
#43340=CARTESIAN_POINT('Ctrl Pts',(-59.25,2.75129702511905,-2.99988915288066));
#43341=CARTESIAN_POINT('Ctrl Pts',(-90.0683458050225,-1.79217368492204,
3.6547344271606));
#43342=CARTESIAN_POINT('Ctrl Pts',(-90.0288351052725,-2.39703965939263,
3.35812604043492));
#43343=CARTESIAN_POINT('Ctrl Pts',(-89.9498137057724,-3.4560716865392,2.45910294398196));
#43344=CARTESIAN_POINT('Ctrl Pts',(-89.8312816065225,-4.21012624900965,
0.515537866574306));
#43345=CARTESIAN_POINT('Ctrl Pts',(-89.7127495072723,-3.94736126811263,
-1.55208240117109));
#43346=CARTESIAN_POINT('Ctrl Pts',(-89.5942174080221,-2.73137303949805,
-3.24509720256334));
#43347=CARTESIAN_POINT('Ctrl Pts',(-89.4756853087722,-0.855747416393033,
-4.15432931934335));
#43348=CARTESIAN_POINT('Ctrl Pts',(-89.357153209522,1.22652580399161,-4.06036256423134));
#43349=CARTESIAN_POINT('Ctrl Pts',(-89.2386211102719,3.0126043279509,-2.98581045744857));
#43350=CARTESIAN_POINT('Ctrl Pts',(-89.1200890110218,4.07114973607406,-1.19021168789138));
#43351=CARTESIAN_POINT('Ctrl Pts',(-89.0015569117718,4.14653236502477,0.892824265437017));
#43352=CARTESIAN_POINT('Ctrl Pts',(-88.8830248125217,3.22054554208703,2.76024400176603));
#43353=CARTESIAN_POINT('Ctrl Pts',(-88.7644927132716,1.51681193095975,3.96107892847728));
#43354=CARTESIAN_POINT('Ctrl Pts',(-88.6459606140215,-0.553225051728948,
4.20533047603355));
#43355=CARTESIAN_POINT('Ctrl Pts',(-88.5274285147713,-2.48966060894145,
3.43401418720049));
#43356=CARTESIAN_POINT('Ctrl Pts',(-88.4088964155214,-3.82485446805869,
1.83339885856207));
#43357=CARTESIAN_POINT('Ctrl Pts',(-88.2903643162712,-4.23636330669712,
-0.209973878906397));
#43358=CARTESIAN_POINT('Ctrl Pts',(-88.1718322170211,-3.62480963907511,
-2.20263892537862));
#43359=CARTESIAN_POINT('Ctrl Pts',(-88.0533001177711,-2.13788088541058,
-3.6633766416475));
#43360=CARTESIAN_POINT('Ctrl Pts',(-87.9347680185209,-0.134663600797729,
-4.23942553278804));
#43361=CARTESIAN_POINT('Ctrl Pts',(-87.8162359192709,1.9010743336757,-3.79167238760187));
#43362=CARTESIAN_POINT('Ctrl Pts',(-87.6977038200208,3.47771144175241,-2.42824756783923));
#43363=CARTESIAN_POINT('Ctrl Pts',(-87.5791717207707,4.2144970165252,-0.478411976782104));
#43364=CARTESIAN_POINT('Ctrl Pts',(-87.4606396215207,3.93350068426081,1.58695793523026));
#43365=CARTESIAN_POINT('Ctrl Pts',(-87.3421075222705,2.70258178445977,3.26908470681113));
#43366=CARTESIAN_POINT('Ctrl Pts',(-87.2235754230204,0.819001646208479,
4.16174235447228));
#43367=CARTESIAN_POINT('Ctrl Pts',(-87.1050433237704,-1.2623636734931,4.04935810686113));
#43368=CARTESIAN_POINT('Ctrl Pts',(-86.9865112245203,-3.03887389383025,
2.95907224971836));
#43369=CARTESIAN_POINT('Ctrl Pts',(-86.8679791252702,-4.08150985721014,
1.15418387061051));
#43370=CARTESIAN_POINT('Ctrl Pts',(-86.7494470260202,-4.13847970927864,
-0.929434676334609));
#43371=CARTESIAN_POINT('Ctrl Pts',(-86.63091492677,-3.19602548924936,-2.78859896610174));
#43372=CARTESIAN_POINT('Ctrl Pts',(-86.51238282752,-1.48174561502481,-3.97432925838274));
#43373=CARTESIAN_POINT('Ctrl Pts',(-86.3938507282698,0.590369102043211,
-4.20027706765055));
#43374=CARTESIAN_POINT('Ctrl Pts',(-86.2753186290198,2.51991235967365,-3.41187702317127));
#43375=CARTESIAN_POINT('Ctrl Pts',(-86.1567865297697,3.84090821614495,-1.79952415844573));
#43376=CARTESIAN_POINT('Ctrl Pts',(-86.0382544305196,4.234342165928,0.247405625489327));
#43377=CARTESIAN_POINT('Ctrl Pts',(-85.9197223312695,3.6052016952943,2.23458807343251));
#43378=CARTESIAN_POINT('Ctrl Pts',(-85.8011902320195,2.10542137327692,3.68212764073006));
#43379=CARTESIAN_POINT('Ctrl Pts',(-85.6826581327693,0.0971913426281407,
4.24045008986049));
#43380=CARTESIAN_POINT('Ctrl Pts',(-85.5641260335193,-1.93450995627506,
3.77472308265816));
#43381=CARTESIAN_POINT('Ctrl Pts',(-85.4455939342692,-3.49903587826941,
2.39741757820016));
#43382=CARTESIAN_POINT('Ctrl Pts',(-85.3270618350191,-4.21856051198106,
0.441146606508185));
#43383=CARTESIAN_POINT('Ctrl Pts',(-85.2085297357689,-3.91932192309739,
-1.62165926902288));
#43384=CARTESIAN_POINT('Ctrl Pts',(-85.089997636519,-2.67358487308622,-3.29284178910621));
#43385=CARTESIAN_POINT('Ctrl Pts',(-84.9714655372688,-0.782189207191325,
-4.16881795786684));
#43386=CARTESIAN_POINT('Ctrl Pts',(-84.8529334380188,1.29810160318103,-4.03804350515179));
#43387=CARTESIAN_POINT('Ctrl Pts',(-84.7344013387685,3.06490676631494,-2.93209986792342));
#43388=CARTESIAN_POINT('Ctrl Pts',(-84.6158692395186,4.09155085191131,-1.11806741652885));
#43389=CARTESIAN_POINT('Ctrl Pts',(-84.4973371402684,4.13010397153302,0.965973242904165));
#43390=CARTESIAN_POINT('Ctrl Pts',(-84.3788050410185,3.17125572172011,2.81673574712594));
#43391=CARTESIAN_POINT('Ctrl Pts',(-84.2602729417682,1.44656360418077,3.98726934890774));
#43392=CARTESIAN_POINT('Ctrl Pts',(-84.1417408425183,-0.627467060215684,
4.19489549452951));
#43393=CARTESIAN_POINT('Ctrl Pts',(-84.0232087432681,-2.54996727660215,
3.38947341189422));
#43394=CARTESIAN_POINT('Ctrl Pts',(-83.904676644018,-3.85666196576058,1.76550887948358));
#43395=CARTESIAN_POINT('Ctrl Pts',(-83.786144544768,-4.23199028917877,-0.284818036606317));
#43396=CARTESIAN_POINT('Ctrl Pts',(-83.6676124455178,-3.58531215974383,
-2.26636268917237));
#43397=CARTESIAN_POINT('Ctrl Pts',(-83.5490803462679,-2.07279741151507,
-3.70059103556392));
#43398=CARTESIAN_POINT('Ctrl Pts',(-83.4305482470176,-0.0597114933943472,
-4.24114343771067));
#43399=CARTESIAN_POINT('Ctrl Pts',(-83.3120161477677,1.96779447944969,-3.75747894316481));
#43400=CARTESIAN_POINT('Ctrl Pts',(-83.1934840485175,3.52008701406145,-2.36640033280838));
#43401=CARTESIAN_POINT('Ctrl Pts',(-83.0749519492674,4.22229450661292,-0.403846779244268));
#43402=CARTESIAN_POINT('Ctrl Pts',(-82.9564198500173,3.90483703380788,1.65623393911674));
#43403=CARTESIAN_POINT('Ctrl Pts',(-82.8378877507673,2.64437913491587,3.31634167607942));
#43404=CARTESIAN_POINT('Ctrl Pts',(-82.7193556515171,0.745315673391867,
4.17556794564238));
#43405=CARTESIAN_POINT('Ctrl Pts',(-82.6008235522671,-1.33373814150481,
4.02641350230884));
#43406=CARTESIAN_POINT('Ctrl Pts',(-82.482291453017,-3.09070024685299,2.90489846737928));
#43407=CARTESIAN_POINT('Ctrl Pts',(-82.363759353767,-4.1012722661475,1.0818636330929));
#43408=CARTESIAN_POINT('Ctrl Pts',(-82.2452272545168,-4.1214056420387,-1.00243635980107));
#43409=CARTESIAN_POINT('Ctrl Pts',(-82.1266951552668,-3.14623825560085,
-2.84465252019879));
#43410=CARTESIAN_POINT('Ctrl Pts',(-82.0081630560165,-1.41126860599162,
-3.99989800412737));
#43411=CARTESIAN_POINT('Ctrl Pts',(-81.8896309567667,0.664516008557521,
-4.18918626896089));
#43412=CARTESIAN_POINT('Ctrl Pts',(-81.7710988575164,2.57982302217583,-3.36680505760746));
#43413=CARTESIAN_POINT('Ctrl Pts',(-81.6525667582664,3.87211448147575,-1.73135570118489));
#43414=CARTESIAN_POINT('Ctrl Pts',(-81.5340346590163,4.22930786260355,0.322208201322427));
#43415=CARTESIAN_POINT('Ctrl Pts',(-81.4155025597663,3.56514258472508,2.29796028517889));
#43416=CARTESIAN_POINT('Ctrl Pts',(-81.2969704605161,2.04001154890355,3.71876538679436));
#43417=CARTESIAN_POINT('Ctrl Pts',(-81.178438361266,0.0222269802501248,
4.24150552080608));
#43418=CARTESIAN_POINT('Ctrl Pts',(-81.0599062620159,-2.00092530328236,
3.73994131670062));
#43419=CARTESIAN_POINT('Ctrl Pts',(-80.9413741627659,-3.54086320495273,
2.33519825400134));
#43420=CARTESIAN_POINT('Ctrl Pts',(-80.8228420635157,-4.22569870873143,
0.366515408552093));
#43421=CARTESIAN_POINT('Ctrl Pts',(-80.7043099642657,-3.8900471477876,-1.69067924505763));
#43422=CARTESIAN_POINT('Ctrl Pts',(-80.5857778650156,-2.61496685112479,
-3.33958253217321));
#43423=CARTESIAN_POINT('Ctrl Pts',(-80.4672457657655,-0.708383924910281,
-4.18199179059653));
#43424=CARTESIAN_POINT('Ctrl Pts',(-80.3487136665154,1.36927050498713,-4.01446900670923));
#43425=CARTESIAN_POINT('Ctrl Pts',(-80.2301815672654,3.11625232078442,-2.87747017272681));
#43426=CARTESIAN_POINT('Ctrl Pts',(-80.1116494680153,4.11067334059816,-1.04557534807476));
#43427=CARTESIAN_POINT('Ctrl Pts',(-79.9931173687652,4.11238540021266,1.03882117896535));
#43428=CARTESIAN_POINT('Ctrl Pts',(-79.8745852695151,3.12097504491475,2.87234710485192));
#43429=CARTESIAN_POINT('Ctrl Pts',(-79.756053170265,1.37586337731199,4.01221423757314));
#43430=CARTESIAN_POINT('Ctrl Pts',(-79.6375210710149,-0.701513053379031,
4.18314983703188));
#43431=CARTESIAN_POINT('Ctrl Pts',(-79.5189889717648,-2.60947726422201,
3.343873730567));
#43432=CARTESIAN_POINT('Ctrl Pts',(-79.4004568725148,-3.88726455677248,
1.69706729179175));
#43433=CARTESIAN_POINT('Ctrl Pts',(-79.2819247732647,-4.22629509483729,
-0.359573200448428));
#43434=CARTESIAN_POINT('Ctrl Pts',(-79.1633926740146,-3.54469454740893,
-2.32937839090772));
#43435=CARTESIAN_POINT('Ctrl Pts',(-79.0448605747645,-2.00706634268101,
-3.73664927998142));
#43436=CARTESIAN_POINT('Ctrl Pts',(-78.9263284755144,0.0152592617744791,
-4.24153630056935));
#43437=CARTESIAN_POINT('Ctrl Pts',(-78.8077963762643,2.03389985453592,-3.72211159382277));
#43438=CARTESIAN_POINT('Ctrl Pts',(-78.6892642770142,3.56136279891019,-2.30381373712066));
#43439=CARTESIAN_POINT('Ctrl Pts',(-78.5707321777641,4.22877291137641,-0.329155494427314));
#43440=CARTESIAN_POINT('Ctrl Pts',(-78.4522000785141,3.87495330153115,1.72499266588648));
#43441=CARTESIAN_POINT('Ctrl Pts',(-78.333667979264,2.58535055813011,3.36256220074308));
#43442=CARTESIAN_POINT('Ctrl Pts',(-78.2151358800139,0.671396364788188,
4.18808967855972));
#43443=CARTESIAN_POINT('Ctrl Pts',(-78.0966037807638,-1.40469494822981,
4.00220956636128));
#43444=CARTESIAN_POINT('Ctrl Pts',(-77.9780716815137,-3.14156294622147,
2.84981991591854));
#43445=CARTESIAN_POINT('Ctrl Pts',(-77.8595395822636,-4.11974940532679,
1.00919977696215));
#43446=CARTESIAN_POINT('Ctrl Pts',(-77.7410074830135,-4.10305187789505,
-1.07511354071959));
#43447=CARTESIAN_POINT('Ctrl Pts',(-77.6224753837634,-3.09545209551088,
-2.89984013449786));
#43448=CARTESIAN_POINT('Ctrl Pts',(-77.5039432845133,-1.34038284556851,
-4.02417116971747));
#43449=CARTESIAN_POINT('Ctrl Pts',(-77.3854111852633,0.738520086648723,
-4.17687915873197));
#43450=CARTESIAN_POINT('Ctrl Pts',(-77.2668790860131,2.63879720128349,-3.32049492888954));
#43451=CARTESIAN_POINT('Ctrl Pts',(-77.1483469867632,3.90237383473824,-1.66302156401962));
#43452=CARTESIAN_POINT('Ctrl Pts',(-77.0298148875129,4.22242284177216,0.397665888508434));
#43453=CARTESIAN_POINT('Ctrl Pts',(-76.911282788263,3.52503575024894,2.35909274883029));
#43454=CARTESIAN_POINT('Ctrl Pts',(-76.7927506890127,1.97181984252191,3.75729912712469));
#43455=CARTESIAN_POINT('Ctrl Pts',(-76.6742185897627,-0.0484579238967644,
4.23516823465935));
#43456=CARTESIAN_POINT('Ctrl Pts',(-76.5161757907627,-2.75000559908163,
3.54082966140385));
#43457=CARTESIAN_POINT('Ctrl Pts',(-76.3186222920125,-4.79203870408418,
0.336434116267563));
#43458=CARTESIAN_POINT('Ctrl Pts',(-76.0815580935123,-2.89441002508752,
-3.83698970964484));
#43459=CARTESIAN_POINT('Ctrl Pts',(-75.8444938950122,1.63095801340486,-4.51688897627564));
#43460=CARTESIAN_POINT('Ctrl Pts',(-75.607429696512,4.67567242759371,-1.10249052069397));
#43461=CARTESIAN_POINT('Ctrl Pts',(-75.3703654980118,3.47661902182452,3.31543652103366));
#43462=CARTESIAN_POINT('Ctrl Pts',(-75.1333012995117,-0.878131813745364,
4.72260507390595));
#43463=CARTESIAN_POINT('Ctrl Pts',(-74.8962371010114,-4.43574436453777,
1.84399067006013));
#43464=CARTESIAN_POINT('Ctrl Pts',(-74.6591729025114,-3.96732235451901,
-2.70870511280469));
#43465=CARTESIAN_POINT('Ctrl Pts',(-74.422108704011,0.102291553945791,-4.80267280759255));
#43466=CARTESIAN_POINT('Ctrl Pts',(-74.185044505511,4.07867853910156,-2.53741907084073));
#43467=CARTESIAN_POINT('Ctrl Pts',(-73.9479803070107,4.35373227228281,2.03076696083007));
#43468=CARTESIAN_POINT('Ctrl Pts',(-73.7109161085106,0.675669024164784,
4.75614017541162));
#43469=CARTESIAN_POINT('Ctrl Pts',(-73.4738519100105,-3.6129693088472,3.16366288324438));
#43470=CARTESIAN_POINT('Ctrl Pts',(-73.2367877115102,-4.62749258109677,
-1.29861920405548));
#43471=CARTESIAN_POINT('Ctrl Pts',(-72.9997235130101,-1.43150958571139,
-4.58558645780951));
#43472=CARTESIAN_POINT('Ctrl Pts',(-72.8021700142599,2.29645120176649,-3.85049572963833));
#43473=CARTESIAN_POINT('Ctrl Pts',(-72.6441272152598,3.92679810234926,-1.58721605638371));
#43474=CARTESIAN_POINT('Ctrl Pts',(-72.5255951160097,4.21734429791554,0.468377299721421));
#43475=CARTESIAN_POINT('Ctrl Pts',(-72.4070630167596,3.4806665638518,2.42407836288371));
#43476=CARTESIAN_POINT('Ctrl Pts',(-72.2885309175095,1.90781163232082,3.78777607431905));
#43477=CARTESIAN_POINT('Ctrl Pts',(-72.1699988182595,-0.127952933172336,
4.24002244278688));
#43478=CARTESIAN_POINT('Ctrl Pts',(-72.0514667190093,-2.13173404035006,
3.66669431825119));
#43479=CARTESIAN_POINT('Ctrl Pts',(-71.9329346197594,-3.62124894073959,
2.20868457101181));
#43480=CARTESIAN_POINT('Ctrl Pts',(-71.8144025205091,-4.23598160600254,
0.216886167119235));
#43481=CARTESIAN_POINT('Ctrl Pts',(-71.6958704212593,-3.82787651363011,
-1.82709000261242));
#43482=CARTESIAN_POINT('Ctrl Pts',(-71.5773383220089,-2.49529078987354,
-3.42993115267771));
#43483=CARTESIAN_POINT('Ctrl Pts',(-71.458806222759,-0.560136340693826,
-4.20441037867915));
#43484=CARTESIAN_POINT('Ctrl Pts',(-71.3402741235088,1.5103047169698,-3.96356795830934));
#43485=CARTESIAN_POINT('Ctrl Pts',(-71.2217420242588,3.21600598369556,-2.76552975458416));
#43486=CARTESIAN_POINT('Ctrl Pts',(-71.1032099250086,4.14506039630085,-0.899634673257719));
#43487=CARTESIAN_POINT('Ctrl Pts',(-70.9846778257586,4.07309954546553,1.18352108347017));
#43488=CARTESIAN_POINT('Ctrl Pts',(-70.8661457265085,3.01750462107274,2.98086038723955));
#43489=CARTESIAN_POINT('Ctrl Pts',(-70.7476136272584,1.23319553280523,4.0583361681078));
#43490=CARTESIAN_POINT('Ctrl Pts',(-70.6290815280083,-0.848924438267781,
4.15574181331312));
#43491=CARTESIAN_POINT('Ctrl Pts',(-70.5105494287582,-2.72603312996977,
3.24955484789199));
#43492=CARTESIAN_POINT('Ctrl Pts',(-70.3920173295082,-3.94481712984691,
1.5586150410489));
#43493=CARTESIAN_POINT('Ctrl Pts',(-70.273485230258,-4.21094572157516,-0.508723181559844));
#43494=CARTESIAN_POINT('Ctrl Pts',(-70.154953131008,-3.46015001328113,-2.45320708625443));
#43495=CARTESIAN_POINT('Ctrl Pts',(-70.0364210317579,-1.87374378398806,
-3.80525259964336));
#43496=CARTESIAN_POINT('Ctrl Pts',(-69.9178889325078,0.165163070961228,
-4.23834688141492));
#43497=CARTESIAN_POINT('Ctrl Pts',(-69.7993568332577,2.16418379186852,-3.64789961943599));
#43498=CARTESIAN_POINT('Ctrl Pts',(-69.6808247340076,3.64056394757633,-2.17650115247581));
#43499=CARTESIAN_POINT('Ctrl Pts',(-69.5622926347575,4.2377644279798,-0.179487532051847));
#43500=CARTESIAN_POINT('Ctrl Pts',(-69.4437605355075,3.81156402742994,1.8608715126343));
#43501=CARTESIAN_POINT('Ctrl Pts',(-69.3252284362573,2.46488820851225,3.45183853059299));
#43502=CARTESIAN_POINT('Ctrl Pts',(-69.2066963370073,0.522953071331976,
4.20920220550053));
#43503=CARTESIAN_POINT('Ctrl Pts',(-69.0881642377572,-1.54527285978556,
3.95006264640662));
#43504=CARTESIAN_POINT('Ctrl Pts',(-68.9696321385071,-3.24032240668157,
2.737000880967));
#43505=CARTESIAN_POINT('Ctrl Pts',(-68.851100039257,-4.15284879481873,0.862965821490488));
#43506=CARTESIAN_POINT('Ctrl Pts',(-68.7325679400069,-4.06248104189545,
-1.21947156831061));
#43507=CARTESIAN_POINT('Ctrl Pts',(-68.6140358407569,-2.99104255021837,
-3.00741210752073));
#43508=CARTESIAN_POINT('Ctrl Pts',(-68.4955037415068,-1.19728085404309,
-4.06907626842045));
#43509=CARTESIAN_POINT('Ctrl Pts',(-68.3769716422567,0.885618735911535,
-4.14807697328309));
#43510=CARTESIAN_POINT('Ctrl Pts',(-68.2584395430066,2.75464541949803,-3.22533591033841));
#43511=CARTESIAN_POINT('Ctrl Pts',(-68.1399074437565,3.9584377330416,-1.52369085949611));
#43512=CARTESIAN_POINT('Ctrl Pts',(-68.0213753445065,4.20628529483797,0.54591862040923));
#43513=CARTESIAN_POINT('Ctrl Pts',(-67.9028432452563,3.43833404328219,2.48369123050478));
#43514=CARTESIAN_POINT('Ctrl Pts',(-67.7843111460063,1.84004072116821,3.82166367778779));
#43515=CARTESIAN_POINT('Ctrl Pts',(-67.6657790467562,-0.202614086215485,
4.23672168707678));
#43516=CARTESIAN_POINT('Ctrl Pts',(-67.5472469475061,-2.19633851110734,
3.62863063238826));
#43517=CARTESIAN_POINT('Ctrl Pts',(-67.428714848256,-3.65965715110381,2.14424174431298));
#43518=CARTESIAN_POINT('Ctrl Pts',(-67.3101827490059,-4.23918519422161,
0.142028204142372));
#43519=CARTESIAN_POINT('Ctrl Pts',(-67.1916506497558,-3.79496924756422,
-1.89448450289823));
#43520=CARTESIAN_POINT('Ctrl Pts',(-67.0731185505057,-2.43428544669007,
-3.47348779841137));
#43521=CARTESIAN_POINT('Ctrl Pts',(-66.9545864512557,-0.485732755623718,
-4.21365955100716));
#43522=CARTESIAN_POINT('Ctrl Pts',(-66.8360543520056,1.58012219199054,-3.93625164084547));
#43523=CARTESIAN_POINT('Ctrl Pts',(-66.7175222527555,3.26438479979246,-2.70825681953606));
#43524=CARTESIAN_POINT('Ctrl Pts',(-66.5989901535054,4.16031329007191,-0.826230264593738));
#43525=CARTESIAN_POINT('Ctrl Pts',(-66.4804580542553,4.05154499755959,1.25532715035943));
#43526=CARTESIAN_POINT('Ctrl Pts',(-66.3619259550052,2.96434697137833,3.03372875434832));
#43527=CARTESIAN_POINT('Ctrl Pts',(-66.2433938557551,1.16127260186261,4.07949862922429));
#43528=CARTESIAN_POINT('Ctrl Pts',(-66.124861756505,-0.922243831912986,
4.14008809521949));
#43529=CARTESIAN_POINT('Ctrl Pts',(-66.006329657255,-2.78304256481646,3.20086507121113));
#43530=CARTESIAN_POINT('Ctrl Pts',(-65.8877975580049,-3.97174914593023,
1.48864765592202));
#43531=CARTESIAN_POINT('Ctrl Pts',(-65.7692654587548,-4.20129632948259,
-0.583071413770052));
#43532=CARTESIAN_POINT('Ctrl Pts',(-65.6507333595047,-3.41624951217949,
-2.51398138263055));
#43533=CARTESIAN_POINT('Ctrl Pts',(-65.5322012602546,-1.80619393837446,
-3.83777625437688));
#43534=CARTESIAN_POINT('Ctrl Pts',(-65.4136691610045,0.240049276229987,
-4.23476557399121));
#43535=CARTESIAN_POINT('Ctrl Pts',(-65.2951370617545,2.22832167981034,-3.60907822206265));
#43536=CARTESIAN_POINT('Ctrl Pts',(-65.1766049625043,3.6784645083721,-2.11181485512497));
#43537=CARTESIAN_POINT('Ctrl Pts',(-65.0580728632543,4.24027484861026,-0.104557782698988));
#43538=CARTESIAN_POINT('Ctrl Pts',(-64.9395407640041,3.77807805248247,1.92794951983446));
#43539=CARTESIAN_POINT('Ctrl Pts',(-64.8210086647541,2.4034925491091,3.4948657610925));
#43540=CARTESIAN_POINT('Ctrl Pts',(-64.7024765655039,0.448474500591471,
4.21778777844487));
#43541=CARTESIAN_POINT('Ctrl Pts',(-64.583944466254,-1.61484810493722,3.92213318484474));
#43542=CARTESIAN_POINT('Ctrl Pts',(-64.4654123670038,-3.2881922202403,2.67930122316078));
#43543=CARTESIAN_POINT('Ctrl Pts',(-64.3468802677538,-4.16745283400511,
0.789430172987094));
#43544=CARTESIAN_POINT('Ctrl Pts',(-64.2283481685037,-4.04029249751279,
-1.29108468204897));
#43545=CARTESIAN_POINT('Ctrl Pts',(-64.1098160692536,-2.93741985505644,
-3.05980844446182));
#43546=CARTESIAN_POINT('Ctrl Pts',(-63.9912839700035,-1.12517364567985,
-4.08960235093184));
#43547=CARTESIAN_POINT('Ctrl Pts',(-63.8727518707534,0.95879689383177,-4.13177584557272));
#43548=CARTESIAN_POINT('Ctrl Pts',(-63.7542197715033,2.81122233387158,-3.17614422078426));
#43549=CARTESIAN_POINT('Ctrl Pts',(-63.6356876722533,3.98475033575612,-1.45348817792618));
#43550=CARTESIAN_POINT('Ctrl Pts',(-63.5171555730031,4.1959792117271,0.620178664929396));
#43551=CARTESIAN_POINT('Ctrl Pts',(-63.3986234737531,3.39389814665504,2.54407517416668));
#43552=CARTESIAN_POINT('Ctrl Pts',(-63.2800913745029,1.77220607843935,3.85358907217963));
#43553=CARTESIAN_POINT('Ctrl Pts',(-63.1615592752529,-0.277465716615854,
4.23247869430933));
#43554=CARTESIAN_POINT('Ctrl Pts',(-63.0430271760028,-2.26013080006508,
3.58924391596298));
#43555=CARTESIAN_POINT('Ctrl Pts',(-62.9244950767527,-3.69698455028266,
2.07922301753555));
#43556=CARTESIAN_POINT('Ctrl Pts',(-62.8059629775026,-4.2410333060877,0.0670791945175098));
#43557=CARTESIAN_POINT('Ctrl Pts',(-62.6874308782525,-3.76089176148606,
-1.96126394961557));
#43558=CARTESIAN_POINT('Ctrl Pts',(-62.5688987790024,-2.37251192093704,
-3.51597074883963));
#43559=CARTESIAN_POINT('Ctrl Pts',(-62.4503666797524,-0.411181216372217,
-4.22158656537844));
#43560=CARTESIAN_POINT('Ctrl Pts',(-62.3318345805023,1.64944788626615,-3.90770838115492));
#43561=CARTESIAN_POINT('Ctrl Pts',(-62.2133024812522,3.3117428085009,-2.65013635349193));
#43562=CARTESIAN_POINT('Ctrl Pts',(-62.0947703820021,4.17426686894535,-0.752568421026256));
#43563=CARTESIAN_POINT('Ctrl Pts',(-61.976238282752,4.02872442070117,1.32674137044345));
#43564=CARTESIAN_POINT('Ctrl Pts',(-61.8577061835019,2.91026330437545,3.08564914085777));
#43565=CARTESIAN_POINT('Ctrl Pts',(-61.7391740842519,1.08898680526139,4.09938664434021));
#43566=CARTESIAN_POINT('Ctrl Pts',(-61.6206419850017,-0.995275066945756,
4.12314087364582));
#43567=CARTESIAN_POINT('Ctrl Pts',(-61.5021098857517,-2.83918252492348,
3.15117528982951));
#43568=CARTESIAN_POINT('Ctrl Pts',(-61.3835777865016,-3.99744028842169,
1.41821517194611));
#43569=CARTESIAN_POINT('Ctrl Pts',(-61.2650456872515,-4.19033435407454,
-0.657237475982055));
#43570=CARTESIAN_POINT('Ctrl Pts',(-61.1465135880014,-3.3712816981627,-2.57397025366613));
#43571=CARTESIAN_POINT('Ctrl Pts',(-61.0279814887513,-1.73807978469344,
-3.86910089790803));
#43572=CARTESIAN_POINT('Ctrl Pts',(-60.9094493895012,0.314860461962913,
-4.22986122300694));
#43573=CARTESIAN_POINT('Ctrl Pts',(-60.7909172902512,2.29176343348649,-3.56912927064055));
#43574=CARTESIAN_POINT('Ctrl Pts',(-60.672385191001,3.71521573733988,-2.04646876241471));
#43575=CARTESIAN_POINT('Ctrl Pts',(-60.553853091751,4.24146069462157,-0.0295953967523683));
#43576=CARTESIAN_POINT('Ctrl Pts',(-60.4353209925008,3.74341133987005,1.99442525015962));
#43577=CARTESIAN_POINT('Ctrl Pts',(-60.3167888932508,2.34134674152,3.53680099229865));
#43578=CARTESIAN_POINT('Ctrl Pts',(-60.1982567940007,0.373854285980798,
4.22505585861098));
#43579=CARTESIAN_POINT('Ctrl Pts',(-60.0797246947506,-1.68391575197083,
3.89297786596098));
#43580=CARTESIAN_POINT('Ctrl Pts',(-59.9611925955005,-3.33504093198254,
2.62076547651056));
#43581=CARTESIAN_POINT('Ctrl Pts',(-59.8426604962505,-4.18074236031188,
0.715645897712674));
#43582=CARTESIAN_POINT('Ctrl Pts',(-59.7241283970003,-4.0168668570281,-1.36229041980425));
#43583=CARTESIAN_POINT('Ctrl Pts',(-59.6055962977503,-2.88282865866802,
-3.11125693021052));
#43584=CARTESIAN_POINT('Ctrl Pts',(-59.4870641985001,-1.05281798849905,
-4.10883397176923));
#43585=CARTESIAN_POINT('Ctrl Pts',(-59.3685320992501,1.03189169588001,-4.11422147186713));
#43586=CARTESIAN_POINT('Ctrl Pts',(-59.28951069975,2.25480927425104,-3.45523440144076));
#43587=CARTESIAN_POINT('Ctrl Pts',(-59.25,2.75129702511905,-2.99988915288066));
#43588=CARTESIAN_POINT('Ctrl Pts',(-89.9038972033484,-1.91758108071826,
3.91047455474599));
#43589=CARTESIAN_POINT('Ctrl Pts',(-89.8643865035983,-2.56477256599302,
3.59311098917602));
#43590=CARTESIAN_POINT('Ctrl Pts',(-89.7853651040982,-3.69791038417238,
2.63117873038272));
#43591=CARTESIAN_POINT('Ctrl Pts',(-89.6668330048482,-4.5047299324047,0.551612640925381));
#43592=CARTESIAN_POINT('Ctrl Pts',(-89.5483009055982,-4.22357796578305,
-1.66068940373427));
#43593=CARTESIAN_POINT('Ctrl Pts',(-89.429768806348,-2.9225009322427,-3.47217295571325));
#43594=CARTESIAN_POINT('Ctrl Pts',(-89.3112367070979,-0.915628362002354,
-4.44502861127136));
#43595=CARTESIAN_POINT('Ctrl Pts',(-89.1927046078479,1.31235197600245,-4.34448653025811));
#43596=CARTESIAN_POINT('Ctrl Pts',(-89.0741725085977,3.22341138672613,-3.19474261450462));
#43597=CARTESIAN_POINT('Ctrl Pts',(-88.9556404093477,4.35602853470446,-1.27349677877322));
#43598=CARTESIAN_POINT('Ctrl Pts',(-88.8371083100975,4.43668606489078,0.955299664431044));
#43599=CARTESIAN_POINT('Ctrl Pts',(-88.7185762108476,3.44590329221712,2.95339214077506));
#43600=CARTESIAN_POINT('Ctrl Pts',(-88.6000441115973,1.62295088153958,4.23825551975466));
#43601=CARTESIAN_POINT('Ctrl Pts',(-88.4815120123475,-0.591936987748441,
4.4995985751017));
#43602=CARTESIAN_POINT('Ctrl Pts',(-88.3629799130971,-2.66387466866712,
3.67430941079818));
#43603=CARTESIAN_POINT('Ctrl Pts',(-88.2444478138472,-4.0924987495111,1.96169098685439));
#43604=CARTESIAN_POINT('Ctrl Pts',(-88.125915714597,-4.53280292882157,-0.224666806026332));
#43605=CARTESIAN_POINT('Ctrl Pts',(-88.007383615347,-3.87845577890968,-2.35676863603953));
#43606=CARTESIAN_POINT('Ctrl Pts',(-87.8888515160968,-2.28747915070016,
-3.91972150839504));
#43607=CARTESIAN_POINT('Ctrl Pts',(-87.7703194168468,-0.144086689434017,
-4.5360794342553));
#43608=CARTESIAN_POINT('Ctrl Pts',(-87.6517873175967,2.03410205493234,-4.05699475219311));
#43609=CARTESIAN_POINT('Ctrl Pts',(-87.5332552183467,3.72106438176611,-2.59816424856796));
#43610=CARTESIAN_POINT('Ctrl Pts',(-87.4147231190965,4.50940654448005,-0.511888866120898));
#43611=CARTESIAN_POINT('Ctrl Pts',(-87.2961910198465,4.20874748724988,1.69800535411033));
#43612=CARTESIAN_POINT('Ctrl Pts',(-87.1776589205963,2.89169500845528,3.49783898613552));
#43613=CARTESIAN_POINT('Ctrl Pts',(-87.0591268213463,0.876311305684017,
4.45296037370795));
#43614=CARTESIAN_POINT('Ctrl Pts',(-86.9405947220962,-1.35069760126606,
4.33271203572432));
#43615=CARTESIAN_POINT('Ctrl Pts',(-86.8220626228461,-3.25151916609637,
3.166133400059));
#43616=CARTESIAN_POINT('Ctrl Pts',(-86.703530523596,-4.36711360556095,1.2349479141299));
#43617=CARTESIAN_POINT('Ctrl Pts',(-86.5849984243459,-4.42806992436922,
-0.994471889693123));
#43618=CARTESIAN_POINT('Ctrl Pts',(-86.4664663250958,-3.41966744810485,
-2.98373124440774));
#43619=CARTESIAN_POINT('Ctrl Pts',(-86.3479342258457,-1.5854307993215,-4.25243304180721));
#43620=CARTESIAN_POINT('Ctrl Pts',(-86.2294021265957,0.631680193857936,
-4.49419155434812));
#43621=CARTESIAN_POINT('Ctrl Pts',(-86.1108700273456,2.69624328636905,-3.65062319819482));
#43622=CARTESIAN_POINT('Ctrl Pts',(-85.9923379280955,4.10967585899764,-1.92544590379988));
#43623=CARTESIAN_POINT('Ctrl Pts',(-85.8738058288454,4.53064035867955,0.264717839957676));
#43624=CARTESIAN_POINT('Ctrl Pts',(-85.7552737295953,3.85747576880117,2.39095342648068));
#43625=CARTESIAN_POINT('Ctrl Pts',(-85.6367416303453,2.25274828344074,3.93978460907987));
#43626=CARTESIAN_POINT('Ctrl Pts',(-85.5182095310951,0.103992309116789,
4.53717568473301));
#43627=CARTESIAN_POINT('Ctrl Pts',(-85.3996774318451,-2.06987733601028,
4.03885941923692));
#43628=CARTESIAN_POINT('Ctrl Pts',(-85.2811453325949,-3.74388099623042,
2.56517692967806));
#43629=CARTESIAN_POINT('Ctrl Pts',(-85.162613233345,-4.51375438312612,0.47201585068471));
#43630=CARTESIAN_POINT('Ctrl Pts',(-85.0440811340948,-4.19357656694023,
-1.73513491455207));
#43631=CARTESIAN_POINT('Ctrl Pts',(-84.9255490348447,-2.86066903752568,
-3.52325847082353));
#43632=CARTESIAN_POINT('Ctrl Pts',(-84.8070169355947,-0.836922915379946,
-4.46053109261663));
#43633=CARTESIAN_POINT('Ctrl Pts',(-84.6884848363446,1.38893629342528,-4.32060569449399));
#43634=CARTESIAN_POINT('Ctrl Pts',(-84.5699527370945,3.27937368944608,-3.13727362521293));
#43635=CARTESIAN_POINT('Ctrl Pts',(-84.4514206378443,4.37785721910273,-1.19630421032357));
#43636=CARTESIAN_POINT('Ctrl Pts',(-84.3328885385943,4.41910809417767,1.03356724331863));
#43637=CARTESIAN_POINT('Ctrl Pts',(-84.2143564393443,3.39316441550957,3.01383689734654));
#43638=CARTESIAN_POINT('Ctrl Pts',(-84.095824340094,1.54778692644035,4.26627861547135));
#43639=CARTESIAN_POINT('Ctrl Pts',(-83.9772922408442,-0.671374082526944,
4.48843340552124));
#43640=CARTESIAN_POINT('Ctrl Pts',(-83.8587601415938,-2.72840129681721,
3.6266518936912));
#43641=CARTESIAN_POINT('Ctrl Pts',(-83.7402280423439,-4.12653197761353,
1.88905040489152));
#43642=CARTESIAN_POINT('Ctrl Pts',(-83.6216959430938,-4.52812390929942,
-0.304748185423393));
#43643=CARTESIAN_POINT('Ctrl Pts',(-83.5031638438436,-3.8361944625323,-2.42495147170502));
#43644=CARTESIAN_POINT('Ctrl Pts',(-83.3846317445937,-2.21784145918652,
-3.95953998040192));
#43645=CARTESIAN_POINT('Ctrl Pts',(-83.2660996453435,-0.0638898065504608,
-4.53791754961532));
#43646=CARTESIAN_POINT('Ctrl Pts',(-83.1475675460934,2.10549094447769,-4.02040862067655));
#43647=CARTESIAN_POINT('Ctrl Pts',(-83.0290354468434,3.76640518574513,-2.53198925180974));
#43648=CARTESIAN_POINT('Ctrl Pts',(-82.9105033475932,4.51774966412024,-0.432105967129836));
#43649=CARTESIAN_POINT('Ctrl Pts',(-82.7919712483431,4.17807809718167,1.77212894799975));
#43650=CARTESIAN_POINT('Ctrl Pts',(-82.6734391490932,2.82941962713926,3.54840276294096));
#43651=CARTESIAN_POINT('Ctrl Pts',(-82.5549070498429,0.797469155184746,
4.46775341094568));
#43652=CARTESIAN_POINT('Ctrl Pts',(-82.436374950593,-1.42706649935728,4.3081618819283));
#43653=CARTESIAN_POINT('Ctrl Pts',(-82.3178428513427,-3.30697206939204,
3.1081688060253));
#43654=CARTESIAN_POINT('Ctrl Pts',(-82.1993107520927,-4.38825888952899,
1.15756706628934));
#43655=CARTESIAN_POINT('Ctrl Pts',(-82.0807786528427,-4.40980109887219,
-1.07258186767885));
#43656=CARTESIAN_POINT('Ctrl Pts',(-81.9622465535925,-3.36639635160963,
-3.04370714727242));
#43657=CARTESIAN_POINT('Ctrl Pts',(-81.8437144543425,-1.51002215992195,
-4.2797909611373));
#43658=CARTESIAN_POINT('Ctrl Pts',(-81.7251823550924,0.711015531901254,
-4.48232467675905));
#43659=CARTESIAN_POINT('Ctrl Pts',(-81.6066502558422,2.76034619889032,-3.60239732077954));
#43660=CARTESIAN_POINT('Ctrl Pts',(-81.4881181565923,4.14306578347967,-1.8525073571373));
#43661=CARTESIAN_POINT('Ctrl Pts',(-81.3695860573421,4.52525377986144,0.344754727795806));
#43662=CARTESIAN_POINT('Ctrl Pts',(-81.251053958092,3.81461352102674,2.458760110236));
#43663=CARTESIAN_POINT('Ctrl Pts',(-81.132521858842,2.18276140506687,3.97898608228761));
#43664=CARTESIAN_POINT('Ctrl Pts',(-81.0139897595918,0.0237823137164571,
4.53830496948386));
#43665=CARTESIAN_POINT('Ctrl Pts',(-80.8954576603418,-2.14094009848806,
4.00164379838764));
#43666=CARTESIAN_POINT('Ctrl Pts',(-80.7769255610918,-3.78863519108316,
2.49860380680357));
#43667=CARTESIAN_POINT('Ctrl Pts',(-80.6583934618415,-4.52139207536215,
0.392162332894574));
#43668=CARTESIAN_POINT('Ctrl Pts',(-80.5398613625916,-4.16225328853891,
-1.80898456503483));
#43669=CARTESIAN_POINT('Ctrl Pts',(-80.4213292633414,-2.79794921809744,
-3.57326989848707));
#43670=CARTESIAN_POINT('Ctrl Pts',(-80.3027971640913,-0.75795310673366,
-4.47462676460175));
#43671=CARTESIAN_POINT('Ctrl Pts',(-80.1842650648413,1.46508524081083,-4.29538156996789));
#43672=CARTESIAN_POINT('Ctrl Pts',(-80.0657329655912,3.3343121502984,-3.07882121580877));
#43673=CARTESIAN_POINT('Ctrl Pts',(-79.9472008663411,4.39831780438567,-1.1187395076727));
#43674=CARTESIAN_POINT('Ctrl Pts',(-79.828668767091,4.400149665412,1.11151271542078));
#43675=CARTESIAN_POINT('Ctrl Pts',(-79.7101366678409,3.33936534716099,3.07333966113867));
#43676=CARTESIAN_POINT('Ctrl Pts',(-79.5916045685908,1.4721394495319,4.2929690233084));
#43677=CARTESIAN_POINT('Ctrl Pts',(-79.4730724693408,-0.750601445805186,
4.47586584536369));
#43678=CARTESIAN_POINT('Ctrl Pts',(-79.3545403700905,-2.79207549722183,
3.57786137358953));
#43679=CARTESIAN_POINT('Ctrl Pts',(-79.2360082708406,-4.15927598565198,
1.81581961548961));
#43680=CARTESIAN_POINT('Ctrl Pts',(-79.1174761715905,-4.5220301935998,-0.384734343615344));
#43681=CARTESIAN_POINT('Ctrl Pts',(-78.9989440723404,-3.79273463181798,
-2.4923766986529));
#43682=CARTESIAN_POINT('Ctrl Pts',(-78.8804119730903,-2.14751085726326,
-3.99812140132146));
#43683=CARTESIAN_POINT('Ctrl Pts',(-78.7618798738402,0.0163270289763692,
-4.5383379030618));
#43684=CARTESIAN_POINT('Ctrl Pts',(-78.6433477745902,2.17622204474192,-3.98256644023163));
#43685=CARTESIAN_POINT('Ctrl Pts',(-78.52481567534,3.81056924461044,-2.46502315761527));
#43686=CARTESIAN_POINT('Ctrl Pts',(-78.4062835760899,4.52468139540959,-0.35218815789933));
#43687=CARTESIAN_POINT('Ctrl Pts',(-78.2877514768399,4.1461032500353,1.84569906829402));
#43688=CARTESIAN_POINT('Ctrl Pts',(-78.1692193775898,2.76626052430319,3.59785756990614));
#43689=CARTESIAN_POINT('Ctrl Pts',(-78.0506872783397,0.718377341221213,
4.48115135241873));
#43690=CARTESIAN_POINT('Ctrl Pts',(-77.9321551790897,-1.50298851030343,
4.28226427499296));
#43691=CARTESIAN_POINT('Ctrl Pts',(-77.8136230798394,-3.3613938873463,3.04923613162936));
#43692=CARTESIAN_POINT('Ctrl Pts',(-77.6950909805895,-4.40802896695736,
1.07981855511509));
#43693=CARTESIAN_POINT('Ctrl Pts',(-77.5765588813393,-4.39016302965047,
-1.15034463604321));
#43694=CARTESIAN_POINT('Ctrl Pts',(-77.4580267820892,-3.31205642877169,
-3.10275651618137));
#43695=CARTESIAN_POINT('Ctrl Pts',(-77.3394946828392,-1.43417616674434,
-4.30576264206103));
#43696=CARTESIAN_POINT('Ctrl Pts',(-77.2209625835891,0.790198047099194,
-4.46915637620211));
#43697=CARTESIAN_POINT('Ctrl Pts',(-77.102430484339,2.82344709756949,-3.55284663971428));
#43698=CARTESIAN_POINT('Ctrl Pts',(-76.983898385089,4.17544253569911,-1.77939153711507));
#43699=CARTESIAN_POINT('Ctrl Pts',(-76.8653662858387,4.51788697953528,0.425492568419178));
#43700=CARTESIAN_POINT('Ctrl Pts',(-76.7468341865888,3.77170020986389,2.52417031947069));
#43701=CARTESIAN_POINT('Ctrl Pts',(-76.6283020873386,2.10979798242572,4.02021622200475));
#43702=CARTESIAN_POINT('Ctrl Pts',(-76.5097699880885,-0.0518487682622708,
4.53152423158982));
#43703=CARTESIAN_POINT('Ctrl Pts',(-76.3517271890885,-2.94243730562177,
3.78859930032371));
#43704=CARTESIAN_POINT('Ctrl Pts',(-76.1541736903383,-5.12736172522327,
0.359976101474219));
#43705=CARTESIAN_POINT('Ctrl Pts',(-75.9171094918381,-3.09694643473724,
-4.10548315491292));
#43706=CARTESIAN_POINT('Ctrl Pts',(-75.6800452933379,1.7450843387911,-4.83295838873338));
#43707=CARTESIAN_POINT('Ctrl Pts',(-75.4429810948378,5.00285271579571,-1.17963732083592));
#43708=CARTESIAN_POINT('Ctrl Pts',(-75.2059168963375,3.71989551972808,3.54743426964955));
#43709=CARTESIAN_POINT('Ctrl Pts',(-74.9688526978376,-0.939579108086353,
5.05306947513863));
#43710=CARTESIAN_POINT('Ctrl Pts',(-74.7317884993371,-4.74613568087871,
1.97302396061139));
#43711=CARTESIAN_POINT('Ctrl Pts',(-74.4947243008372,-4.24493582968068,
-2.89824681684524));
#43712=CARTESIAN_POINT('Ctrl Pts',(-74.2576601023368,0.109449407841399,
-5.138739950375));
#43713=CARTESIAN_POINT('Ctrl Pts',(-74.0205959038369,4.36408416590106,-2.71497503006226));
#43714=CARTESIAN_POINT('Ctrl Pts',(-73.7835317053365,4.6583847905374,2.17286992672524));
#43715=CARTESIAN_POINT('Ctrl Pts',(-73.5464675068365,0.722948980038282,
5.08895119616166));
#43716=CARTESIAN_POINT('Ctrl Pts',(-73.3094033083362,-3.86578692129527,
3.38504026798275));
#43717=CARTESIAN_POINT('Ctrl Pts',(-73.0723391098361,-4.95130148340585,
-1.38949011343312));
#43718=CARTESIAN_POINT('Ctrl Pts',(-72.8352749113358,-1.53167950267415,
-4.90646297815493));
#43719=CARTESIAN_POINT('Ctrl Pts',(-72.6377214125857,2.4571454286763,-4.11993425897348));
#43720=CARTESIAN_POINT('Ctrl Pts',(-72.4796786135857,4.20157589201124,-1.69828153729762));
#43721=CARTESIAN_POINT('Ctrl Pts',(-72.3611465143355,4.51245306445273,0.50115201229658));
#43722=CARTESIAN_POINT('Ctrl Pts',(-72.2426144150855,3.72422628860401,2.59370330339747));
#43723=CARTESIAN_POINT('Ctrl Pts',(-72.1240823158353,2.04131079620884,4.05282579429657));
#43724=CARTESIAN_POINT('Ctrl Pts',(-72.0055502165853,-0.136906442683483,
4.53671811304536));
#43725=CARTESIAN_POINT('Ctrl Pts',(-71.8870181173352,-2.28090218001176,
3.92327133949721));
#43726=CARTESIAN_POINT('Ctrl Pts',(-71.7684860180852,-3.87464592062427,
2.36323732586829));
#43727=CARTESIAN_POINT('Ctrl Pts',(-71.6499539188349,-4.53239451861189,
0.232062781769669));
#43728=CARTESIAN_POINT('Ctrl Pts',(-71.531421819585,-4.09573226279255,-1.95494066856108));
#43729=CARTESIAN_POINT('Ctrl Pts',(-71.4128897203348,-2.66989882164255,
-3.66994066583849));
#43730=CARTESIAN_POINT('Ctrl Pts',(-71.2943576210847,-0.599331894321411,
-4.49861409391326));
#43731=CARTESIAN_POINT('Ctrl Pts',(-71.1758255218347,1.61598832509741,-4.24091871950784));
#43732=CARTESIAN_POINT('Ctrl Pts',(-71.0572934225845,3.44104607812029,-2.95904776427113));
#43733=CARTESIAN_POINT('Ctrl Pts',(-70.9387613233345,4.43511109512073,-0.962586630699401));
#43734=CARTESIAN_POINT('Ctrl Pts',(-70.8202292240844,4.35811478205403,1.26633799915005));
#43735=CARTESIAN_POINT('Ctrl Pts',(-70.7016971248343,3.22865457797459,3.18944616301615));
#43736=CARTESIAN_POINT('Ctrl Pts',(-70.5831650255842,1.3194884192469,4.34231833701809));
#43737=CARTESIAN_POINT('Ctrl Pts',(-70.4646329263342,-0.90832794582209,
4.44653994453993));
#43738=CARTESIAN_POINT('Ctrl Pts',(-70.3461008270841,-2.91678736241942,
3.47694252487875));
#43739=CARTESIAN_POINT('Ctrl Pts',(-70.227568727834,-4.22085580138227,1.6676791652414));
#43740=CARTESIAN_POINT('Ctrl Pts',(-70.1090366285839,-4.50560674758229,
-0.544321098166527));
#43741=CARTESIAN_POINT('Ctrl Pts',(-69.9905045293338,-3.70227409192413,
-2.62487030987185));
#43742=CARTESIAN_POINT('Ctrl Pts',(-69.8719724300837,-2.00485904938691,
-4.0715252398919));
#43743=CARTESIAN_POINT('Ctrl Pts',(-69.7534403308337,0.176720360740206,
-4.53492530422694));
#43744=CARTESIAN_POINT('Ctrl Pts',(-69.6349082315836,2.31562260365669,-3.90316148118993));
#43745=CARTESIAN_POINT('Ctrl Pts',(-69.5163761323335,3.89531249551915,-2.32880187186253));
#43746=CARTESIAN_POINT('Ctrl Pts',(-69.3978440330833,4.53430209359898,-0.192047176332951));
#43747=CARTESIAN_POINT('Ctrl Pts',(-69.2793119338334,4.07827830998647,1.99108604054206));
#43748=CARTESIAN_POINT('Ctrl Pts',(-69.1607798345831,2.63736881893472,3.69338101303916));
#43749=CARTESIAN_POINT('Ctrl Pts',(-69.0422477353331,0.559546724810547,
4.50374122892928));
#43750=CARTESIAN_POINT('Ctrl Pts',(-68.9237156360831,-1.65340336452998,
4.22646837308677));
#43751=CARTESIAN_POINT('Ctrl Pts',(-68.8051835368329,-3.46706404337724,
2.92852258205094));
#43752=CARTESIAN_POINT('Ctrl Pts',(-68.6866514375829,-4.44344448700827,
0.923351875166453));
#43753=CARTESIAN_POINT('Ctrl Pts',(-68.5681193383327,-4.34675324844664,
-1.3048041200136));
#43754=CARTESIAN_POINT('Ctrl Pts',(-68.4495872390827,-3.20034082308918,
-3.21785584054912));
#43755=CARTESIAN_POINT('Ctrl Pts',(-68.3310551398326,-1.28106060999283,
-4.35380997610297));
#43756=CARTESIAN_POINT('Ctrl Pts',(-68.2125230405825,0.947589927807374,
-4.43833875714834));
#43757=CARTESIAN_POINT('Ctrl Pts',(-68.0939909413324,2.94740179758105,-3.45102886659968));
#43758=CARTESIAN_POINT('Ctrl Pts',(-67.9754588420823,4.23542950660619,-1.63031116326222));
#43759=CARTESIAN_POINT('Ctrl Pts',(-67.8569267428322,4.50062020737443,0.584119288725105));
#43760=CARTESIAN_POINT('Ctrl Pts',(-67.7383946435822,3.6789315489109,2.65748758283382));
#43761=CARTESIAN_POINT('Ctrl Pts',(-67.6198625443321,1.96879761395276,4.08908468361586));
#43762=CARTESIAN_POINT('Ctrl Pts',(-67.5013304450819,-0.216792011668601,
4.53318638687673));
#43763=CARTESIAN_POINT('Ctrl Pts',(-67.382798345832,-2.35002735013129,3.88254414631988));
#43764=CARTESIAN_POINT('Ctrl Pts',(-67.2642662465817,-3.91574174641298,
2.29428511085401));
#43765=CARTESIAN_POINT('Ctrl Pts',(-67.1457341473317,-4.53582227799202,
0.151966631071091));
#43766=CARTESIAN_POINT('Ctrl Pts',(-67.0272020480817,-4.06052231000895,
-2.02705110059108));
#43767=CARTESIAN_POINT('Ctrl Pts',(-66.9086699488315,-2.60462462813354,
-3.71654518888283));
#43768=CARTESIAN_POINT('Ctrl Pts',(-66.7901378495815,-0.51972191663431,
-4.50851047729267));
#43769=CARTESIAN_POINT('Ctrl Pts',(-66.6716057503314,1.69069127957646,-4.21169094208632));
#43770=CARTESIAN_POINT('Ctrl Pts',(-66.5530736510813,3.49281020301257,-2.89776715424464));
#43771=CARTESIAN_POINT('Ctrl Pts',(-66.4345415518312,4.45143131049253,-0.884045746810973));
#43772=CARTESIAN_POINT('Ctrl Pts',(-66.3160094525812,4.3350519541509,1.34316869726045));
#43773=CARTESIAN_POINT('Ctrl Pts',(-66.197477353331,3.17177722049131,3.24601399535804));
#43774=CARTESIAN_POINT('Ctrl Pts',(-66.078945254081,1.24253267951826,4.36496164184945));
#43775=CARTESIAN_POINT('Ctrl Pts',(-65.9604131548308,-0.986777865763803,
4.42979085715414));
#43776=CARTESIAN_POINT('Ctrl Pts',(-65.8418810555808,-2.9777860338117,3.42484567992835));
#43777=CARTESIAN_POINT('Ctrl Pts',(-65.7233489563307,-4.2496723859251,1.59281581069298));
#43778=CARTESIAN_POINT('Ctrl Pts',(-65.6048168570806,-4.49528213905086,
-0.623871849676049));
#43779=CARTESIAN_POINT('Ctrl Pts',(-65.4862847578305,-3.65530165222434,
-2.68989728906772));
#43780=CARTESIAN_POINT('Ctrl Pts',(-65.3677526585804,-1.93258240173615,
-4.10632473813112));
#43781=CARTESIAN_POINT('Ctrl Pts',(-65.2492205593303,0.25684672998572,-4.53109339473195));
#43782=CARTESIAN_POINT('Ctrl Pts',(-65.1306884600803,2.38424854181727,-3.8616235556214));
#43783=CARTESIAN_POINT('Ctrl Pts',(-65.0121563608302,3.93586514894891,-2.25958914933163));
#43784=CARTESIAN_POINT('Ctrl Pts',(-64.8936242615801,4.53698818097217,-0.111874216005024));
#43785=CARTESIAN_POINT('Ctrl Pts',(-64.7750921623301,4.04244915315367,2.06285783287529));
#43786=CARTESIAN_POINT('Ctrl Pts',(-64.6565600630799,2.57167699681937,3.73941907500589));
#43787=CARTESIAN_POINT('Ctrl Pts',(-64.5380279638298,0.479856514328996,
4.51292757754252));
#43788=CARTESIAN_POINT('Ctrl Pts',(-64.4194958645798,-1.72784713909916,
4.19658454679454));
#43789=CARTESIAN_POINT('Ctrl Pts',(-64.3009637653296,-3.51828354826676,
2.86678538933129));
#43790=CARTESIAN_POINT('Ctrl Pts',(-64.1824316660796,-4.45907044418055,
0.844670567927753));
#43791=CARTESIAN_POINT('Ctrl Pts',(-64.0638995668294,-4.3230120601484,-1.38142836307181));
#43792=CARTESIAN_POINT('Ctrl Pts',(-63.9453674675794,-3.14296587857083,
-3.27391861240125));
#43793=CARTESIAN_POINT('Ctrl Pts',(-63.8268353683293,-1.20390769802672,
-4.37577237172135));
#43794=CARTESIAN_POINT('Ctrl Pts',(-63.7083032690792,1.02588872905094,-4.42089695764265));
#43795=CARTESIAN_POINT('Ctrl Pts',(-63.5897711698291,3.00793768286991,-3.39839498741083));
#43796=CARTESIAN_POINT('Ctrl Pts',(-63.4712390705791,4.26358333431514,-1.55519604739662));
#43797=CARTESIAN_POINT('Ctrl Pts',(-63.3527069713289,4.48959295585525,0.663575681608901));
#43798=CARTESIAN_POINT('Ctrl Pts',(-63.2341748720788,3.63138624937108,2.7220968943751));
#43799=CARTESIAN_POINT('Ctrl Pts',(-63.1156427728288,1.8962162405019,4.1232440582319));
#43800=CARTESIAN_POINT('Ctrl Pts',(-62.9971106735786,-0.296881386668499,
4.52864649059049));
#43801=CARTESIAN_POINT('Ctrl Pts',(-62.8785785743287,-2.41828350601072,
3.84040134348544));
#43802=CARTESIAN_POINT('Ctrl Pts',(-62.7600464750784,-3.95568113122819,
2.22471669713957));
#43803=CARTESIAN_POINT('Ctrl Pts',(-62.6415143758285,-4.53779971152945,
0.0717730627331741));
#43804=CARTESIAN_POINT('Ctrl Pts',(-62.5229822765783,-4.02406025104017,
-2.09850344066467));
#43805=CARTESIAN_POINT('Ctrl Pts',(-62.4044501773283,-2.53852849846159,
-3.7620008847675));
#43806=CARTESIAN_POINT('Ctrl Pts',(-62.2859180780781,-0.439953631668492,
-4.5169921846812));
#43807=CARTESIAN_POINT('Ctrl Pts',(-62.1673859788281,1.76486804094118,-4.18115036712692));
#43808=CARTESIAN_POINT('Ctrl Pts',(-62.048853879578,3.54348208949535,-2.83557970722072));
#43809=CARTESIAN_POINT('Ctrl Pts',(-61.9303217803279,4.46636129137614,-0.805229414005605));
#43810=CARTESIAN_POINT('Ctrl Pts',(-61.8117896810778,4.31063450688954,1.41958012907617));
#43811=CARTESIAN_POINT('Ctrl Pts',(-61.6932575818278,3.11390904761658,3.30156751213588));
#43812=CARTESIAN_POINT('Ctrl Pts',(-61.5747254825776,1.16518868259802,4.38624132129133));
#43813=CARTESIAN_POINT('Ctrl Pts',(-61.4561933833276,-1.06491946318739,
4.41165775335188));
#43814=CARTESIAN_POINT('Ctrl Pts',(-61.3376612840774,-3.03785438894894,
3.37167885492467));
#43815=CARTESIAN_POINT('Ctrl Pts',(-61.2191291848274,-4.27716126671725,
1.51745481199265));
#43816=CARTESIAN_POINT('Ctrl Pts',(-61.1005970855773,-4.48355309915555,
-0.703227683837457));
#43817=CARTESIAN_POINT('Ctrl Pts',(-60.9820649863272,-3.60718721436302,
-2.75408388276636));
#43818=CARTESIAN_POINT('Ctrl Pts',(-60.8635328870771,-1.85970195854767,
-4.13984132433085));
#43819=CARTESIAN_POINT('Ctrl Pts',(-60.745000787827,0.336892830201615,-4.52584586167209));
#43820=CARTESIAN_POINT('Ctrl Pts',(-60.6264686885769,2.45212963370055,-3.81887917538301));
#43821=CARTESIAN_POINT('Ctrl Pts',(-60.5079365893269,3.97518804602896,-2.1896704622455));
#43822=CARTESIAN_POINT('Ctrl Pts',(-60.3894044900767,4.53825700658604,-0.0316663353369214));
#43823=CARTESIAN_POINT('Ctrl Pts',(-60.2708723908267,4.00535663651003,2.13398520399503));
#43824=CARTESIAN_POINT('Ctrl Pts',(-60.1523402915766,2.50518253488111,3.78428872500298));
#43825=CARTESIAN_POINT('Ctrl Pts',(-60.0338081923265,0.40001474844413,4.52070424178939));
#43826=CARTESIAN_POINT('Ctrl Pts',(-59.9152760930764,-1.80174779636003,
4.16538908378548));
#43827=CARTESIAN_POINT('Ctrl Pts',(-59.7967439938263,-3.56841049971614,
2.80415360243109));
#43828=CARTESIAN_POINT('Ctrl Pts',(-59.6782118945762,-4.47328990540352,
0.765723236253875));
#43829=CARTESIAN_POINT('Ctrl Pts',(-59.5596797953262,-4.29794720991927,
-1.45761672400295));
#43830=CARTESIAN_POINT('Ctrl Pts',(-59.4411476960761,-3.08455466192987,
-3.32896720715149));
#43831=CARTESIAN_POINT('Ctrl Pts',(-59.322615596826,-1.12648895203119,-4.39634972567962));
#43832=CARTESIAN_POINT('Ctrl Pts',(-59.2040834975759,1.1040983415934,-4.40211421622372));
#43833=CARTESIAN_POINT('Ctrl Pts',(-59.1250620980759,2.41258960630257,-3.6970145100295));
#43834=CARTESIAN_POINT('Ctrl Pts',(-59.0855513983258,2.94381909922657,-3.20980646698104));
#43835=CARTESIAN_POINT('Ctrl Pts',(-89.7394486016742,-2.04298847651448,
4.16621468233137));
#43836=CARTESIAN_POINT('Ctrl Pts',(-89.6999379019242,-2.73250547259342,
3.82809593791711));
#43837=CARTESIAN_POINT('Ctrl Pts',(-89.6209165024241,-3.93974908180555,
2.80325451678348));
#43838=CARTESIAN_POINT('Ctrl Pts',(-89.502384403174,-4.79933361579976,0.587687415276454));
#43839=CARTESIAN_POINT('Ctrl Pts',(-89.3838523039239,-4.49979466345347,
-1.76929640629746));
#43840=CARTESIAN_POINT('Ctrl Pts',(-89.2653202046738,-3.11362882498736,
-3.69924870886316));
#43841=CARTESIAN_POINT('Ctrl Pts',(-89.1467881054238,-0.975509307611675,
-4.73572790319936));
#43842=CARTESIAN_POINT('Ctrl Pts',(-89.0282560061737,1.3981781480133,-4.62861049628486));
#43843=CARTESIAN_POINT('Ctrl Pts',(-88.9097239069235,3.43421844550137,-3.40367477156069));
#43844=CARTESIAN_POINT('Ctrl Pts',(-88.7911918076735,4.64090733333486,-1.35678186965505));
#43845=CARTESIAN_POINT('Ctrl Pts',(-88.6726597084234,4.72683976475678,1.01777506342507));
#43846=CARTESIAN_POINT('Ctrl Pts',(-88.5541276091732,3.67126104234722,3.14654027978409));
#43847=CARTESIAN_POINT('Ctrl Pts',(-88.4355955099233,1.72908983211939,4.51543211103203));
#43848=CARTESIAN_POINT('Ctrl Pts',(-88.3170634106731,-0.630648923767926,
4.79386667416986));
#43849=CARTESIAN_POINT('Ctrl Pts',(-88.198531311423,-2.83808872839281,3.91460463439585));
#43850=CARTESIAN_POINT('Ctrl Pts',(-88.0799992121731,-4.36014303096349,
2.08998311514671));
#43851=CARTESIAN_POINT('Ctrl Pts',(-87.9614671129227,-4.82924255094602,
-0.239359733146274));
#43852=CARTESIAN_POINT('Ctrl Pts',(-87.8429350136729,-4.13210191874425,
-2.51089834670044));
#43853=CARTESIAN_POINT('Ctrl Pts',(-87.7244029144226,-2.43707741598974,
-4.17606637514258));
#43854=CARTESIAN_POINT('Ctrl Pts',(-87.6058708151727,-0.153509778070305,
-4.83273333572255));
#43855=CARTESIAN_POINT('Ctrl Pts',(-87.4873387159224,2.16712977618899,-4.32231711678435));
#43856=CARTESIAN_POINT('Ctrl Pts',(-87.3688066166725,3.9644173217798,-2.7680809292967));
#43857=CARTESIAN_POINT('Ctrl Pts',(-87.2502745174223,4.80431607243491,-0.545365755459693));
#43858=CARTESIAN_POINT('Ctrl Pts',(-87.1317424181723,4.48399429023895,1.80905277299039));
#43859=CARTESIAN_POINT('Ctrl Pts',(-87.0132103189222,3.08080823245079,3.72659326545992));
#43860=CARTESIAN_POINT('Ctrl Pts',(-86.8946782196721,0.933620965159556,
4.74417839294364));
#43861=CARTESIAN_POINT('Ctrl Pts',(-86.7761461204221,-1.43903152903902,
4.61606596458752));
#43862=CARTESIAN_POINT('Ctrl Pts',(-86.6576140211718,-3.46416443836248,
3.37319455039963));
#43863=CARTESIAN_POINT('Ctrl Pts',(-86.5390819219218,-4.65271735391176,
1.31571195764929));
#43864=CARTESIAN_POINT('Ctrl Pts',(-86.4205498226717,-4.71766013945981,
-1.05950910305164));
#43865=CARTESIAN_POINT('Ctrl Pts',(-86.3020177234217,-3.64330940696034,
-3.17886352271374));
#43866=CARTESIAN_POINT('Ctrl Pts',(-86.1834856241716,-1.68911598361819,
-4.53053682523168));
#43867=CARTESIAN_POINT('Ctrl Pts',(-86.0649535249214,0.672991285672667,
-4.7881060410457));
#43868=CARTESIAN_POINT('Ctrl Pts',(-85.9464214256714,2.87257421306444,-3.88936937321837));
#43869=CARTESIAN_POINT('Ctrl Pts',(-85.8278893264213,4.37844350185034,-2.05136764915404));
#43870=CARTESIAN_POINT('Ctrl Pts',(-85.7093572271713,4.82693855143109,0.282030054426027));
#43871=CARTESIAN_POINT('Ctrl Pts',(-85.5908251279211,4.10974984230804,2.54731877952885));
#43872=CARTESIAN_POINT('Ctrl Pts',(-85.4722930286711,2.40007519360456,4.19744157742968));
#43873=CARTESIAN_POINT('Ctrl Pts',(-85.353760929421,0.110793275605439,4.83390127960553));
#43874=CARTESIAN_POINT('Ctrl Pts',(-85.2352288301709,-2.20524471574551,
4.30299575581568));
#43875=CARTESIAN_POINT('Ctrl Pts',(-85.1166967309208,-3.98872611419144,
2.73293628115596));
#43876=CARTESIAN_POINT('Ctrl Pts',(-84.9981646316707,-4.80894825427117,
0.502885094861233));
#43877=CARTESIAN_POINT('Ctrl Pts',(-84.8796325324206,-4.46783121078307,
-1.84861056008126));
#43878=CARTESIAN_POINT('Ctrl Pts',(-84.7611004331705,-3.04775320196515,
-3.75367515254084));
#43879=CARTESIAN_POINT('Ctrl Pts',(-84.6425683339205,-0.891656623568571,
-4.75224422736644));
#43880=CARTESIAN_POINT('Ctrl Pts',(-84.5240362346703,1.47977098366955,-4.60316788383619));
#43881=CARTESIAN_POINT('Ctrl Pts',(-84.4055041354203,3.49384061257721,-3.34244738250244));
#43882=CARTESIAN_POINT('Ctrl Pts',(-84.2869720361702,4.66416358629416,-1.2745410041183));
#43883=CARTESIAN_POINT('Ctrl Pts',(-84.1684399369201,4.70811221682231,1.1011612437331));
#43884=CARTESIAN_POINT('Ctrl Pts',(-84.0499078376701,3.61507310929904,3.21093804756714));
#43885=CARTESIAN_POINT('Ctrl Pts',(-83.9313757384199,1.64901024869993,4.54528788203497));
#43886=CARTESIAN_POINT('Ctrl Pts',(-83.8128436391698,-0.715281104838201,
4.78197131651296));
#43887=CARTESIAN_POINT('Ctrl Pts',(-83.6943115399198,-2.90683531703227,
3.86383037548819));
#43888=CARTESIAN_POINT('Ctrl Pts',(-83.5757794406696,-4.39640198946648,
2.01259193029946));
#43889=CARTESIAN_POINT('Ctrl Pts',(-83.4572473414197,-4.82425752942006,
-0.324678334240465));
#43890=CARTESIAN_POINT('Ctrl Pts',(-83.3387152421694,-4.08707676532076,
-2.58354025423768));
#43891=CARTESIAN_POINT('Ctrl Pts',(-83.2201831429194,-2.36288550685798,
-4.21848892523991));
#43892=CARTESIAN_POINT('Ctrl Pts',(-83.1016510436693,-0.0680681197065716,
-4.83469166151999));
#43893=CARTESIAN_POINT('Ctrl Pts',(-82.9831189444192,2.24318740950569,-4.28333829818827));
#43894=CARTESIAN_POINT('Ctrl Pts',(-82.8645868451692,4.01272335742881,-2.6975781708111));
#43895=CARTESIAN_POINT('Ctrl Pts',(-82.7460547459191,4.81320482162757,-0.460365155015403));
#43896=CARTESIAN_POINT('Ctrl Pts',(-82.6275226466689,4.45131916055545,1.88802395688276));
#43897=CARTESIAN_POINT('Ctrl Pts',(-82.508990547419,3.01446011936265,3.78046384980249));
#43898=CARTESIAN_POINT('Ctrl Pts',(-82.3904584481687,0.849622636977626,
4.75993887624899));
#43899=CARTESIAN_POINT('Ctrl Pts',(-82.2719263489188,-1.52039485720976,
4.58991026154776));
#43900=CARTESIAN_POINT('Ctrl Pts',(-82.1533942496686,-3.52324389193109,
3.31143914467132));
#43901=CARTESIAN_POINT('Ctrl Pts',(-82.0348621504185,-4.67524551291046,
1.23327049948577));
#43902=CARTESIAN_POINT('Ctrl Pts',(-81.9163300511685,-4.69819655570569,
-1.14272737555664));
#43903=CARTESIAN_POINT('Ctrl Pts',(-81.7977979519183,-3.58655444761841,
-3.24276177434604));
#43904=CARTESIAN_POINT('Ctrl Pts',(-81.6792658526683,-1.60877571385228,
-4.55968391814722));
#43905=CARTESIAN_POINT('Ctrl Pts',(-81.5607337534183,0.757515055244992,
-4.7754630845572));
#43906=CARTESIAN_POINT('Ctrl Pts',(-81.442201654168,2.9408693756048,-3.83798958395162));
#43907=CARTESIAN_POINT('Ctrl Pts',(-81.3236695549181,4.4140170854836,-1.97365901308971));
#43908=CARTESIAN_POINT('Ctrl Pts',(-81.2051374556679,4.82119969711933,0.367301254269179));
#43909=CARTESIAN_POINT('Ctrl Pts',(-81.0866053564178,4.06408445732841,2.61955993529313));
#43910=CARTESIAN_POINT('Ctrl Pts',(-80.9680732571678,2.32551126123019,4.23920677778083));
#43911=CARTESIAN_POINT('Ctrl Pts',(-80.8495411579176,0.0253376471827901,
4.83510441816165));
#43912=CARTESIAN_POINT('Ctrl Pts',(-80.7310090586676,-2.28095489369376,
4.26334628007464));
#43913=CARTESIAN_POINT('Ctrl Pts',(-80.6124769594175,-4.03640717721361,
2.66200935960581));
#43914=CARTESIAN_POINT('Ctrl Pts',(-80.4939448601674,-4.81708544199286,
0.417809257237047));
#43915=CARTESIAN_POINT('Ctrl Pts',(-80.3754127609174,-4.43445942929022,
-1.92728988501201));
#43916=CARTESIAN_POINT('Ctrl Pts',(-80.2568806616671,-2.98093158507008,
-3.80695726480094));
#43917=CARTESIAN_POINT('Ctrl Pts',(-80.1383485624172,-0.807522288557044,
-4.76726173860696));
#43918=CARTESIAN_POINT('Ctrl Pts',(-80.019816463167,1.56089997663453,-4.57629413322656));
#43919=CARTESIAN_POINT('Ctrl Pts',(-79.901284363917,3.55237197981238,-3.28017225889073));
#43920=CARTESIAN_POINT('Ctrl Pts',(-79.7827522646669,4.68596226817316,-1.19190366727064));
#43921=CARTESIAN_POINT('Ctrl Pts',(-79.6642201654169,4.68791393061135,1.18420425187621));
#43922=CARTESIAN_POINT('Ctrl Pts',(-79.5456880661667,3.55775564940722,3.27433221742542));
#43923=CARTESIAN_POINT('Ctrl Pts',(-79.4271559669167,1.56841552175181,4.57372380904366));
#43924=CARTESIAN_POINT('Ctrl Pts',(-79.3086238676665,-0.799689838231343,
4.76858185369549));
#43925=CARTESIAN_POINT('Ctrl Pts',(-79.1900917684164,-2.97467373022166,
3.81184901661207));
#43926=CARTESIAN_POINT('Ctrl Pts',(-79.0715596691664,-4.43128741453147,
1.93457193918746));
#43927=CARTESIAN_POINT('Ctrl Pts',(-78.9530275699163,-4.81776529236232,
-0.409895486782259));
#43928=CARTESIAN_POINT('Ctrl Pts',(-78.8344954706662,-4.04077471622703,
-2.65537500639809));
#43929=CARTESIAN_POINT('Ctrl Pts',(-78.7159633714162,-2.28795537184552,
-4.25959352266151));
#43930=CARTESIAN_POINT('Ctrl Pts',(-78.5974312721659,0.01739479617826,-4.83513950555424));
#43931=CARTESIAN_POINT('Ctrl Pts',(-78.478899172916,2.31854423494792,-4.24302128664049));
#43932=CARTESIAN_POINT('Ctrl Pts',(-78.3603670736658,4.05977569031068,-2.62623257810987));
#43933=CARTESIAN_POINT('Ctrl Pts',(-78.2418349744158,4.82058987944276,-0.375220821371348));
#43934=CARTESIAN_POINT('Ctrl Pts',(-78.1233028751657,4.41725319853946,1.96640547070156));
#43935=CARTESIAN_POINT('Ctrl Pts',(-78.0047707759156,2.94717049047626,3.8331529390692));
#43936=CARTESIAN_POINT('Ctrl Pts',(-77.8862386766655,0.76535831765424,4.77421302627773));
#43937=CARTESIAN_POINT('Ctrl Pts',(-77.7677065774155,-1.60128207237705,
4.56231898362465));
#43938=CARTESIAN_POINT('Ctrl Pts',(-77.6491744781652,-3.58122482847114,
3.24865234734018));
#43939=CARTESIAN_POINT('Ctrl Pts',(-77.5306423789153,-4.69630852858792,
1.15043733326802));
#43940=CARTESIAN_POINT('Ctrl Pts',(-77.4121102796651,-4.67727418140591,
-1.22557573136684));
#43941=CARTESIAN_POINT('Ctrl Pts',(-77.2935781804151,-3.52866076203249,
-3.30567289786488));
#43942=CARTESIAN_POINT('Ctrl Pts',(-77.175046081165,-1.52796948792018,-4.58735411440459));
#43943=CARTESIAN_POINT('Ctrl Pts',(-77.0565139819149,0.841876007549669,
-4.76143359367224));
#43944=CARTESIAN_POINT('Ctrl Pts',(-76.9379818826649,3.00809699385548,-3.78519835053903));
#43945=CARTESIAN_POINT('Ctrl Pts',(-76.8194497834148,4.44851123665998,-1.89576151021052));
#43946=CARTESIAN_POINT('Ctrl Pts',(-76.7009176841646,4.8133511172984,0.453319248329923));
#43947=CARTESIAN_POINT('Ctrl Pts',(-76.5823855849146,4.01836466947884,2.68924789011108));
#43948=CARTESIAN_POINT('Ctrl Pts',(-76.4638534856645,2.24777612232952,4.28313331688481));
#43949=CARTESIAN_POINT('Ctrl Pts',(-76.3453213864143,-0.0552396126277808,
4.82788022852029));
#43950=CARTESIAN_POINT('Ctrl Pts',(-76.1872785874144,-3.1348690121619,4.03636893924357));
#43951=CARTESIAN_POINT('Ctrl Pts',(-75.9897250886641,-5.46268474636236,
0.383518086680876));
#43952=CARTESIAN_POINT('Ctrl Pts',(-75.752660890164,-3.29948284438696,-4.37397660018102));
#43953=CARTESIAN_POINT('Ctrl Pts',(-75.5155966916638,1.85921066417732,-5.14902780119111));
#43954=CARTESIAN_POINT('Ctrl Pts',(-75.2785324931636,5.33003300399772,-1.25678412097787));
#43955=CARTESIAN_POINT('Ctrl Pts',(-75.0414682946635,3.96317201763163,3.77943201826544));
#43956=CARTESIAN_POINT('Ctrl Pts',(-74.8044040961632,-1.00102640242734,
5.38353387637129));
#43957=CARTESIAN_POINT('Ctrl Pts',(-74.5673398976631,-5.05652699721965,
2.10205725116266));
#43958=CARTESIAN_POINT('Ctrl Pts',(-74.330275699163,-4.52254930484235,-3.0877885208858));
#43959=CARTESIAN_POINT('Ctrl Pts',(-74.0932115006627,0.116607261737008,
-5.47480709315744));
#43960=CARTESIAN_POINT('Ctrl Pts',(-73.8561473021626,4.64948979270055,-2.8925309892838));
#43961=CARTESIAN_POINT('Ctrl Pts',(-73.6190831036624,4.96303730879198,2.31497289262041));
#43962=CARTESIAN_POINT('Ctrl Pts',(-73.3820189051621,0.770228935911782,
5.42176221691171));
#43963=CARTESIAN_POINT('Ctrl Pts',(-73.1449547066622,-4.11860453374334,
3.60641765272112));
#43964=CARTESIAN_POINT('Ctrl Pts',(-72.9078905081617,-5.27511038571493,
-1.48036102281075));
#43965=CARTESIAN_POINT('Ctrl Pts',(-72.6708263096619,-1.63184941963692,
-5.22733949850035));
#43966=CARTESIAN_POINT('Ctrl Pts',(-72.4732728109114,2.6178396555861,-4.38937278830862));
#43967=CARTESIAN_POINT('Ctrl Pts',(-72.3152300119115,4.47635368167322,-1.80934701821154));
#43968=CARTESIAN_POINT('Ctrl Pts',(-72.1966979126613,4.80756183098992,0.533926724871739));
#43969=CARTESIAN_POINT('Ctrl Pts',(-72.0781658134113,3.96778601335621,2.76332824391123));
#43970=CARTESIAN_POINT('Ctrl Pts',(-71.9596337141612,2.17480996009685,4.31787551427408));
#43971=CARTESIAN_POINT('Ctrl Pts',(-71.8411016149111,-0.145859952194633,
4.83341378330383));
#43972=CARTESIAN_POINT('Ctrl Pts',(-71.7225695156611,-2.43007031967345,
4.17984836074324));
#43973=CARTESIAN_POINT('Ctrl Pts',(-71.6040374164109,-4.12804290050896,
2.51779008072477));
#43974=CARTESIAN_POINT('Ctrl Pts',(-71.4855053171608,-4.82880743122124,
0.247239396420105));
#43975=CARTESIAN_POINT('Ctrl Pts',(-71.3669732179108,-4.36358801195499,
-2.08279133450973));
#43976=CARTESIAN_POINT('Ctrl Pts',(-71.2484411186607,-2.84450685341156,
-3.90995017899927));
#43977=CARTESIAN_POINT('Ctrl Pts',(-71.1299090194105,-0.638527447948997,
-4.79281780914737));
#43978=CARTESIAN_POINT('Ctrl Pts',(-71.0113769201606,1.72167193322502,-4.51826948070633));
#43979=CARTESIAN_POINT('Ctrl Pts',(-70.8928448209103,3.66608617254502,-3.1525657739581));
#43980=CARTESIAN_POINT('Ctrl Pts',(-70.7743127216604,4.72516179394061,-1.02553858814108));
#43981=CARTESIAN_POINT('Ctrl Pts',(-70.6557806224102,4.64313001864252,1.34915491482993));
#43982=CARTESIAN_POINT('Ctrl Pts',(-70.5372485231601,3.43980453487644,3.39803193879275));
#43983=CARTESIAN_POINT('Ctrl Pts',(-70.41871642391,1.40578130568857,4.62630050592838));
#43984=CARTESIAN_POINT('Ctrl Pts',(-70.30018432466,-0.967731453376396,4.73733807576673));
#43985=CARTESIAN_POINT('Ctrl Pts',(-70.1816522254099,-3.10754159486907,
3.70433020186553));
#43986=CARTESIAN_POINT('Ctrl Pts',(-70.0631201261598,-4.49689447291763,
1.77674328943389));
#43987=CARTESIAN_POINT('Ctrl Pts',(-69.9445880269097,-4.80026777358941,
-0.579919014773209));
#43988=CARTESIAN_POINT('Ctrl Pts',(-69.8260559276597,-3.94439817056713,
-2.79653353348927));
#43989=CARTESIAN_POINT('Ctrl Pts',(-69.7075238284095,-2.13597431478577,
-4.33779788014045));
#43990=CARTESIAN_POINT('Ctrl Pts',(-69.5889917291594,0.188277650519182,
-4.83150372703897));
#43991=CARTESIAN_POINT('Ctrl Pts',(-69.4704596299094,2.46706141544487,-4.15842334294387));
#43992=CARTESIAN_POINT('Ctrl Pts',(-69.3519275306592,4.15006104346198,-2.48110259124925));
#43993=CARTESIAN_POINT('Ctrl Pts',(-69.2333954314092,4.83083975921817,-0.204606820614051));
#43994=CARTESIAN_POINT('Ctrl Pts',(-69.1148633321591,4.34499259254299,2.12130056844982));
#43995=CARTESIAN_POINT('Ctrl Pts',(-68.9963312329089,2.8098494293572,3.93492349548534));
#43996=CARTESIAN_POINT('Ctrl Pts',(-68.877799133659,0.596140378289115,4.79828025235803));
#43997=CARTESIAN_POINT('Ctrl Pts',(-68.7592670344088,-1.76153386927439,
4.50287409976691));
#43998=CARTESIAN_POINT('Ctrl Pts',(-68.6407349351588,-3.6938056800729,3.12004428313488));
#43999=CARTESIAN_POINT('Ctrl Pts',(-68.5222028359086,-4.7340401791978,0.983737928842413));
#44000=CARTESIAN_POINT('Ctrl Pts',(-68.4036707366586,-4.63102545499782,
-1.39013667171659));
#44001=CARTESIAN_POINT('Ctrl Pts',(-68.2851386374085,-3.40963909595999,
-3.42829957357751));
#44002=CARTESIAN_POINT('Ctrl Pts',(-68.1666065381584,-1.36484036594256,
-4.6385436837855));
#44003=CARTESIAN_POINT('Ctrl Pts',(-68.0480744389084,1.00956111970321,-4.72860054101359));
#44004=CARTESIAN_POINT('Ctrl Pts',(-67.9295423396582,3.14015817566407,-3.67672182286094));
#44005=CARTESIAN_POINT('Ctrl Pts',(-67.8110102404082,4.51242128017076,-1.73693146702832));
#44006=CARTESIAN_POINT('Ctrl Pts',(-67.692478141158,4.79495511991091,0.622319957040978));
#44007=CARTESIAN_POINT('Ctrl Pts',(-67.573946041908,3.9195290545396,2.83128393516286));
#44008=CARTESIAN_POINT('Ctrl Pts',(-67.4554139426579,2.09755450673732,4.35650568944393));
#44009=CARTESIAN_POINT('Ctrl Pts',(-67.3368818434078,-0.23096993712172,
4.82965108667669));
#44010=CARTESIAN_POINT('Ctrl Pts',(-67.2183497441577,-2.50371618915523,
4.1364576602515));
#44011=CARTESIAN_POINT('Ctrl Pts',(-67.0998176449076,-4.17182634172216,
2.44432847739504));
#44012=CARTESIAN_POINT('Ctrl Pts',(-66.9812855456576,-4.83245936176243,
0.161905057999808));
#44013=CARTESIAN_POINT('Ctrl Pts',(-66.8627534464075,-4.32607537245367,
-2.15961769828392));
#44014=CARTESIAN_POINT('Ctrl Pts',(-66.7442213471574,-2.77496380957702,
-3.95960257935429));
#44015=CARTESIAN_POINT('Ctrl Pts',(-66.6256892479073,-0.553711077644903,
-4.80336140357819));
#44016=CARTESIAN_POINT('Ctrl Pts',(-66.5071571486572,1.80126036716239,-4.48713024332717));
#44017=CARTESIAN_POINT('Ctrl Pts',(-66.3886250494071,3.72123560623268,-3.08727748895322));
#44018=CARTESIAN_POINT('Ctrl Pts',(-66.270092950157,4.74254933091315,-0.941861229028204));
#44019=CARTESIAN_POINT('Ctrl Pts',(-66.151560850907,4.61855891074222,1.43101024416146));
#44020=CARTESIAN_POINT('Ctrl Pts',(-66.0330287516568,3.37920746960428,3.45829923636778));
#44021=CARTESIAN_POINT('Ctrl Pts',(-65.9144966524068,1.32379275717391,4.6504246544746));
#44022=CARTESIAN_POINT('Ctrl Pts',(-65.7959645531566,-1.05131189961462,
4.71949361908881));
#44023=CARTESIAN_POINT('Ctrl Pts',(-65.6774324539066,-3.17252950280694,
3.64882628864555));
#44024=CARTESIAN_POINT('Ctrl Pts',(-65.5589003546565,-4.52759562591996,
1.69698396546396));
#44025=CARTESIAN_POINT('Ctrl Pts',(-65.4403682554064,-4.78926794861912,
-0.664672285582053));
#44026=CARTESIAN_POINT('Ctrl Pts',(-65.3218361561563,-3.89435379226919,
-2.86581319550488));
#44027=CARTESIAN_POINT('Ctrl Pts',(-65.2033040569063,-2.05897086509784,
-4.37487322188536));
#44028=CARTESIAN_POINT('Ctrl Pts',(-65.0847719576561,0.273644183741452,
-4.82742121547268));
#44029=CARTESIAN_POINT('Ctrl Pts',(-64.9662398584062,2.5401754038242,-4.11416888918016));
#44030=CARTESIAN_POINT('Ctrl Pts',(-64.8477077591559,4.19326578952573,-2.40736344353829));
#44031=CARTESIAN_POINT('Ctrl Pts',(-64.7291756599059,4.83370151333408,-0.119190649311063));
#44032=CARTESIAN_POINT('Ctrl Pts',(-64.6106435606558,4.30682025382488,2.19776614591613));
#44033=CARTESIAN_POINT('Ctrl Pts',(-64.4921114614057,2.73986144452965,3.98397238891927));
#44034=CARTESIAN_POINT('Ctrl Pts',(-64.3735793621556,0.511238528066523,
4.80806737664019));
#44035=CARTESIAN_POINT('Ctrl Pts',(-64.2550472629056,-1.8408461732611,4.47103590874434));
#44036=CARTESIAN_POINT('Ctrl Pts',(-64.1365151636554,-3.74837487629322,
3.0542695555018));
#44037=CARTESIAN_POINT('Ctrl Pts',(-64.0179830644054,-4.75068805435598,
0.899910962868411));
#44038=CARTESIAN_POINT('Ctrl Pts',(-63.8994509651552,-4.60573162278402,
-1.47177204409466));
#44039=CARTESIAN_POINT('Ctrl Pts',(-63.7809188659052,-3.34851190208522,
-3.48802878034068));
#44040=CARTESIAN_POINT('Ctrl Pts',(-63.6623867666551,-1.28264175037359,
-4.66194239251087));
#44041=CARTESIAN_POINT('Ctrl Pts',(-63.5438546674051,1.09298056427011,-4.71001806971258));
#44042=CARTESIAN_POINT('Ctrl Pts',(-63.4253225681549,3.20465303186822,-3.62064575403741));
#44043=CARTESIAN_POINT('Ctrl Pts',(-63.3067904689049,4.54241633287416,-1.65690391686706));
#44044=CARTESIAN_POINT('Ctrl Pts',(-63.1882583696547,4.78320669998339,0.706972698288407));
#44045=CARTESIAN_POINT('Ctrl Pts',(-63.0697262704047,3.86887435208713,2.90011861458352));
#44046=CARTESIAN_POINT('Ctrl Pts',(-62.9511941711546,2.02022640256444,4.39289904428418));
#44047=CARTESIAN_POINT('Ctrl Pts',(-62.8326620719045,-0.316297056721141,
4.82481428687165));
#44048=CARTESIAN_POINT('Ctrl Pts',(-62.7141299726544,-2.57643621195637,
4.09155877100791));
#44049=CARTESIAN_POINT('Ctrl Pts',(-62.5955978734043,-4.21437771217373,
2.37021037674359));
#44050=CARTESIAN_POINT('Ctrl Pts',(-62.4770657741542,-4.8345661169712,0.0764669309488382));
#44051=CARTESIAN_POINT('Ctrl Pts',(-62.3585336749042,-4.28722874059428,
-2.23574293171377));
#44052=CARTESIAN_POINT('Ctrl Pts',(-62.2400015756541,-2.70454507598614,
-4.00803102069538));
#44053=CARTESIAN_POINT('Ctrl Pts',(-62.121469476404,-0.468726046964763,
-4.81239780398398));
#44054=CARTESIAN_POINT('Ctrl Pts',(-62.0029373771539,1.8802881956162,-4.45459235309891));
#44055=CARTESIAN_POINT('Ctrl Pts',(-61.8844052779038,3.77522137048981,-3.02102306094952));
#44056=CARTESIAN_POINT('Ctrl Pts',(-61.7658731786537,4.75845571380694,-0.857890406984954));
#44057=CARTESIAN_POINT('Ctrl Pts',(-61.6473410794037,4.59254459307791,1.5124188877089));
#44058=CARTESIAN_POINT('Ctrl Pts',(-61.5288089801535,3.31755479085771,3.517485883414));
#44059=CARTESIAN_POINT('Ctrl Pts',(-61.4102768809035,1.24139055993465,4.67309599824245));
#44060=CARTESIAN_POINT('Ctrl Pts',(-61.2917447816533,-1.13456385942904,
4.70017463305793));
#44061=CARTESIAN_POINT('Ctrl Pts',(-61.1732126824033,-3.23652625297439,
3.59218242001983));
#44062=CARTESIAN_POINT('Ctrl Pts',(-61.0546805831532,-4.55688224501281,
1.61669445203919));
#44063=CARTESIAN_POINT('Ctrl Pts',(-60.9361484839031,-4.77677184423655,
-0.749217891692864));
#44064=CARTESIAN_POINT('Ctrl Pts',(-60.817616384653,-3.84309273056335,-2.93419751186658));
#44065=CARTESIAN_POINT('Ctrl Pts',(-60.699084285403,-1.9813241324019,-4.41058175075367));
#44066=CARTESIAN_POINT('Ctrl Pts',(-60.5805521861528,0.358925198440316,
-4.82183050033724));
#44067=CARTESIAN_POINT('Ctrl Pts',(-60.4620200869028,2.6124958339146,-4.06862908012547));
#44068=CARTESIAN_POINT('Ctrl Pts',(-60.3434879876527,4.23516035471804,-2.33287216207629));
#44069=CARTESIAN_POINT('Ctrl Pts',(-60.2249558884025,4.83505331855051,-0.0337372739214764));
#44070=CARTESIAN_POINT('Ctrl Pts',(-60.1064237891525,4.26730193315002,2.27354515783043));
#44071=CARTESIAN_POINT('Ctrl Pts',(-59.9878916899025,2.66901832824221,4.03177645770732));
#44072=CARTESIAN_POINT('Ctrl Pts',(-59.8693595906523,0.426175210907464,
4.81635262496778));
#44073=CARTESIAN_POINT('Ctrl Pts',(-59.7508274914023,-1.91957984074924,
4.43780030160997));
#44074=CARTESIAN_POINT('Ctrl Pts',(-59.6322953921521,-3.80178006744974,
2.98754172835162));
#44075=CARTESIAN_POINT('Ctrl Pts',(-59.5137632929021,-4.76583745049515,
0.815800574795077));
#44076=CARTESIAN_POINT('Ctrl Pts',(-59.395231193652,-4.57902756281045,-1.55294302820165));
#44077=CARTESIAN_POINT('Ctrl Pts',(-59.2766990944019,-3.28628066519173,
-3.54667748409246));
#44078=CARTESIAN_POINT('Ctrl Pts',(-59.1581669951518,-1.20015991556334,
-4.68386547959001));
#44079=CARTESIAN_POINT('Ctrl Pts',(-59.0396348959018,1.17630498730679,-4.69000696058032));
#44080=CARTESIAN_POINT('Ctrl Pts',(-58.9606134964017,2.57036993835409,-3.93879461861823));
#44081=CARTESIAN_POINT('Ctrl Pts',(-58.9211027966516,3.13634117333409,-3.41972378108142));
#44082=CARTESIAN_POINT('Ctrl Pts',(-89.575,-2.1683958723107,4.42195480991675));
#44083=CARTESIAN_POINT('Ctrl Pts',(-89.53548930025,-2.90023837919381,4.0630808866582));
#44084=CARTESIAN_POINT('Ctrl Pts',(-89.4564679007499,-4.18158777943873,
2.97533030318424));
#44085=CARTESIAN_POINT('Ctrl Pts',(-89.3379358014998,-5.09393729919481,
0.623762189627529));
#44086=CARTESIAN_POINT('Ctrl Pts',(-89.2194037022498,-4.7760113611239,-1.87790340886064));
#44087=CARTESIAN_POINT('Ctrl Pts',(-89.1008716029996,-3.30475671773202,
-3.92632446201307));
#44088=CARTESIAN_POINT('Ctrl Pts',(-88.9823395037497,-1.035390253221,-5.02642719512737));
#44089=CARTESIAN_POINT('Ctrl Pts',(-88.8638074044994,1.48400432002415,-4.91273446231162));
#44090=CARTESIAN_POINT('Ctrl Pts',(-88.7452753052495,3.6450255042766,-3.61260692861675));
#44091=CARTESIAN_POINT('Ctrl Pts',(-88.6267432059992,4.92578613196527,-1.44006696053689));
#44092=CARTESIAN_POINT('Ctrl Pts',(-88.5082111067493,5.01699346462279,1.08025046241909));
#44093=CARTESIAN_POINT('Ctrl Pts',(-88.3896790074991,3.89661879247731,3.33968841879312));
#44094=CARTESIAN_POINT('Ctrl Pts',(-88.2711469082491,1.83522878269921,4.79260870230941));
#44095=CARTESIAN_POINT('Ctrl Pts',(-88.1526148089989,-0.669360859787416,
5.08813477323801));
#44096=CARTESIAN_POINT('Ctrl Pts',(-88.0340827097489,-3.01230278811849,
4.15489985799353));
#44097=CARTESIAN_POINT('Ctrl Pts',(-87.9155506104988,-4.62778731241589,
2.21827524343903));
#44098=CARTESIAN_POINT('Ctrl Pts',(-87.7970185112487,-5.12568217307047,
-0.254052660266212));
#44099=CARTESIAN_POINT('Ctrl Pts',(-87.6784864119986,-4.38574805857882,
-2.66502805736134));
#44100=CARTESIAN_POINT('Ctrl Pts',(-87.5599543127485,-2.58667568127932,
-4.43241124189013));
#44101=CARTESIAN_POINT('Ctrl Pts',(-87.4414222134984,-0.162932866706595,
-5.1293872371898));
#44102=CARTESIAN_POINT('Ctrl Pts',(-87.3228901142484,2.30015749744563,-4.5876394813756));
#44103=CARTESIAN_POINT('Ctrl Pts',(-87.2043580149983,4.20777026179349,-2.93799761002543));
#44104=CARTESIAN_POINT('Ctrl Pts',(-87.0858259157481,5.09922560038977,-0.578842644798489));
#44105=CARTESIAN_POINT('Ctrl Pts',(-86.9672938164982,4.75924109322802,1.92010019187045));
#44106=CARTESIAN_POINT('Ctrl Pts',(-86.8487617172479,3.2699214564463,3.95534754478431));
#44107=CARTESIAN_POINT('Ctrl Pts',(-86.730229617998,0.990930624635091,5.03539641217931));
#44108=CARTESIAN_POINT('Ctrl Pts',(-86.6116975187478,-1.52736545681198,
4.89941989345072));
#44109=CARTESIAN_POINT('Ctrl Pts',(-86.4931654194978,-3.6768097106286,3.58025570074025));
#44110=CARTESIAN_POINT('Ctrl Pts',(-86.3746333202476,-4.93832110226258,
1.39647600116869));
#44111=CARTESIAN_POINT('Ctrl Pts',(-86.2561012209977,-5.0072503545504,-1.12454631641016));
#44112=CARTESIAN_POINT('Ctrl Pts',(-86.1375691217474,-3.86695136581583,
-3.37399580101973));
#44113=CARTESIAN_POINT('Ctrl Pts',(-86.0190370224974,-1.79280116791488,
-4.80864060865615));
#44114=CARTESIAN_POINT('Ctrl Pts',(-85.9005049232473,0.71430237748739,-5.08202052774328));
#44115=CARTESIAN_POINT('Ctrl Pts',(-85.7819728239972,3.04890513975984,-4.12811554824192));
#44116=CARTESIAN_POINT('Ctrl Pts',(-85.6634407247472,4.64721114470303,-2.17728939450819));
#44117=CARTESIAN_POINT('Ctrl Pts',(-85.544908625497,5.12323674418264,0.299342268894373));
#44118=CARTESIAN_POINT('Ctrl Pts',(-85.426376526247,4.36202391581492,2.70368413257703));
#44119=CARTESIAN_POINT('Ctrl Pts',(-85.3078444269969,2.54740210376838,4.45509854577948));
#44120=CARTESIAN_POINT('Ctrl Pts',(-85.1893123277468,0.117594242094089,
5.13062687447805));
#44121=CARTESIAN_POINT('Ctrl Pts',(-85.0707802284967,-2.34061209548073,
4.56713209239445));
#44122=CARTESIAN_POINT('Ctrl Pts',(-84.9522481292467,-4.23357123215246,
2.90069563263386));
#44123=CARTESIAN_POINT('Ctrl Pts',(-84.8337160299965,-5.10414212541622,
0.533754339037759));
#44124=CARTESIAN_POINT('Ctrl Pts',(-84.7151839307465,-4.74208585462591,
-1.96208620561045));
#44125=CARTESIAN_POINT('Ctrl Pts',(-84.5966518314963,-3.23483736640461,
-3.98409183425815));
#44126=CARTESIAN_POINT('Ctrl Pts',(-84.4781197322463,-0.946390331757192,
-5.04395736211623));
#44127=CARTESIAN_POINT('Ctrl Pts',(-84.3595876329962,1.57060567391381,-4.88573007317839));
#44128=CARTESIAN_POINT('Ctrl Pts',(-84.2410555337461,3.70830753570835,-3.54762113979195));
#44129=CARTESIAN_POINT('Ctrl Pts',(-84.122523434496,4.95046995348558,-1.35277779791302));
#44130=CARTESIAN_POINT('Ctrl Pts',(-84.0039913352459,4.99711633946695,1.16875524414756));
#44131=CARTESIAN_POINT('Ctrl Pts',(-83.885459235996,3.83698180308851,3.40803919778774));
#44132=CARTESIAN_POINT('Ctrl Pts',(-83.7669271367456,1.7502335709595,4.82429714859857));
#44133=CARTESIAN_POINT('Ctrl Pts',(-83.6483950374958,-0.759188127149455,
5.0755092275047));
#44134=CARTESIAN_POINT('Ctrl Pts',(-83.5298629382456,-3.08526933724734,
4.10100885728516));
#44135=CARTESIAN_POINT('Ctrl Pts',(-83.4113308389955,-4.66627200131942,
2.13613345570741));
#44136=CARTESIAN_POINT('Ctrl Pts',(-83.2927987397455,-5.12039114954072,
-0.344608483057541));
#44137=CARTESIAN_POINT('Ctrl Pts',(-83.1742666404952,-4.33795906810922,
-2.74212903677033));
#44138=CARTESIAN_POINT('Ctrl Pts',(-83.0557345412453,-2.50792955452944,
-4.47743787007791));
#44139=CARTESIAN_POINT('Ctrl Pts',(-82.9372024419952,-0.0722464328626828,
-5.13146577342465));
#44140=CARTESIAN_POINT('Ctrl Pts',(-82.818670342745,2.38088387453369,-4.54626797570001));
#44141=CARTESIAN_POINT('Ctrl Pts',(-82.7001382434951,4.25904152911249,-2.86316708981246));
#44142=CARTESIAN_POINT('Ctrl Pts',(-82.5816061442448,5.1086599791349,-0.488624342900971));
#44143=CARTESIAN_POINT('Ctrl Pts',(-82.4630740449948,4.72456022392924,2.00391896576577));
#44144=CARTESIAN_POINT('Ctrl Pts',(-82.3445419457448,3.19950061158604,4.01252493666403));
#44145=CARTESIAN_POINT('Ctrl Pts',(-82.2260098464945,0.901776118770504,
5.05212434155229));
#44146=CARTESIAN_POINT('Ctrl Pts',(-82.1074777472446,-1.61372321506223,
4.87165864116722));
#44147=CARTESIAN_POINT('Ctrl Pts',(-81.9889456479944,-3.73951571447014,
3.51470948331734));
#44148=CARTESIAN_POINT('Ctrl Pts',(-81.8704135487444,-4.96223213629194,
1.30897393268221));
#44149=CARTESIAN_POINT('Ctrl Pts',(-81.7518814494944,-4.98659201253917,
-1.21287288343444));
#44150=CARTESIAN_POINT('Ctrl Pts',(-81.6333493502442,-3.80671254362719,
-3.44181640141966));
#44151=CARTESIAN_POINT('Ctrl Pts',(-81.5148172509941,-1.70752926778261,
-4.83957687515715));
#44152=CARTESIAN_POINT('Ctrl Pts',(-81.3962851517441,0.804014578588726,
-5.06860149235535));
#44153=CARTESIAN_POINT('Ctrl Pts',(-81.2777530524939,3.12139255231928,-4.0735818471237));
#44154=CARTESIAN_POINT('Ctrl Pts',(-81.1592209532439,4.68496838748752,-2.09481066904211));
#44155=CARTESIAN_POINT('Ctrl Pts',(-81.0406888539937,5.11714561437722,0.389847780742552));
#44156=CARTESIAN_POINT('Ctrl Pts',(-80.9221567547437,4.31355539363008,2.78035976035025));
#44157=CARTESIAN_POINT('Ctrl Pts',(-80.8036246554936,2.46826111739352,4.49942747327406));
#44158=CARTESIAN_POINT('Ctrl Pts',(-80.6850925562435,0.0268929806491242,
5.13190386683944));
#44159=CARTESIAN_POINT('Ctrl Pts',(-80.5665604569934,-2.42096968889947,
4.52504876176164));
#44160=CARTESIAN_POINT('Ctrl Pts',(-80.4480283577434,-4.28417916334405,
2.82541491240804));
#44161=CARTESIAN_POINT('Ctrl Pts',(-80.3294962584932,-5.11277880862357,
0.443456181579524));
#44162=CARTESIAN_POINT('Ctrl Pts',(-80.2109641592432,-4.70666557004154,
-2.04559520498919));
#44163=CARTESIAN_POINT('Ctrl Pts',(-80.0924320599931,-3.16391395204272,
-4.04064463111481));
#44164=CARTESIAN_POINT('Ctrl Pts',(-79.9738999607429,-0.857091470380425,
-5.05989671261218));
#44165=CARTESIAN_POINT('Ctrl Pts',(-79.855367861493,1.65671471245823,-4.85720669648522));
#44166=CARTESIAN_POINT('Ctrl Pts',(-79.7368357622428,3.77043180932637,-3.48152330197269));
#44167=CARTESIAN_POINT('Ctrl Pts',(-79.6183036629927,4.97360673196066,-1.26506782686858));
#44168=CARTESIAN_POINT('Ctrl Pts',(-79.4997715637427,4.9756781958107,1.25689578833165));
#44169=CARTESIAN_POINT('Ctrl Pts',(-79.3812394644924,3.77614595165346,3.47532477371217));
#44170=CARTESIAN_POINT('Ctrl Pts',(-79.2627073652425,1.66469159397173,4.85447859477892));
#44171=CARTESIAN_POINT('Ctrl Pts',(-79.1441752659923,-0.848778230657501,
5.06129786202729));
#44172=CARTESIAN_POINT('Ctrl Pts',(-79.0256431667423,-3.15727196322148,
4.04583665963461));
#44173=CARTESIAN_POINT('Ctrl Pts',(-78.9071110674922,-4.70329884341097,
2.05332426288532));
#44174=CARTESIAN_POINT('Ctrl Pts',(-78.7885789682421,-5.11350039112483,
-0.435056629949174));
#44175=CARTESIAN_POINT('Ctrl Pts',(-78.670046868992,-4.28881480063609,-2.81837331414327));
#44176=CARTESIAN_POINT('Ctrl Pts',(-78.551514769742,-2.42839988642778,-4.52106564400155));
#44177=CARTESIAN_POINT('Ctrl Pts',(-78.4329826704918,0.0184625633801521,
-5.13194110804669));
#44178=CARTESIAN_POINT('Ctrl Pts',(-78.3144505712419,2.46086642515392,-4.50347613304934));
#44179=CARTESIAN_POINT('Ctrl Pts',(-78.1959184719916,4.30898213601093,-2.78744199860449));
#44180=CARTESIAN_POINT('Ctrl Pts',(-78.0773863727416,5.11649836347594,-0.398253484843363));
#44181=CARTESIAN_POINT('Ctrl Pts',(-77.9588542734915,4.68840314704361,2.08711187310909));
#44182=CARTESIAN_POINT('Ctrl Pts',(-77.8403221742414,3.12808045664934,4.06844830823227));
#44183=CARTESIAN_POINT('Ctrl Pts',(-77.7217900749914,0.812339294087262,
5.06727470013674));
#44184=CARTESIAN_POINT('Ctrl Pts',(-77.6032579757413,-1.69957563445067,
4.84237369225633));
#44185=CARTESIAN_POINT('Ctrl Pts',(-77.4847258764911,-3.80105576959598,
3.44806856305101));
#44186=CARTESIAN_POINT('Ctrl Pts',(-77.3661937772411,-4.98458809021849,
1.22105611142095));
#44187=CARTESIAN_POINT('Ctrl Pts',(-77.247661677991,-4.96438533316134,-1.30080682669047));
#44188=CARTESIAN_POINT('Ctrl Pts',(-77.1291295787408,-3.74526509529329,
-3.50858927954838));
#44189=CARTESIAN_POINT('Ctrl Pts',(-77.0105974794909,-1.62176280909601,
-4.86894558674816));
#44190=CARTESIAN_POINT('Ctrl Pts',(-76.8920653802408,0.89355396800014,-5.05371081114237));
#44191=CARTESIAN_POINT('Ctrl Pts',(-76.7735332809906,3.19274689014148,-4.01755006136377));
#44192=CARTESIAN_POINT('Ctrl Pts',(-76.6550011817407,4.72157993762085,-2.01213148330597));
#44193=CARTESIAN_POINT('Ctrl Pts',(-76.5364690824904,5.10881525506152,0.481145928240669));
#44194=CARTESIAN_POINT('Ctrl Pts',(-76.4179369832404,4.26502912909379,2.85432546075147));
#44195=CARTESIAN_POINT('Ctrl Pts',(-76.2994048839903,2.38575426223333,4.54605041176487));
#44196=CARTESIAN_POINT('Ctrl Pts',(-76.1808727847402,-0.0586304569932881,
5.12423622545075));
#44197=CARTESIAN_POINT('Ctrl Pts',(-76.0228299857401,-3.32730071870205,
4.28413857816343));
#44198=CARTESIAN_POINT('Ctrl Pts',(-75.8252764869899,-5.79800776750144,
0.407060071887531));
#44199=CARTESIAN_POINT('Ctrl Pts',(-75.5882122884898,-3.50201925403669,
-4.6424700454491));
#44200=CARTESIAN_POINT('Ctrl Pts',(-75.3511480899896,1.97333698956357,-5.46509721364885));
#44201=CARTESIAN_POINT('Ctrl Pts',(-75.1140838914894,5.65721329219971,-1.33393092111982));
#44202=CARTESIAN_POINT('Ctrl Pts',(-74.8770196929893,4.2064485155352,4.01142976688134));
#44203=CARTESIAN_POINT('Ctrl Pts',(-74.6399554944891,-1.06247369676832,
5.71399827760396));
#44204=CARTESIAN_POINT('Ctrl Pts',(-74.4028912959888,-5.36691831356058,
2.23109054171393));
#44205=CARTESIAN_POINT('Ctrl Pts',(-74.1658270974888,-4.80016278000401,
-3.27733022492635));
#44206=CARTESIAN_POINT('Ctrl Pts',(-73.9287628989886,0.123765115632612,
-5.81087423593989));
#44207=CARTESIAN_POINT('Ctrl Pts',(-73.6916987004883,4.93489541950005,-3.07008694850533));
#44208=CARTESIAN_POINT('Ctrl Pts',(-73.4546345019883,5.26768982704656,2.45707585851558));
#44209=CARTESIAN_POINT('Ctrl Pts',(-73.217570303488,0.817508891785283,5.75457323766176));
#44210=CARTESIAN_POINT('Ctrl Pts',(-72.9805061049879,-4.37142214619141,
3.82779503745949));
#44211=CARTESIAN_POINT('Ctrl Pts',(-72.7434419064876,-5.59891928802401,
-1.57123193218838));
#44212=CARTESIAN_POINT('Ctrl Pts',(-72.5063777079877,-1.73201933659968,
-5.54821601884577));
#44213=CARTESIAN_POINT('Ctrl Pts',(-72.3088242092372,2.77853388249591,-4.65881131764377));
#44214=CARTESIAN_POINT('Ctrl Pts',(-72.1507814102373,4.75113147133521,-1.92041249912545));
#44215=CARTESIAN_POINT('Ctrl Pts',(-72.0322493109871,5.1026705975271,0.566701437446899));
#44216=CARTESIAN_POINT('Ctrl Pts',(-71.9137172117371,4.21134573810842,2.93295318442499));
#44217=CARTESIAN_POINT('Ctrl Pts',(-71.795185112487,2.30830912398487,4.5829252342516));
#44218=CARTESIAN_POINT('Ctrl Pts',(-71.6766530132369,-0.154813461705778,
5.13010945356231));
#44219=CARTESIAN_POINT('Ctrl Pts',(-71.5581209139868,-2.57923845933515,
4.43642538198926));
#44220=CARTESIAN_POINT('Ctrl Pts',(-71.4395888147368,-4.38143988039363,
2.67234283558125));
#44221=CARTESIAN_POINT('Ctrl Pts',(-71.3210567154866,-5.1252203438306,0.262416011070538));
#44222=CARTESIAN_POINT('Ctrl Pts',(-71.2025246162366,-4.63144376111743,
-2.21064200045838));
#44223=CARTESIAN_POINT('Ctrl Pts',(-71.0839925169864,-3.01911488518057,
-4.14995969216005));
#44224=CARTESIAN_POINT('Ctrl Pts',(-70.9654604177364,-0.677723001576583,
-5.08702152438147));
#44225=CARTESIAN_POINT('Ctrl Pts',(-70.8469283184864,1.82735554135264,-4.79562024190483));
#44226=CARTESIAN_POINT('Ctrl Pts',(-70.7283962192361,3.89112626696975,-3.34608378364507));
#44227=CARTESIAN_POINT('Ctrl Pts',(-70.6098641199861,5.01521249276049,-1.08849054558277));
#44228=CARTESIAN_POINT('Ctrl Pts',(-70.4913320207361,4.92814525523101,1.43197183050982));
#44229=CARTESIAN_POINT('Ctrl Pts',(-70.3727999214859,3.65095449177829,3.60661771456934));
#44230=CARTESIAN_POINT('Ctrl Pts',(-70.2542678222359,1.49207419213024,4.91028267483867));
#44231=CARTESIAN_POINT('Ctrl Pts',(-70.1357357229858,-1.02713496093071,
5.02813620699353));
#44232=CARTESIAN_POINT('Ctrl Pts',(-70.0172036237357,-3.29829582731872,
3.9317178788523));
#44233=CARTESIAN_POINT('Ctrl Pts',(-69.8986715244855,-4.77293314445299,
1.88580741362638));
#44234=CARTESIAN_POINT('Ctrl Pts',(-69.7801394252356,-5.09492879959653,
-0.61551693137989));
#44235=CARTESIAN_POINT('Ctrl Pts',(-69.6616073259854,-4.18652224921013,
-2.96819675710668));
#44236=CARTESIAN_POINT('Ctrl Pts',(-69.5430752267354,-2.26708958018463,
-4.60407052038899));
#44237=CARTESIAN_POINT('Ctrl Pts',(-69.4245431274853,0.199834940298159,
-5.12808214985099));
#44238=CARTESIAN_POINT('Ctrl Pts',(-69.3060110282352,2.61850022723304,-4.41368520469782));
#44239=CARTESIAN_POINT('Ctrl Pts',(-69.1874789289851,4.4048095914048,-2.63340331063596));
#44240=CARTESIAN_POINT('Ctrl Pts',(-69.068946829735,5.12737742483736,-0.217166464895158));
#44241=CARTESIAN_POINT('Ctrl Pts',(-68.950414730485,4.61170687509952,2.25151509635759));
#44242=CARTESIAN_POINT('Ctrl Pts',(-68.8318826312348,2.98233003977967,4.17646597793152));
#44243=CARTESIAN_POINT('Ctrl Pts',(-68.7133505319847,0.632734031767687,
5.09281927578678));
#44244=CARTESIAN_POINT('Ctrl Pts',(-68.5948184327347,-1.8696643740188,4.77927982644706));
#44245=CARTESIAN_POINT('Ctrl Pts',(-68.4762863334846,-3.92054731676857,
3.31156598421883));
#44246=CARTESIAN_POINT('Ctrl Pts',(-68.3577542342345,-5.02463587138733,
1.04412398251837));
#44247=CARTESIAN_POINT('Ctrl Pts',(-68.2392221349844,-4.915297661549,-1.47546922341958));
#44248=CARTESIAN_POINT('Ctrl Pts',(-68.1206900357343,-3.61893736883079,
-3.6387433066059));
#44249=CARTESIAN_POINT('Ctrl Pts',(-68.0021579364842,-1.4486201218923,-4.92327739146802));
#44250=CARTESIAN_POINT('Ctrl Pts',(-67.8836258372342,1.07153231159905,-5.01886232487884));
#44251=CARTESIAN_POINT('Ctrl Pts',(-67.765093737984,3.33291455374709,-3.9024147791222));
#44252=CARTESIAN_POINT('Ctrl Pts',(-67.646561638734,4.78941305373535,-1.84355177079443));
#44253=CARTESIAN_POINT('Ctrl Pts',(-67.5280295394838,5.08929003244738,0.660520625356854));
#44254=CARTESIAN_POINT('Ctrl Pts',(-67.4094974402338,4.16012656016829,3.00508028749189));
#44255=CARTESIAN_POINT('Ctrl Pts',(-67.2909653409837,2.22631139952188,4.62392669527201));
#44256=CARTESIAN_POINT('Ctrl Pts',(-67.1724332417336,-0.24514786257484,
5.12611578647664));
#44257=CARTESIAN_POINT('Ctrl Pts',(-67.0539011424836,-2.65740502817917,
4.39037117418312));
#44258=CARTESIAN_POINT('Ctrl Pts',(-66.9353690432334,-4.42791093703134,
2.59437184393606));
#44259=CARTESIAN_POINT('Ctrl Pts',(-66.8168369439834,-5.12909644553283,
0.171843484928528));
#44260=CARTESIAN_POINT('Ctrl Pts',(-66.6983048447333,-4.59162843489841,
-2.29218429597677));
#44261=CARTESIAN_POINT('Ctrl Pts',(-66.5797727454832,-2.94530299102049,
-4.20265996982576));
#44262=CARTESIAN_POINT('Ctrl Pts',(-66.4612406462331,-0.587700238655496,
-5.0982123298637));
#44263=CARTESIAN_POINT('Ctrl Pts',(-66.342708546983,1.91182945474832,-4.76256954456801));
#44264=CARTESIAN_POINT('Ctrl Pts',(-66.2241764477329,3.9496610094528,-3.2767878236618));
#44265=CARTESIAN_POINT('Ctrl Pts',(-66.1056443484829,5.03366735133376,-0.999676711245437));
#44266=CARTESIAN_POINT('Ctrl Pts',(-65.9871122492328,4.90206586733353,1.51885179106248));
#44267=CARTESIAN_POINT('Ctrl Pts',(-65.8685801499827,3.58663771871725,3.67058447737751));
#44268=CARTESIAN_POINT('Ctrl Pts',(-65.7500480507326,1.40505283482956,4.93588766709976));
#44269=CARTESIAN_POINT('Ctrl Pts',(-65.6315159514825,-1.11584593346544,
5.00919638102347));
#44270=CARTESIAN_POINT('Ctrl Pts',(-65.5129838522324,-3.36727297180218,
3.87280689736275));
#44271=CARTESIAN_POINT('Ctrl Pts',(-65.3944517529823,-4.80551886591482,
1.80115212023493));
#44272=CARTESIAN_POINT('Ctrl Pts',(-65.2759196537322,-5.08325375818739,
-0.705472721488053));
#44273=CARTESIAN_POINT('Ctrl Pts',(-65.1573875544821,-4.13340593231403,
-3.04172910194205));
#44274=CARTESIAN_POINT('Ctrl Pts',(-65.0388554552321,-2.18535932845954,
-4.6434217056396));
#44275=CARTESIAN_POINT('Ctrl Pts',(-64.9203233559819,0.290441637497185,
-5.12374903621342));
#44276=CARTESIAN_POINT('Ctrl Pts',(-64.8017912567319,2.69610226583112,-4.36671422273892));
#44277=CARTESIAN_POINT('Ctrl Pts',(-64.6832591574818,4.45066643010254,-2.55513773774495));
#44278=CARTESIAN_POINT('Ctrl Pts',(-64.5647270582317,5.13041484569598,-0.126507082617098));
#44279=CARTESIAN_POINT('Ctrl Pts',(-64.4461949589817,4.57119135449609,2.33267445895697));
#44280=CARTESIAN_POINT('Ctrl Pts',(-64.3276628597315,2.90804589223992,4.22852570283266));
#44281=CARTESIAN_POINT('Ctrl Pts',(-64.2091307604815,0.54262054180405,5.10320717573785));
#44282=CARTESIAN_POINT('Ctrl Pts',(-64.0905986612314,-1.95384520742303,
4.74548727069414));
#44283=CARTESIAN_POINT('Ctrl Pts',(-63.9720665619812,-3.97846620431968,
3.24175372167231));
#44284=CARTESIAN_POINT('Ctrl Pts',(-63.8535344627312,-5.04230566453141,
0.955151357809071));
#44285=CARTESIAN_POINT('Ctrl Pts',(-63.7350023634811,-4.88845118541963,
-1.5621157251175));
#44286=CARTESIAN_POINT('Ctrl Pts',(-63.616470264231,-3.55405792559961,-3.70213894828012));
#44287=CARTESIAN_POINT('Ctrl Pts',(-63.4979381649809,-1.36137580272046,
-4.94811241330038));
#44288=CARTESIAN_POINT('Ctrl Pts',(-63.3794060657308,1.16007239948927,-4.99913918178251));
#44289=CARTESIAN_POINT('Ctrl Pts',(-63.2608739664808,3.40136838086655,-3.84289652066398));
#44290=CARTESIAN_POINT('Ctrl Pts',(-63.1423418672306,4.82124933143318,-1.7586117863375));
#44291=CARTESIAN_POINT('Ctrl Pts',(-63.0238097679807,5.07682044411155,0.750369714967913));
#44292=CARTESIAN_POINT('Ctrl Pts',(-62.9052776687304,4.10636245480316,3.07814033479194));
#44293=CARTESIAN_POINT('Ctrl Pts',(-62.7867455694805,2.14423656462699,4.66255403033645));
#44294=CARTESIAN_POINT('Ctrl Pts',(-62.6682134702303,-0.335712726773787,
5.12098208315281));
#44295=CARTESIAN_POINT('Ctrl Pts',(-62.5496813709803,-2.73458891790202,
4.34271619853037));
#44296=CARTESIAN_POINT('Ctrl Pts',(-62.4311492717301,-4.47307429311926,
2.51570405634761));
#44297=CARTESIAN_POINT('Ctrl Pts',(-62.3126171724801,-5.13133252241295,
0.0811607991645035));
#44298=CARTESIAN_POINT('Ctrl Pts',(-62.19408507323,-4.55039723014839,-2.37298242276288));
#44299=CARTESIAN_POINT('Ctrl Pts',(-62.0755529739799,-2.87056165351069,
-4.25406115662326));
#44300=CARTESIAN_POINT('Ctrl Pts',(-61.9570208747298,-0.497498462261037,
-5.10780342328676));
#44301=CARTESIAN_POINT('Ctrl Pts',(-61.8384887754797,1.99570835029122,-4.72803433907091));
#44302=CARTESIAN_POINT('Ctrl Pts',(-61.7199566762297,4.00696065148427,-3.20646641467831));
#44303=CARTESIAN_POINT('Ctrl Pts',(-61.6014245769795,5.05055013623774,-0.910551399964303));
#44304=CARTESIAN_POINT('Ctrl Pts',(-61.4828924777295,4.87445467926628,1.60525764634163));
#44305=CARTESIAN_POINT('Ctrl Pts',(-61.3643603784793,3.52120053409885,3.73340425469211));
#44306=CARTESIAN_POINT('Ctrl Pts',(-61.2458282792294,1.31759243727128,4.95995067519358));
#44307=CARTESIAN_POINT('Ctrl Pts',(-61.1272961799792,-1.20420825567067,
4.98869151276398));
#44308=CARTESIAN_POINT('Ctrl Pts',(-61.0087640807292,-3.43519811699984,
3.81268598511499));
#44309=CARTESIAN_POINT('Ctrl Pts',(-60.890231981479,-4.83660322330837,1.71593409208573));
#44310=CARTESIAN_POINT('Ctrl Pts',(-60.771699882229,-5.06999058931756,-0.795208099548269));
#44311=CARTESIAN_POINT('Ctrl Pts',(-60.6531677829788,-4.07899824676367,
-3.11431114096681));
#44312=CARTESIAN_POINT('Ctrl Pts',(-60.5346356837288,-2.10294630625613,
-4.68132217717649));
#44313=CARTESIAN_POINT('Ctrl Pts',(-60.4161035844787,0.38095756667902,-5.11781513900239));
#44314=CARTESIAN_POINT('Ctrl Pts',(-60.2975714852286,2.77286203412865,-4.31837898486793));
#44315=CARTESIAN_POINT('Ctrl Pts',(-60.1790393859785,4.49513266340712,-2.47607386190709));
#44316=CARTESIAN_POINT('Ctrl Pts',(-60.0605072867284,5.13184963051497,-0.0358082125060307));
#44317=CARTESIAN_POINT('Ctrl Pts',(-59.9419751874783,4.52924722979,2.41310511166584));
#44318=CARTESIAN_POINT('Ctrl Pts',(-59.8234430882283,2.83285412160331,4.27926419041165));
#44319=CARTESIAN_POINT('Ctrl Pts',(-59.7049109889781,0.452335673370796,
5.11200100814619));
#44320=CARTESIAN_POINT('Ctrl Pts',(-59.5863788897281,-2.03741188513844,
4.71021151943447));
#44321=CARTESIAN_POINT('Ctrl Pts',(-59.467846790478,-4.03514963518333,3.17092985427215));
#44322=CARTESIAN_POINT('Ctrl Pts',(-59.3493146912279,-5.05838499558678,
0.865877913336275));
#44323=CARTESIAN_POINT('Ctrl Pts',(-59.2307825919778,-4.86010791570163,
-1.64826933240034));
#44324=CARTESIAN_POINT('Ctrl Pts',(-59.1122504927277,-3.48800666845358,
-3.76438776103343));
#44325=CARTESIAN_POINT('Ctrl Pts',(-58.9937183934777,-1.27383087909548,
-4.9713812335004));
#44326=CARTESIAN_POINT('Ctrl Pts',(-58.8751862942275,1.24851163302018,-4.97789970493691));
#44327=CARTESIAN_POINT('Ctrl Pts',(-58.7961648947275,2.72815027040562,-4.18057472720697));
#44328=CARTESIAN_POINT('Ctrl Pts',(-58.7566541949775,3.3288632474416,-3.6296410951818));
#44329=CARTESIAN_POINT('Ctrl Pts',(-59.3088415259036,-4.92475008045824,
0.000102229393649578));
#44330=CARTESIAN_POINT('Ctrl Pts',(-59.2892276839357,-4.92444723141628,
-0.40457869844043));
#44331=CARTESIAN_POINT('Ctrl Pts',(-59.2696138419679,-4.8746433485405,-0.809333178910587));
#44332=CARTESIAN_POINT('Ctrl Pts',(-59.25,-4.77631074058413,-1.20178265305869));
#44333=CARTESIAN_POINT('',(-89.575,-2.36246668965802,-3.31495875354372));
#44334=CARTESIAN_POINT('Ctrl Pts',(-89.575,-2.36246668965807,-3.31495875354369));
#44335=CARTESIAN_POINT('Ctrl Pts',(-89.575,-2.45838582797249,-3.26042738788591));
#44336=CARTESIAN_POINT('Ctrl Pts',(-89.575,-2.55193566874186,-3.20204001451282));
#44337=CARTESIAN_POINT('Ctrl Pts',(-89.575,-2.64286961056085,-3.1399345520892));
#44338=CARTESIAN_POINT('Ctrl Pts',(-89.575,-2.74661604656181,-3.06907849709195));
#44339=CARTESIAN_POINT('Ctrl Pts',(-89.575,-2.84695857765234,-2.99338381919177));
#44340=CARTESIAN_POINT('Ctrl Pts',(-89.575,-2.94368691211655,-2.91320714995187));
#44341=CARTESIAN_POINT('Ctrl Pts',(-89.575,-2.99886142577539,-2.86747382107156));
#44342=CARTESIAN_POINT('Ctrl Pts',(-89.575,-3.05285970924591,-2.82028127789999));
#44343=CARTESIAN_POINT('Ctrl Pts',(-89.575,-3.10563962166236,-2.77168887175325));
#44344=CARTESIAN_POINT('Ctrl Pts',(-89.575,-3.14178581168165,-2.73841048485076));
#44345=CARTESIAN_POINT('Ctrl Pts',(-89.575,-3.17736051677501,-2.70447543873133));
#44346=CARTESIAN_POINT('Ctrl Pts',(-89.575,-3.2123494287601,-2.66990159034028));
#44347=CARTESIAN_POINT('Ctrl Pts',(-89.575,-3.2275095232409,-2.65492133578431));
#44348=CARTESIAN_POINT('Ctrl Pts',(-89.575,-3.24255591559887,-2.63982476295436));
#44349=CARTESIAN_POINT('Ctrl Pts',(-89.575,-3.25748199328786,-2.62461929378221));
#44350=CARTESIAN_POINT('Ctrl Pts',(-89.575,-3.3480487337272,-2.53235729378015));
#44351=CARTESIAN_POINT('Ctrl Pts',(-89.575,-3.43425145592165,-2.43602714319471));
#44352=CARTESIAN_POINT('Ctrl Pts',(-89.575,-3.51587104376023,-2.33600610480426));
#44353=CARTESIAN_POINT('Ctrl Pts',(-89.575,-3.59801431578674,-2.235343315608));
#44354=CARTESIAN_POINT('Ctrl Pts',(-89.575,-3.6755160971797,-2.1309416141852));
#44355=CARTESIAN_POINT('Ctrl Pts',(-89.575,-3.74812577356222,-2.02314026876673));
#44356=CARTESIAN_POINT('Ctrl Pts',(-89.575,-3.7758648375512,-1.98195693663194));
#44357=CARTESIAN_POINT('Ctrl Pts',(-89.575,-3.80288958155743,-1.94027700948081));
#44358=CARTESIAN_POINT('Ctrl Pts',(-89.575,-3.8291846840685,-1.89811791855068));
#44359=CARTESIAN_POINT('Ctrl Pts',(-89.575,-3.84379722111461,-1.87468955283935));
#44360=CARTESIAN_POINT('Ctrl Pts',(-89.575,-3.85818441792707,-1.85111319949648));
#44361=CARTESIAN_POINT('Ctrl Pts',(-89.575,-3.87234353149911,-1.82739175299238));
#44362=CARTESIAN_POINT('Ctrl Pts',(-89.575,-3.88684146846591,-1.80310265929821));
#44363=CARTESIAN_POINT('Ctrl Pts',(-89.575,-3.90110312921264,-1.77865622603159));
#44364=CARTESIAN_POINT('Ctrl Pts',(-89.575,-3.91510906401187,-1.75408492413592));
#44365=CARTESIAN_POINT('Ctrl Pts',(-89.575,-3.9483574032939,-1.69575572342643));
#44366=CARTESIAN_POINT('Ctrl Pts',(-89.575,-3.98018043165855,-1.63669813276525));
#44367=CARTESIAN_POINT('Ctrl Pts',(-89.575,-4.01055012113675,-1.57696270795028));
#44368=CARTESIAN_POINT('Ctrl Pts',(-89.575,-4.06930739859425,-1.46139053746715));
#44369=CARTESIAN_POINT('Ctrl Pts',(-89.575,-4.1226270049118,-1.34328346094576));
#44370=CARTESIAN_POINT('Ctrl Pts',(-89.575,-4.17052221117986,-1.22307026261548));
#44371=CARTESIAN_POINT('Ctrl Pts',(-89.575,-4.21917412213225,-1.10095779508101));
#44372=CARTESIAN_POINT('Ctrl Pts',(-89.575,-4.26222923077464,-0.976671519362465));
#44373=CARTESIAN_POINT('Ctrl Pts',(-89.575,-4.29966099444105,-0.850625465759895));
#44374=CARTESIAN_POINT('Ctrl Pts',(-89.575,-4.33321105482267,-0.73765048689121));
#44375=CARTESIAN_POINT('Ctrl Pts',(-89.575,-4.36224318317356,-0.623260954448138));
#44376=CARTESIAN_POINT('Ctrl Pts',(-89.575,-4.38670787296779,-0.507737782983998));
#44377=CARTESIAN_POINT('Ctrl Pts',(-89.575,-4.40505639031346,-0.421095404385893));
#44378=CARTESIAN_POINT('Ctrl Pts',(-89.575,-4.42083514843072,-0.333814983468863));
#44379=CARTESIAN_POINT('Ctrl Pts',(-89.575,-4.43401182496587,-0.246011295920075));
#44380=CARTESIAN_POINT('Ctrl Pts',(-89.575,-4.43670953231835,-0.228034938008987));
#44381=CARTESIAN_POINT('Ctrl Pts',(-89.575,-4.43929843122109,-0.210034488347497));
#44382=CARTESIAN_POINT('Ctrl Pts',(-89.575,-4.44177724376552,-0.192017850254865));
#44383=CARTESIAN_POINT('Ctrl Pts',(-89.575,-4.46034107829701,-0.0570911938942948));
#44384=CARTESIAN_POINT('Ctrl Pts',(-89.575,-4.47268850119797,0.0783965346303783));
#44385=CARTESIAN_POINT('Ctrl Pts',(-89.575,-4.47881882237079,0.213996674459185));
#44386=CARTESIAN_POINT('Ctrl Pts',(-89.575,-4.48386468385179,0.325609019570174));
#44387=CARTESIAN_POINT('Ctrl Pts',(-89.575,-4.48469780383174,0.437298380135437));
#44388=CARTESIAN_POINT('Ctrl Pts',(-89.575,-4.48129460116943,0.548827278861343));
#44389=CARTESIAN_POINT('Ctrl Pts',(-89.575,-4.47718033749732,0.683658889537804));
#44390=CARTESIAN_POINT('Ctrl Pts',(-89.575,-4.46687624340075,0.81825623328625));
#44391=CARTESIAN_POINT('Ctrl Pts',(-89.575,-4.45055932884642,0.95224187162625));
#44392=CARTESIAN_POINT('Ctrl Pts',(-89.575,-4.43410929567778,1.08732060771176));
#44393=CARTESIAN_POINT('Ctrl Pts',(-89.575,-4.41154788824619,1.22177838109377));
#44394=CARTESIAN_POINT('Ctrl Pts',(-89.575,-4.38300371631061,1.3552312292716));
#44395=CARTESIAN_POINT('Ctrl Pts',(-89.575,-4.37317942089486,1.40116285438693));
#44396=CARTESIAN_POINT('Ctrl Pts',(-89.575,-4.36264596032573,1.44697540796571));
#44397=CARTESIAN_POINT('Ctrl Pts',(-89.575,-4.35140716440663,1.49265305345994));
#44398=CARTESIAN_POINT('Ctrl Pts',(-89.575,-4.34684379106549,1.51119989346264));
#44399=CARTESIAN_POINT('Ctrl Pts',(-89.575,-4.34216363098046,1.52972638380862));
#44400=CARTESIAN_POINT('Ctrl Pts',(-89.575,-4.33736846843864,1.54822544889459));
#44401=CARTESIAN_POINT('Ctrl Pts',(-89.575,-4.30255455258104,1.6825326574052));
#44402=CARTESIAN_POINT('Ctrl Pts',(-89.575,-4.26178334036351,1.81501182220626));
#44403=CARTESIAN_POINT('Ctrl Pts',(-89.575,-4.21527927082535,1.94527034803996));
#44404=CARTESIAN_POINT('Ctrl Pts',(-89.575,-4.16622998832337,2.08265804970475));
#44405=CARTESIAN_POINT('Ctrl Pts',(-89.575,-4.11080349897274,2.21757625221622));
#44406=CARTESIAN_POINT('Ctrl Pts',(-89.575,-4.04920152128966,2.34956945526825));
#44407=CARTESIAN_POINT('Ctrl Pts',(-89.575,-3.98759954360659,2.48156265832028));
#44408=CARTESIAN_POINT('Ctrl Pts',(-89.575,-3.91982188875961,2.61063186325139));
#44409=CARTESIAN_POINT('Ctrl Pts',(-89.575,-3.84600984132568,2.73631219024261));
#44410=CARTESIAN_POINT('Ctrl Pts',(-89.575,-3.79539462233335,2.82249510339621));
#44411=CARTESIAN_POINT('Ctrl Pts',(-89.575,-3.74194059919316,2.90708427153108));
#44412=CARTESIAN_POINT('Ctrl Pts',(-89.575,-3.685757800253,2.98998307575975));
#44413=CARTESIAN_POINT('Ctrl Pts',(-89.575,-3.66117782571668,3.0262513026098));
#44414=CARTESIAN_POINT('Ctrl Pts',(-89.575,-3.63607538756102,3.06219590136944));
#44415=CARTESIAN_POINT('Ctrl Pts',(-89.575,-3.61045898680098,3.09780836070636));
#44416=CARTESIAN_POINT('Ctrl Pts',(-89.575,-3.59444414953696,3.12007252444251));
#44417=CARTESIAN_POINT('Ctrl Pts',(-89.575,-3.57822842220398,3.14220686647649));
#44418=CARTESIAN_POINT('Ctrl Pts',(-89.575,-3.561813801149,3.16420924915912));
#44419=CARTESIAN_POINT('Ctrl Pts',(-89.575,-3.55121738546721,3.17841282974219));
#44420=CARTESIAN_POINT('Ctrl Pts',(-89.575,-3.54054059736235,3.19255799856896));
#44421=CARTESIAN_POINT('Ctrl Pts',(-89.575,-3.52978895491108,3.20663801030847));
#44422=CARTESIAN_POINT('Ctrl Pts',(-89.575,-3.44442130591044,3.31843279008742));
#44423=CARTESIAN_POINT('Ctrl Pts',(-89.575,-3.35424955362964,3.42624081848301));
#44424=CARTESIAN_POINT('Ctrl Pts',(-89.575,-3.25965520939464,3.52983805565444));
#44425=CARTESIAN_POINT('Ctrl Pts',(-89.575,-3.16306466624511,3.63562147736009));
#44426=CARTESIAN_POINT('Ctrl Pts',(-89.575,-3.061862594744,3.73701515673525));
#44427=CARTESIAN_POINT('Ctrl Pts',(-89.575,-2.95640427239074,3.83376236101877));
#44428=CARTESIAN_POINT('Ctrl Pts',(-89.575,-2.85057033496809,3.9308541536386));
#44429=CARTESIAN_POINT('Ctrl Pts',(-89.575,-2.74044929333694,4.02326694680084));
#44430=CARTESIAN_POINT('Ctrl Pts',(-89.575,-2.62635571134329,4.11071350969491));
#44431=CARTESIAN_POINT('Ctrl Pts',(-89.575,-2.51324470319011,4.19740698285653));
#44432=CARTESIAN_POINT('Ctrl Pts',(-89.575,-2.39622873242727,4.27921996512691));
#44433=CARTESIAN_POINT('Ctrl Pts',(-89.575,-2.27557844519584,4.35583648142124));
#44434=CARTESIAN_POINT('Ctrl Pts',(-89.575,-2.2401621729428,4.37832686633806));
#44435=CARTESIAN_POINT('Ctrl Pts',(-89.575,-2.20443252938109,4.40036920957963));
#44436=CARTESIAN_POINT('Ctrl Pts',(-89.575,-2.16839587231077,4.42195480991672));
#44437=CARTESIAN_POINT('Ctrl Pts',(-89.575,-2.36246668965802,-3.31495875354372));
#44438=CARTESIAN_POINT('Ctrl Pts',(-89.541895102924,-1.90253119087213,-3.64205446939111));
#44439=CARTESIAN_POINT('Ctrl Pts',(-89.4692795060981,-0.743215608995184,
-4.14925109584965));
#44440=CARTESIAN_POINT('Ctrl Pts',(-89.357153209522,1.22652580399161,-4.06036256423134));
#44441=CARTESIAN_POINT('Ctrl Pts',(-89.2386211102719,3.0126043279509,-2.98581045744857));
#44442=CARTESIAN_POINT('Ctrl Pts',(-89.1200890110218,4.07114973607406,-1.19021168789138));
#44443=CARTESIAN_POINT('Ctrl Pts',(-89.0015569117718,4.14653236502477,0.892824265437017));
#44444=CARTESIAN_POINT('Ctrl Pts',(-88.8830248125217,3.22054554208703,2.76024400176603));
#44445=CARTESIAN_POINT('Ctrl Pts',(-88.7644927132716,1.51681193095975,3.96107892847728));
#44446=CARTESIAN_POINT('Ctrl Pts',(-88.6459606140215,-0.553225051728948,
4.20533047603355));
#44447=CARTESIAN_POINT('Ctrl Pts',(-88.5274285147713,-2.48966060894145,
3.43401418720049));
#44448=CARTESIAN_POINT('Ctrl Pts',(-88.4128374204063,-3.78046138336312,
1.88661678745238));
#44449=CARTESIAN_POINT('Ctrl Pts',(-88.3377570257912,-4.07029801574691,
0.60629401811437));
#44450=CARTESIAN_POINT('Ctrl Pts',(-88.3021873309261,-4.07075680315937,
-6.4153765865849E-5));
#44451=CARTESIAN_POINT('Origin',(-89.575,-4.52129938221115E-16,0.));
#44452=CARTESIAN_POINT('',(-89.575,-4.925,-6.03138548580071E-16));
#44453=CARTESIAN_POINT('Origin',(-89.575,0.,0.));
#44454=CARTESIAN_POINT('Origin',(-89.575,0.,0.));
#44455=CARTESIAN_POINT('',(-89.575,2.3623075609234,-3.3148866100674));
#44456=CARTESIAN_POINT('Ctrl Pts',(-89.575,2.168571653936,4.4220722318262));
#44457=CARTESIAN_POINT('Ctrl Pts',(-89.575,2.2821250990704,4.35420104629545));
#44458=CARTESIAN_POINT('Ctrl Pts',(-89.575,2.39275344608793,4.28182199486674));
#44459=CARTESIAN_POINT('Ctrl Pts',(-89.575,2.50014797438266,4.20502572098651));
#44460=CARTESIAN_POINT('Ctrl Pts',(-89.575,2.61779725504862,4.12089642200546));
#44461=CARTESIAN_POINT('Ctrl Pts',(-89.575,2.73156660582321,4.03146595669976));
#44462=CARTESIAN_POINT('Ctrl Pts',(-89.575,2.84115665380361,3.93705927886078));
#44463=CARTESIAN_POINT('Ctrl Pts',(-89.575,2.90277481127167,3.88397813099817));
#44464=CARTESIAN_POINT('Ctrl Pts',(-89.575,2.96307101504279,3.82932321285263));
#44465=CARTESIAN_POINT('Ctrl Pts',(-89.575,3.02198593446763,3.77314840125018));
#44466=CARTESIAN_POINT('Ctrl Pts',(-89.575,3.06760205276204,3.72965386919888));
#44467=CARTESIAN_POINT('Ctrl Pts',(-89.575,3.11239001077279,3.68524810911733));
#44468=CARTESIAN_POINT('Ctrl Pts',(-89.575,3.15632026306078,3.63995524989996));
#44469=CARTESIAN_POINT('Ctrl Pts',(-89.575,3.17039174259067,3.62544730814836));
#44470=CARTESIAN_POINT('Ctrl Pts',(-89.575,3.18437396240699,3.61084957134963));
#44471=CARTESIAN_POINT('Ctrl Pts',(-89.575,3.19825970699225,3.59616964172652));
#44472=CARTESIAN_POINT('Ctrl Pts',(-89.575,3.29600568509946,3.49283315366522));
#44473=CARTESIAN_POINT('Ctrl Pts',(-89.575,3.38906451000149,3.38533402227797));
#44474=CARTESIAN_POINT('Ctrl Pts',(-89.575,3.47715297643748,3.27398824380113));
#44475=CARTESIAN_POINT('Ctrl Pts',(-89.575,3.56454504164893,3.16352273194281));
#44476=CARTESIAN_POINT('Ctrl Pts',(-89.575,3.64704539656432,3.04927047926725));
#44477=CARTESIAN_POINT('Ctrl Pts',(-89.575,3.72433174854956,2.93151774737872));
#44478=CARTESIAN_POINT('Ctrl Pts',(-89.575,3.78010696130726,2.84653917735723));
#44479=CARTESIAN_POINT('Ctrl Pts',(-89.575,3.83316575613913,2.75973704453675));
#44480=CARTESIAN_POINT('Ctrl Pts',(-89.575,3.88337035803795,2.67121456473261));
#44481=CARTESIAN_POINT('Ctrl Pts',(-89.575,3.89316127494673,2.65395088348545));
#44482=CARTESIAN_POINT('Ctrl Pts',(-89.575,3.90284479422599,2.6366195765463));
#44483=CARTESIAN_POINT('Ctrl Pts',(-89.575,3.91241586666383,2.61922861666568));
#44484=CARTESIAN_POINT('Ctrl Pts',(-89.575,3.95192210597965,2.5474444537688));
#44485=CARTESIAN_POINT('Ctrl Pts',(-89.575,3.9894735885843,2.47471694815245));
#44486=CARTESIAN_POINT('Ctrl Pts',(-89.575,4.02501789616192,2.40110681671847));
#44487=CARTESIAN_POINT('Ctrl Pts',(-89.575,4.08529830421341,2.27626970321235));
#44488=CARTESIAN_POINT('Ctrl Pts',(-89.575,4.13980858439682,2.1488947134306));
#44489=CARTESIAN_POINT('Ctrl Pts',(-89.575,4.18848418123897,2.01939883110378));
#44490=CARTESIAN_POINT('Ctrl Pts',(-89.575,4.23727899932862,1.88958577422464));
#44491=CARTESIAN_POINT('Ctrl Pts',(-89.575,4.28021061669979,1.75764059664755));
#44492=CARTESIAN_POINT('Ctrl Pts',(-89.575,4.31716264794545,1.62397443606211));
#44493=CARTESIAN_POINT('Ctrl Pts',(-89.575,4.34940277263216,1.50735260125635));
#44494=CARTESIAN_POINT('Ctrl Pts',(-89.575,4.37709030380136,1.38942023503649));
#44495=CARTESIAN_POINT('Ctrl Pts',(-89.575,4.40011523782483,1.2704522302738));
#44496=CARTESIAN_POINT('Ctrl Pts',(-89.575,4.41738393834243,1.18122622670178));
#44497=CARTESIAN_POINT('Ctrl Pts',(-89.575,4.43202930683058,1.09141767980199));
#44498=CARTESIAN_POINT('Ctrl Pts',(-89.575,4.44399344956095,1.00114538980556));
#44499=CARTESIAN_POINT('Ctrl Pts',(-89.575,4.44662217637848,0.98131102348768));
#44500=CARTESIAN_POINT('Ctrl Pts',(-89.575,4.4491214272835,0.961454282731452));
#44501=CARTESIAN_POINT('Ctrl Pts',(-89.575,4.45149052360382,0.941576451469683));
#44502=CARTESIAN_POINT('Ctrl Pts',(-89.575,4.45339217003573,0.925620744405863));
#44503=CARTESIAN_POINT('Ctrl Pts',(-89.575,4.45520977888628,0.909652643593547));
#44504=CARTESIAN_POINT('Ctrl Pts',(-89.575,4.45694206893395,0.893682614227721));
#44505=CARTESIAN_POINT('Ctrl Pts',(-89.575,4.47150613737446,0.759416068626175));
#44506=CARTESIAN_POINT('Ctrl Pts',(-89.575,4.48006670618292,0.624824366933115));
#44507=CARTESIAN_POINT('Ctrl Pts',(-89.575,4.48254040861087,0.490290079290064));
#44508=CARTESIAN_POINT('Ctrl Pts',(-89.575,4.48441082620459,0.388565920505318));
#44509=CARTESIAN_POINT('Ctrl Pts',(-89.575,4.48280022621022,0.286874382300006));
#44510=CARTESIAN_POINT('Ctrl Pts',(-89.575,4.47765283391769,0.185382629909725));
#44511=CARTESIAN_POINT('Ctrl Pts',(-89.575,4.4708173232612,0.0506060448773163));
#44512=CARTESIAN_POINT('Ctrl Pts',(-89.575,4.45774630659774,-0.0838193207669723));
#44513=CARTESIAN_POINT('Ctrl Pts',(-89.575,4.43853463850383,-0.217474622726431));
#44514=CARTESIAN_POINT('Ctrl Pts',(-89.575,4.41948336180413,-0.350014084035258));
#44515=CARTESIAN_POINT('Ctrl Pts',(-89.575,4.3943931624653,-0.481797008446402));
#44516=CARTESIAN_POINT('Ctrl Pts',(-89.575,4.3633124492345,-0.612389322273228));
#44517=CARTESIAN_POINT('Ctrl Pts',(-89.575,4.35249258102604,-0.657851329986865));
#44518=CARTESIAN_POINT('Ctrl Pts',(-89.575,4.34094636247025,-0.703168770078569));
#44519=CARTESIAN_POINT('Ctrl Pts',(-89.575,4.32867469288774,-0.748322346754215));
#44520=CARTESIAN_POINT('Ctrl Pts',(-89.575,4.32188014371106,-0.773322872979495));
#44521=CARTESIAN_POINT('Ctrl Pts',(-89.575,4.31486140087328,-0.798278987057204));
#44522=CARTESIAN_POINT('Ctrl Pts',(-89.575,4.30762822556628,-0.823155012688862));
#44523=CARTESIAN_POINT('Ctrl Pts',(-89.575,4.27082651666219,-0.949721868202683));
#44524=CARTESIAN_POINT('Ctrl Pts',(-89.575,4.2284455418425,-1.07434621957789));
#44525=CARTESIAN_POINT('Ctrl Pts',(-89.575,4.18060902078101,-1.19664913006994));
#44526=CARTESIAN_POINT('Ctrl Pts',(-89.575,4.13330059472136,-1.31760186805133));
#44527=CARTESIAN_POINT('Ctrl Pts',(-89.575,4.08065599662557,-1.43628480391947));
#44528=CARTESIAN_POINT('Ctrl Pts',(-89.575,4.02275110722225,-1.5523066966709));
#44529=CARTESIAN_POINT('Ctrl Pts',(-89.575,3.9669831666924,-1.66404686372408));
#44530=CARTESIAN_POINT('Ctrl Pts',(-89.575,3.90633553434453,-1.77331917779089));
#44531=CARTESIAN_POINT('Ctrl Pts',(-89.575,3.84084200108773,-1.87974354780758));
#44532=CARTESIAN_POINT('Ctrl Pts',(-89.575,3.795406360387,-1.95357464528281));
#44533=CARTESIAN_POINT('Ctrl Pts',(-89.575,3.74763766691163,-2.02603439909253));
#44534=CARTESIAN_POINT('Ctrl Pts',(-89.575,3.69760992698782,-2.09702185867333));
#44535=CARTESIAN_POINT('Ctrl Pts',(-89.575,3.67228386786391,-2.13295857300696));
#44536=CARTESIAN_POINT('Ctrl Pts',(-89.575,3.64637878219349,-2.16851783129296));
#44537=CARTESIAN_POINT('Ctrl Pts',(-89.575,3.61990383706715,-2.20368564459669));
#44538=CARTESIAN_POINT('Ctrl Pts',(-89.575,3.6053546481366,-2.22301196076424));
#44539=CARTESIAN_POINT('Ctrl Pts',(-89.575,3.59063335678628,-2.24222004951615));
#44540=CARTESIAN_POINT('Ctrl Pts',(-89.575,3.57574145307651,-2.26130750712511));
#44541=CARTESIAN_POINT('Ctrl Pts',(-89.575,3.56574983489207,-2.27411410272612));
#44542=CARTESIAN_POINT('Ctrl Pts',(-89.575,3.55568331247211,-2.28686390445547));
#44543=CARTESIAN_POINT('Ctrl Pts',(-89.575,3.54554784644704,-2.29954960063716));
#44544=CARTESIAN_POINT('Ctrl Pts',(-89.575,3.46370593992855,-2.40198411706263));
#44545=CARTESIAN_POINT('Ctrl Pts',(-89.575,3.37727065960685,-2.50037261434585));
#44546=CARTESIAN_POINT('Ctrl Pts',(-89.575,3.2865623996527,-2.59443436453125));
#44547=CARTESIAN_POINT('Ctrl Pts',(-89.575,3.1982374123592,-2.68602473231175));
#44548=CARTESIAN_POINT('Ctrl Pts',(-89.575,3.1058601936877,-2.7735130490358));
#44549=CARTESIAN_POINT('Ctrl Pts',(-89.575,3.00969504058764,-2.85659863268242));
#44550=CARTESIAN_POINT('Ctrl Pts',(-89.575,2.90963765176844,-2.94304706311907));
#44551=CARTESIAN_POINT('Ctrl Pts',(-89.575,2.80547890527683,-3.02473006120895));
#44552=CARTESIAN_POINT('Ctrl Pts',(-89.575,2.69749236355891,-3.10125338927706));
#44553=CARTESIAN_POINT('Ctrl Pts',(-89.575,2.59715794701766,-3.17235413341945));
#44554=CARTESIAN_POINT('Ctrl Pts',(-89.575,2.4935182722296,-3.23900035352837));
#44555=CARTESIAN_POINT('Ctrl Pts',(-89.575,2.3867824989408,-3.30082548293148));
#44556=CARTESIAN_POINT('Ctrl Pts',(-89.575,2.37864216657838,-3.30554065092234));
#44557=CARTESIAN_POINT('Ctrl Pts',(-89.575,2.37048382328845,-3.31022775171822));
#44558=CARTESIAN_POINT('Ctrl Pts',(-89.575,2.36230756092335,-3.31488661006744));
#44559=CARTESIAN_POINT('Origin',(-89.575,0.,0.));
#44560=CARTESIAN_POINT('Origin',(-92.3478126690739,0.,0.));
#44561=CARTESIAN_POINT('Ctrl Pts',(-89.575,2.36230756092335,-3.31488661006744));
#44562=CARTESIAN_POINT('Ctrl Pts',(-89.53548930025,2.91092803106123,-2.9239199082961));
#44563=CARTESIAN_POINT('Ctrl Pts',(-89.4564679007499,3.80977362498712,-1.86473730182378));
#44564=CARTESIAN_POINT('Ctrl Pts',(-89.3379358014998,4.23793920928767,0.175536844418832));
#44565=CARTESIAN_POINT('Ctrl Pts',(-89.2194037022498,3.6426422996848,2.17296520226056));
#44566=CARTESIAN_POINT('Ctrl Pts',(-89.1008716029996,2.16767467238955,3.64585259348834));
#44567=CARTESIAN_POINT('Ctrl Pts',(-88.9823395037495,0.169217900166083,
4.23817423904527));
#44568=CARTESIAN_POINT('Ctrl Pts',(-88.8638074044995,-1.87010146406577,
3.80705007020246));
#44569=CARTESIAN_POINT('Ctrl Pts',(-88.7452753052494,-3.45780118263798,
2.45651375596413));
#44570=CARTESIAN_POINT('Ctrl Pts',(-88.6566103934409,-4.02080610100348,
1.00253375424179));
#44571=CARTESIAN_POINT('Ctrl Pts',(-88.6074561813824,-4.07063751740027,
0.164530271781952));
#44572=CARTESIAN_POINT('Ctrl Pts',(-88.5978126690739,-4.07047297420895,
0.000103779743357239));
#44573=CARTESIAN_POINT('Ctrl Pts',(-90.0683458050225,2.85821514250023,-4.01076441581681));
#44574=CARTESIAN_POINT('Ctrl Pts',(-90.0288351052725,3.52200480358096,-3.5377240015621));
#44575=CARTESIAN_POINT('Ctrl Pts',(-89.9498137057724,4.60954062229736,-2.25619241161589));
#44576=CARTESIAN_POINT('Ctrl Pts',(-89.8312816065224,5.12758889712364,0.212386428881554));
#44577=CARTESIAN_POINT('Ctrl Pts',(-89.7127495072722,4.40732424172653,2.62912507582186));
#44578=CARTESIAN_POINT('Ctrl Pts',(-89.5942174080223,2.62272393109418,4.41120845668343));
#44579=CARTESIAN_POINT('Ctrl Pts',(-89.4756853087721,0.204740979810431,
5.1278732655197));
#44580=CARTESIAN_POINT('Ctrl Pts',(-89.357153209522,-2.26268264599522,4.60624532508225));
#44581=CARTESIAN_POINT('Ctrl Pts',(-89.2386211102719,-4.18368034012819,
2.9721975796889));
#44582=CARTESIAN_POINT('Ctrl Pts',(-89.1200890110219,-5.09433739022707,
0.620393721358178));
#44583=CARTESIAN_POINT('Ctrl Pts',(-89.0015569117718,-4.77473548481351,
-1.88124040813632));
#44584=CARTESIAN_POINT('Ctrl Pts',(-88.8830248125217,-3.30205642110157,
-3.9285595414724));
#44585=CARTESIAN_POINT('Ctrl Pts',(-88.7644927132715,-1.03194581520415,
-5.02715134367899));
#44586=CARTESIAN_POINT('Ctrl Pts',(-88.6459606140217,1.4873750729016,-4.91170792667414));
#44587=CARTESIAN_POINT('Ctrl Pts',(-88.5274285147712,3.6475016047403,-3.61010981787875));
#44588=CARTESIAN_POINT('Ctrl Pts',(-88.4088964155215,4.92677306135157,-1.43668632685003));
#44589=CARTESIAN_POINT('Ctrl Pts',(-88.2903643162711,5.01625117196016,1.08369027345755));
#44590=CARTESIAN_POINT('Ctrl Pts',(-88.1718322170212,3.89432738802994,3.34236064934112));
#44591=CARTESIAN_POINT('Ctrl Pts',(-88.053300117771,1.83194120826945,4.7938660642741));
#44592=CARTESIAN_POINT('Ctrl Pts',(-87.934768018521,-0.672850460394772,
5.08767459077047));
#44593=CARTESIAN_POINT('Ctrl Pts',(-87.8162359192709,-3.01515179619869,
4.15283278082187));
#44594=CARTESIAN_POINT('Ctrl Pts',(-87.6977038200208,-4.62930765380767,
2.21510070074297));
#44595=CARTESIAN_POINT('Ctrl Pts',(-87.5791717207707,-5.12550671786203,
-0.257568149694912));
#44596=CARTESIAN_POINT('Ctrl Pts',(-87.4606396215207,-4.38391916567946,
-2.66803545976375));
#44597=CARTESIAN_POINT('Ctrl Pts',(-87.3421075222705,-2.58363502634467,
-4.43418431252969));
#44598=CARTESIAN_POINT('Ctrl Pts',(-87.2235754230205,-0.159414750969839,
-5.12949777300655));
#44599=CARTESIAN_POINT('Ctrl Pts',(-87.1050433237703,2.30330346343951,-4.58606079569274));
#44600=CARTESIAN_POINT('Ctrl Pts',(-86.9865112245203,4.20978434230453,-2.93511094468713));
#44601=CARTESIAN_POINT('Ctrl Pts',(-86.8679791252702,5.09962140372923,-0.57534511816609));
#44602=CARTESIAN_POINT('Ctrl Pts',(-86.7494470260202,4.7579230348759,1.92336394386835));
#44603=CARTESIAN_POINT('Ctrl Pts',(-86.6309149267699,3.26720784141955,3.95758934041028));
#44604=CARTESIAN_POINT('Ctrl Pts',(-86.51238282752,0.98747677869704,5.03607486817927));
#44605=CARTESIAN_POINT('Ctrl Pts',(-86.3938507282698,-1.5307254455619,4.89837116567092));
#44606=CARTESIAN_POINT('Ctrl Pts',(-86.2753186290198,-3.6792644201411,3.57773305223478));
#44607=CARTESIAN_POINT('Ctrl Pts',(-86.1567865297696,-4.93927773133401,
1.39308864007884));
#44608=CARTESIAN_POINT('Ctrl Pts',(-86.0382544305197,-5.0064778815977,-1.12798035773757));
#44609=CARTESIAN_POINT('Ctrl Pts',(-85.9197223312695,-3.86463633955352,
-3.37664721719212));
#44610=CARTESIAN_POINT('Ctrl Pts',(-85.8011902320194,-1.78950265668055,
-4.80986909469498));
#44611=CARTESIAN_POINT('Ctrl Pts',(-85.6826581327694,0.717787798196774,
-5.08152940984589));
#44612=CARTESIAN_POINT('Ctrl Pts',(-85.5641260335192,3.05173575665768,-4.12602342915134));
#44613=CARTESIAN_POINT('Ctrl Pts',(-85.4455939342692,4.6487033766519,-2.17410151149252));
#44614=CARTESIAN_POINT('Ctrl Pts',(-85.3270618350191,5.12303022393767,0.302856056551541));
#44615=CARTESIAN_POINT('Ctrl Pts',(-85.2085297357689,4.36016851707821,2.70667526109965));
#44616=CARTESIAN_POINT('Ctrl Pts',(-85.089997636519,2.54434589691626,4.45684467120116));
#44617=CARTESIAN_POINT('Ctrl Pts',(-84.9714655372688,0.114075287214313,
5.13070631543219));
#44618=CARTESIAN_POINT('Ctrl Pts',(-84.8529334380187,-2.3437439867514,4.5655256642511));
#44619=CARTESIAN_POINT('Ctrl Pts',(-84.7344013387686,-4.23555972228263,
2.89779128050072));
#44620=CARTESIAN_POINT('Ctrl Pts',(-84.6158692395186,-5.1045070030619,0.530253450776926));
#44621=CARTESIAN_POINT('Ctrl Pts',(-84.4973371402685,-4.74073900349125,
-1.96533818136869));
#44622=CARTESIAN_POINT('Ctrl Pts',(-84.3788050410184,-3.23210404492749,
-3.98630956012352));
#44623=CARTESIAN_POINT('Ctrl Pts',(-84.2602729417683,-0.942930624672344,
-5.0446052673548));
#44624=CARTESIAN_POINT('Ctrl Pts',(-84.1417408425183,1.57395626304328,-4.88465169161484));
#44625=CARTESIAN_POINT('Ctrl Pts',(-84.0232087432681,3.71073985481043,-3.54507689568087));
#44626=CARTESIAN_POINT('Ctrl Pts',(-83.9046766440181,4.95139660853339,-1.34938211466315));
#44627=CARTESIAN_POINT('Ctrl Pts',(-83.786144544768,4.996313547471,1.17218232443875));
#44628=CARTESIAN_POINT('Ctrl Pts',(-83.6676124455178,3.83464343467326,3.41067005077977));
#44629=CARTESIAN_POINT('Ctrl Pts',(-83.5490803462678,1.74692433148727,4.82549643523095));
#44630=CARTESIAN_POINT('Ctrl Pts',(-83.4305482470177,-0.762669071361281,
5.07498732549725));
#44631=CARTESIAN_POINT('Ctrl Pts',(-83.3120161477676,-3.08808135396581,
4.09889180360466));
#44632=CARTESIAN_POINT('Ctrl Pts',(-83.1934840485174,-4.66773600126614,
2.13293250921188));
#44633=CARTESIAN_POINT('Ctrl Pts',(-83.0749519492676,-5.12015358337118,
-0.348120308313184));
#44634=CARTESIAN_POINT('Ctrl Pts',(-82.9564198500172,-4.3360773069755,-2.7451036509212));
#44635=CARTESIAN_POINT('Ctrl Pts',(-82.8378877507673,-2.50485803520711,
-4.47915691730343));
#44636=CARTESIAN_POINT('Ctrl Pts',(-82.7193556515171,-0.0687269133315581,
-5.13151411161976));
#44637=CARTESIAN_POINT('Ctrl Pts',(-82.6008235522671,2.38400144627611,-4.5446339314099));
#44638=CARTESIAN_POINT('Ctrl Pts',(-82.482291453017,4.2610042736359,-2.86024527731897));
#44639=CARTESIAN_POINT('Ctrl Pts',(-82.3637593537669,5.10899390254251,-0.48512036666401));
#44640=CARTESIAN_POINT('Ctrl Pts',(-82.2452272545168,4.72318468523324,2.0071589113837));
#44641=CARTESIAN_POINT('Ctrl Pts',(-82.1266951552668,3.19674779714024,4.01471841949691));
#44642=CARTESIAN_POINT('Ctrl Pts',(-82.0081630560165,0.898310820773131,
5.05274164544861));
#44643=CARTESIAN_POINT('Ctrl Pts',(-81.8896309567667,-1.61706414286808,
4.87055069003692));
#44644=CARTESIAN_POINT('Ctrl Pts',(-81.7710988575164,-3.74192545317829,
3.51214384233125));
#44645=CARTESIAN_POINT('Ctrl Pts',(-81.6525667582665,-4.96312874493817,
1.30557019249725));
#44646=CARTESIAN_POINT('Ctrl Pts',(-81.5340346590162,-4.98575896420362,
-1.21629273500752));
#44647=CARTESIAN_POINT('Ctrl Pts',(-81.4155025597662,-3.80435101570306,
-3.444426485743));
#44648=CARTESIAN_POINT('Ctrl Pts',(-81.2969704605161,-1.70420955854852,
-4.84074686870948));
#44649=CARTESIAN_POINT('Ctrl Pts',(-81.178438361266,0.80749077441535,-5.06804884700245));
#44650=CARTESIAN_POINT('Ctrl Pts',(-81.059906262016,3.12418574921904,-4.07144002421078));
#44651=CARTESIAN_POINT('Ctrl Pts',(-80.9413741627658,4.68640404108277,-2.09159690908447));
#44652=CARTESIAN_POINT('Ctrl Pts',(-80.8228420635158,5.11687702083888,0.393357369297109));
#44653=CARTESIAN_POINT('Ctrl Pts',(-80.7043099642657,4.31164741707871,2.78331762778997));
#44654=CARTESIAN_POINT('Ctrl Pts',(-80.5857778650156,2.46517452550958,4.50111930803315));
#44655=CARTESIAN_POINT('Ctrl Pts',(-80.4672457657655,0.0233731713667585,
5.13192109849988));
#44656=CARTESIAN_POINT('Ctrl Pts',(-80.3487136665154,-2.42407269760731,
4.52338722895587));
#44657=CARTESIAN_POINT('Ctrl Pts',(-80.2301815672654,-4.28611600895748,
2.82247586776921));
#44658=CARTESIAN_POINT('Ctrl Pts',(-80.1116494680152,-5.11308175170773,
0.439949391053537));
#44659=CARTESIAN_POINT('Ctrl Pts',(-79.9931173687653,-4.70526145123102,
-2.04882286740397));
#44660=CARTESIAN_POINT('Ctrl Pts',(-79.874585269515,-3.16114185962938,-4.04281369958593));
#44661=CARTESIAN_POINT('Ctrl Pts',(-79.7560531702651,-0.853620852164372,
-5.0604833669543));
#44662=CARTESIAN_POINT('Ctrl Pts',(-79.6375210710149,1.6600457180465,-4.85606926231917));
#44663=CARTESIAN_POINT('Ctrl Pts',(-79.5189889717648,3.77281877930689,-3.47893646452364));
#44664=CARTESIAN_POINT('Ctrl Pts',(-79.4004568725147,4.97447322440563,-1.26165629557262));
#44665=CARTESIAN_POINT('Ctrl Pts',(-79.2819247732647,4.97481495573534,1.26030814400383));
#44666=CARTESIAN_POINT('Ctrl Pts',(-79.1633926740146,3.77376144961482,3.47791388563469));
#44667=CARTESIAN_POINT('Ctrl Pts',(-79.0448605747645,1.66136167237367,4.85561920359439));
#44668=CARTESIAN_POINT('Ctrl Pts',(-78.9263284755144,-0.852249402763529,
5.0607145170417));
#44669=CARTESIAN_POINT('Ctrl Pts',(-78.8077963762643,-3.16004612982402,
4.04367023367986));
#44670=CARTESIAN_POINT('Ctrl Pts',(-78.6892642770142,-4.70470602303032,
2.05009794270264));
#44671=CARTESIAN_POINT('Ctrl Pts',(-78.5707321777641,-5.11320082239203,
-0.438563712145908));
#44672=CARTESIAN_POINT('Ctrl Pts',(-78.452200078514,-4.28688069486741,-2.82131419484211));
#44673=CARTESIAN_POINT('Ctrl Pts',(-78.333667979264,-2.42529858960037,-4.522730152271));
#44674=CARTESIAN_POINT('Ctrl Pts',(-78.2151358800138,0.0219826423251478,
-5.13192719533143));
#44675=CARTESIAN_POINT('Ctrl Pts',(-78.0966037807639,2.46395411522516,-4.50178731500325));
#44676=CARTESIAN_POINT('Ctrl Pts',(-77.9780716815136,4.31089396507947,-2.78448580336584));
#44677=CARTESIAN_POINT('Ctrl Pts',(-77.8595395822637,5.11676822082183,-0.394744452022419));
#44678=CARTESIAN_POINT('Ctrl Pts',(-77.7410074830134,4.68697475041556,2.0903276005335));
#44679=CARTESIAN_POINT('Ctrl Pts',(-77.6224753837635,3.12528085889329,4.07059158394664));
#44680=CARTESIAN_POINT('Ctrl Pts',(-77.5039432845133,0.808880632638544,
5.06783309384885));
#44681=CARTESIAN_POINT('Ctrl Pts',(-77.3854111852633,-1.70293070733278,
4.84120196057697));
#44682=CARTESIAN_POINT('Ctrl Pts',(-77.2668790860132,-3.80335080595143,
3.44547060595366));
#44683=CARTESIAN_POINT('Ctrl Pts',(-77.1483469867631,-4.98556332054866,
1.21761716875768));
#44684=CARTESIAN_POINT('Ctrl Pts',(-77.0298148875131,-4.96321218223962,
-1.30417137017964));
#44685=CARTESIAN_POINT('Ctrl Pts',(-76.9112827882629,-3.74342128882646,
-3.51123787294802));
#44686=CARTESIAN_POINT('Ctrl Pts',(-76.7927506890129,-1.61728813305841,
-4.86989428648745));
#44687=CARTESIAN_POINT('Ctrl Pts',(-76.6742185897627,0.894735013697703,
-5.05342397500786));
#44688=CARTESIAN_POINT('Ctrl Pts',(-76.5556864905126,3.20009374497158,-4.01469986050394));
#44689=CARTESIAN_POINT('Ctrl Pts',(-76.4371543912626,4.71382864353052,-2.01022859740298));
#44690=CARTESIAN_POINT('Ctrl Pts',(-76.2791115922624,5.26141933163145,1.31995330641));
#44691=CARTESIAN_POINT('Ctrl Pts',(-76.0815580935124,2.70784920336926,5.1429724685161));
#44692=CARTESIAN_POINT('Ctrl Pts',(-75.8444938950121,-2.83874316080605,
5.07524718716688));
#44693=CARTESIAN_POINT('Ctrl Pts',(-75.607429696512,-5.79701303111296,0.394996271206378));
#44694=CARTESIAN_POINT('Ctrl Pts',(-75.3703654980119,-3.49950474856753,
-4.6408040950746));
#44695=CARTESIAN_POINT('Ctrl Pts',(-75.1333012995116,1.9774213757655,-5.46581264071833));
#44696=CARTESIAN_POINT('Ctrl Pts',(-74.8962371010115,5.65797660303749,-1.32902724184649));
#44697=CARTESIAN_POINT('Ctrl Pts',(-74.6591729025112,4.20372685543133,4.01387644762517));
#44698=CARTESIAN_POINT('Ctrl Pts',(-74.4221087040113,-1.06631748846821,
5.71331599545101));
#44699=CARTESIAN_POINT('Ctrl Pts',(-74.1850445055108,-5.3686615009571,2.22772906990762));
#44700=CARTESIAN_POINT('Ctrl Pts',(-73.9479803070108,-4.79746384525761,
-3.28145345655763));
#44701=CARTESIAN_POINT('Ctrl Pts',(-73.7109161085106,0.126862191859868,
-5.809069471218));
#44702=CARTESIAN_POINT('Ctrl Pts',(-73.4738519100104,4.93873592962991,-3.0700951387947));
#44703=CARTESIAN_POINT('Ctrl Pts',(-73.2367877115102,5.26253689341103,2.46745183652891));
#44704=CARTESIAN_POINT('Ctrl Pts',(-73.0392342127601,1.56152334963781,5.19484888547336));
#44705=CARTESIAN_POINT('Ctrl Pts',(-72.88119141376,-1.79039388404845,4.80163401711829));
#44706=CARTESIAN_POINT('Ctrl Pts',(-72.7626593145099,-3.86263253914205,
3.38208291058891));
#44707=CARTESIAN_POINT('Ctrl Pts',(-72.6441272152597,-5.00671250687666,
1.12715326793019));
#44708=CARTESIAN_POINT('Ctrl Pts',(-72.5255951160098,-4.93938671358823,
-1.39066536611891));
#44709=CARTESIAN_POINT('Ctrl Pts',(-72.4070630167596,-3.68036712056178,
-3.57727440993159));
#44710=CARTESIAN_POINT('Ctrl Pts',(-72.2885309175095,-1.53198670632987,
-4.89768872636437));
#44711=CARTESIAN_POINT('Ctrl Pts',(-72.1699988182594,0.986079090438097,
-5.03647507888746));
#44712=CARTESIAN_POINT('Ctrl Pts',(-72.0514667190094,3.26615150869236,-3.9584086918721));
#44713=CARTESIAN_POINT('Ctrl Pts',(-71.9329346197593,4.75739352015727,-1.92468602931411));
#44714=CARTESIAN_POINT('Ctrl Pts',(-71.8144025205092,5.09978115928234,0.573979330983468));
#44715=CARTESIAN_POINT('Ctrl Pts',(-71.6958704212591,4.21057761945873,2.93396189490852));
#44716=CARTESIAN_POINT('Ctrl Pts',(-71.577338322009,2.30454721399284,4.58544042890789));
#44717=CARTESIAN_POINT('Ctrl Pts',(-71.458806222759,-0.158025119865097,
5.12953879695887));
#44718=CARTESIAN_POINT('Ctrl Pts',(-71.3402741235088,-2.5824330026147,4.43488531467397));
#44719=CARTESIAN_POINT('Ctrl Pts',(-71.2217420242588,-4.38319607615567,
2.66922293363304));
#44720=CARTESIAN_POINT('Ctrl Pts',(-71.1032099250087,-5.12543666721089,
0.258957419581195));
#44721=CARTESIAN_POINT('Ctrl Pts',(-70.9846778257586,-4.6299078162659,-2.21384617619623));
#44722=CARTESIAN_POINT('Ctrl Pts',(-70.8661457265085,-3.01627710741838,
-4.15201544906907));
#44723=CARTESIAN_POINT('Ctrl Pts',(-70.7476136272584,-0.674229226436862,
-5.08749208647444));
#44724=CARTESIAN_POINT('Ctrl Pts',(-70.6290815280083,1.83064198501573,-4.79436234138692));
#44725=CARTESIAN_POINT('Ctrl Pts',(-70.5105494287582,3.8934214476962,-3.34341590771825));
#44726=CARTESIAN_POINT('Ctrl Pts',(-70.3920173295081,5.015957304304,-1.08504967117028));
#44727=CARTESIAN_POINT('Ctrl Pts',(-70.2734852302581,4.92716222717632,1.43535112214182));
#44728=CARTESIAN_POINT('Ctrl Pts',(-70.1549531310079,3.64847983031567,3.60912113987176));
#44729=CARTESIAN_POINT('Ctrl Pts',(-70.0364210317579,1.48870610788084,4.91130477429458));
#44730=CARTESIAN_POINT('Ctrl Pts',(-69.9178889325078,-1.03058338436781,
5.02743059189797));
#44731=CARTESIAN_POINT('Ctrl Pts',(-69.7993568332578,-3.30099166563435,
3.92945473177838));
#44732=CARTESIAN_POINT('Ctrl Pts',(-69.6808247340076,-4.77422543725906,
1.88253338368117));
#44733=CARTESIAN_POINT('Ctrl Pts',(-69.5622926347576,-5.09450542813289,
-0.619011235112431));
#44734=CARTESIAN_POINT('Ctrl Pts',(-69.4437605355075,-4.18448547359292,
-2.97106744917556));
#44735=CARTESIAN_POINT('Ctrl Pts',(-69.3252284362574,-2.26393126363252,
-4.60562435506688));
#44736=CARTESIAN_POINT('Ctrl Pts',(-69.2066963370073,0.203352074273813,
-5.12794387646976));
#44737=CARTESIAN_POINT('Ctrl Pts',(-69.0881642377571,2.62152680891723,-4.41188821894996));
#44738=CARTESIAN_POINT('Ctrl Pts',(-68.9696321385072,4.40661471397025,-2.63038157478856));
#44739=CARTESIAN_POINT('Ctrl Pts',(-68.851100039257,5.12752515991275,-0.213649715257704));
#44740=CARTESIAN_POINT('Ctrl Pts',(-68.732567940007,4.61016154506751,2.25467758110799));
#44741=CARTESIAN_POINT('Ctrl Pts',(-68.6140358407568,2.97946483496381,4.17851047187654));
#44742=CARTESIAN_POINT('Ctrl Pts',(-68.4955037415068,0.62924088606478,5.09325204301474));
#44743=CARTESIAN_POINT('Ctrl Pts',(-68.3769716422567,-1.8729418817384,4.7779963555866));
#44744=CARTESIAN_POINT('Ctrl Pts',(-68.2584395430066,-3.92281768327795,
3.30887622768375));
#44745=CARTESIAN_POINT('Ctrl Pts',(-68.1399074437565,-5.02535081346788,
1.04067750429541));
#44746=CARTESIAN_POINT('Ctrl Pts',(-68.0213753445064,-4.91428452393621,
-1.47884011447142));
#44747=CARTESIAN_POINT('Ctrl Pts',(-67.9028432452563,-3.6164408196592,-3.64122455559547));
#44748=CARTESIAN_POINT('Ctrl Pts',(-67.7843111460063,-1.44524306646015,
-4.92426978802113));
#44749=CARTESIAN_POINT('Ctrl Pts',(-67.6657790467562,1.07497432972823,-5.01812620973149));
#44750=CARTESIAN_POINT('Ctrl Pts',(-67.5472469475061,3.33559030281248,-3.9001279207421));
#44751=CARTESIAN_POINT('Ctrl Pts',(-67.428714848256,4.79067635247856,-1.8402664351043));
#44752=CARTESIAN_POINT('Ctrl Pts',(-67.3101827490059,5.0888357999539,0.664011044694645));
#44753=CARTESIAN_POINT('Ctrl Pts',(-67.1916506497558,4.15806449152427,3.00793287004445));
#44754=CARTESIAN_POINT('Ctrl Pts',(-67.0731185505057,2.22313947494855,4.625452555296));
#44755=CARTESIAN_POINT('Ctrl Pts',(-66.9545864512557,-0.248663637685085,
5.12594643569966));
#44756=CARTESIAN_POINT('Ctrl Pts',(-66.8360543520055,-2.66041561008952,
4.3885475100494));
#44757=CARTESIAN_POINT('Ctrl Pts',(-66.7175222527555,-4.42968928387048,
2.5913342730593));
#44758=CARTESIAN_POINT('Ctrl Pts',(-66.5989901535053,-5.12921309460808,
0.168325566892939));
#44759=CARTESIAN_POINT('Ctrl Pts',(-66.4804580542554,-4.59005521598732,
-2.29533299992755));
#44760=CARTESIAN_POINT('Ctrl Pts',(-66.3619259550051,-2.9424198293519,-4.20467906197435));
#44761=CARTESIAN_POINT('Ctrl Pts',(-66.2433938557551,-0.584203404690506,
-5.09861420861756));
#44762=CARTESIAN_POINT('Ctrl Pts',(-66.1248617565051,1.91509549147353,-4.76125715803154));
#44763=CARTESIAN_POINT('Ctrl Pts',(-66.006329657255,3.95190751588822,-3.2740781072288));
#44764=CARTESIAN_POINT('Ctrl Pts',(-65.8877975580048,5.0343518063684,-0.996224049139549));
#44765=CARTESIAN_POINT('Ctrl Pts',(-65.7692654587548,4.90102297818209,1.52221359660857));
#44766=CARTESIAN_POINT('Ctrl Pts',(-65.6507333595047,3.5841193383779,3.67304356557805));
#44767=CARTESIAN_POINT('Ctrl Pts',(-65.5322012602546,1.40166714072751,4.93685017931207));
#44768=CARTESIAN_POINT('Ctrl Pts',(-65.4136691610046,-1.11928131156664,
5.00842987491554));
#44769=CARTESIAN_POINT('Ctrl Pts',(-65.2951370617544,-3.36992840567857,
3.87049648068172));
#44770=CARTESIAN_POINT('Ctrl Pts',(-65.1766049625044,-4.80675308033382,
1.79785574812611));
#44771=CARTESIAN_POINT('Ctrl Pts',(-65.0580728632543,-5.08276869596689,
-0.708958990117128));
#44772=CARTESIAN_POINT('Ctrl Pts',(-64.9395407640041,-4.13131873377937,
-3.04456334903587));
#44773=CARTESIAN_POINT('Ctrl Pts',(-64.8210086647541,-2.1821740425865,-4.64491947338492));
#44774=CARTESIAN_POINT('Ctrl Pts',(-64.702476565504,0.293955778622967,-5.12354862049567));
#44775=CARTESIAN_POINT('Ctrl Pts',(-64.583944466254,2.69909661307265,-4.36486402304454));
#44776=CARTESIAN_POINT('Ctrl Pts',(-64.4654123670038,4.45241786218732,-2.55208456890519));
#44777=CARTESIAN_POINT('Ctrl Pts',(-64.3468802677538,5.13050039972244,-0.122988271053509));
#44778=CARTESIAN_POINT('Ctrl Pts',(-64.2283481685036,4.56959036955502,2.33580913621787));
#44779=CARTESIAN_POINT('Ctrl Pts',(-64.1098160692536,2.90514499893036,4.23051923545547));
#44780=CARTESIAN_POINT('Ctrl Pts',(-63.9912839700034,0.539120292697892,
5.10357813463948));
#44781=CARTESIAN_POINT('Ctrl Pts',(-63.8727518707535,-1.95709951804845,
4.74414607098299));
#44782=CARTESIAN_POINT('Ctrl Pts',(-63.7542197715032,-3.9806886752142,3.23902425699317));
#44783=CARTESIAN_POINT('Ctrl Pts',(-63.6356876722533,-5.04295957905816,
0.951692781497464));
#44784=CARTESIAN_POINT('Ctrl Pts',(-63.5171555730031,-4.88737862618744,
-1.56546818257512));
#44785=CARTESIAN_POINT('Ctrl Pts',(-63.398623473753,-3.55151791079645,-3.70457568361896));
#44786=CARTESIAN_POINT('Ctrl Pts',(-63.280091374503,-1.35798173439636,-4.94904496599238));
#44787=CARTESIAN_POINT('Ctrl Pts',(-63.1615592752529,1.16350086923399,-4.9983423445839));
#44788=CARTESIAN_POINT('Ctrl Pts',(-63.0430271760028,3.40400329214487,-3.84056272614266));
#44789=CARTESIAN_POINT('Ctrl Pts',(-62.9244950767527,4.82245436512648,-1.75530463528116));
#44790=CARTESIAN_POINT('Ctrl Pts',(-62.8059629775026,5.07630459005136,0.753851560584832));
#44791=CARTESIAN_POINT('Ctrl Pts',(-62.6874308782526,4.10425028940277,3.08095602505127));
#44792=CARTESIAN_POINT('Ctrl Pts',(-62.5688987790024,2.14103816625032,4.66402358881631));
#44793=CARTESIAN_POINT('Ctrl Pts',(-62.4503666797523,-0.339224959437705,
5.12075061814821));
#44794=CARTESIAN_POINT('Ctrl Pts',(-62.3318345805022,-2.73756679658748,
4.34083960778975));
#44795=CARTESIAN_POINT('Ctrl Pts',(-62.2133024812522,-4.47479867366276,
2.51263552801999));
#44796=CARTESIAN_POINT('Ctrl Pts',(-62.0947703820021,-5.13138697468224,
0.0776413689181762));
#44797=CARTESIAN_POINT('Ctrl Pts',(-61.976238282752,-4.54876860427843,-2.37610282849254));
#44798=CARTESIAN_POINT('Ctrl Pts',(-61.8577061835019,-2.86764325503598,
-4.25602897401029));
#44799=CARTESIAN_POINT('Ctrl Pts',(-61.7391740842518,-0.493995071621616,
-5.10814343336204));
#44800=CARTESIAN_POINT('Ctrl Pts',(-61.6206419850017,1.99895068105866,-4.7266644309417));
#44801=CARTESIAN_POINT('Ctrl Pts',(-61.5021098857517,4.00915891238501,-3.2037174149467));
#44802=CARTESIAN_POINT('Ctrl Pts',(-61.3835777865016,5.0511734609159,-0.907087179582999));
#44803=CARTESIAN_POINT('Ctrl Pts',(-61.2650456872514,4.87335253023417,1.60860049385013));
#44804=CARTESIAN_POINT('Ctrl Pts',(-61.1465135880015,3.51863909026266,3.73581844686004));
#44805=CARTESIAN_POINT('Ctrl Pts',(-61.0279814887513,1.31419024565512,4.96085319548998));
#44806=CARTESIAN_POINT('Ctrl Pts',(-60.9094493895012,-1.2076295207279,4.98786440678609));
#44807=CARTESIAN_POINT('Ctrl Pts',(-60.7909172902511,-3.43781235735713,
3.81032899489403));
#44808=CARTESIAN_POINT('Ctrl Pts',(-60.6723851910011,-4.83777886638368,
1.71261642068914));
#44809=CARTESIAN_POINT('Ctrl Pts',(-60.5538530917509,-5.06944421686892,
-0.798685250787317));
#44810=CARTESIAN_POINT('Ctrl Pts',(-60.4353209925009,-4.07686080989476,
-3.11710805327251));
#44811=CARTESIAN_POINT('Ctrl Pts',(-60.3167888932508,-2.09973599091779,
-4.68276341400958));
#44812=CARTESIAN_POINT('Ctrl Pts',(-60.1982567940008,0.384469521220488,
-5.11755263795289));
#44813=CARTESIAN_POINT('Ctrl Pts',(-60.0797246947506,2.77581937568727,-4.31647615939701));
#44814=CARTESIAN_POINT('Ctrl Pts',(-59.9611925955006,4.49683758333763,-2.47299019416017));
#44815=CARTESIAN_POINT('Ctrl Pts',(-59.8426604962504,5.13185741717796,-0.032288477837873));
#44816=CARTESIAN_POINT('Ctrl Pts',(-59.7241283970004,4.52762243183336,2.41621107972979));
#44817=CARTESIAN_POINT('Ctrl Pts',(-59.6055962977503,2.82985525829162,4.28120600452079));
#44818=CARTESIAN_POINT('Ctrl Pts',(-59.4870641985002,0.448957713397435,
5.11230993433101));
#44819=CARTESIAN_POINT('Ctrl Pts',(-59.3685320992501,-2.04091141443468,
4.70881615114383));
#44820=CARTESIAN_POINT('Ctrl Pts',(-59.28951069975,-3.3712993556795,3.68162322923883));
#44821=CARTESIAN_POINT('Ctrl Pts',(-59.25,-3.87448963569914,3.04038732119116));
#44822=CARTESIAN_POINT('Ctrl Pts',(-89.9038972033484,2.69291261530793,-3.77880514723369));
#44823=CARTESIAN_POINT('Ctrl Pts',(-89.8643865035983,3.31831254607438,-3.3331226371401));
#44824=CARTESIAN_POINT('Ctrl Pts',(-89.7853651040982,4.34295162319395,-2.12570737501852));
#44825=CARTESIAN_POINT('Ctrl Pts',(-89.6668330048482,4.83103900117832,0.200103234060647));
#44826=CARTESIAN_POINT('Ctrl Pts',(-89.548300905598,4.15243026104595,2.47707178463476));
#44827=CARTESIAN_POINT('Ctrl Pts',(-89.4297688063481,2.4710408448593,4.1560898356184));
#44828=CARTESIAN_POINT('Ctrl Pts',(-89.3112367070978,0.192899953262315,
4.83130692336156));
#44829=CARTESIAN_POINT('Ctrl Pts',(-89.1927046078479,-2.13182225201874,
4.33984690678899));
#44830=CARTESIAN_POINT('Ctrl Pts',(-89.0741725085977,-3.94172062096479,
2.80030297178065));
#44831=CARTESIAN_POINT('Ctrl Pts',(-88.9556404093478,-4.7997105678955,0.584513759605153));
#44832=CARTESIAN_POINT('Ctrl Pts',(-88.8371083100975,-4.49859257640246,
-1.77244041295852));
#44833=CARTESIAN_POINT('Ctrl Pts',(-88.7185762108475,-3.11108469779655,
-3.70135452433616));
#44834=CARTESIAN_POINT('Ctrl Pts',(-88.6000441115974,-0.972264075840879,
-4.73641017121377));
#44835=CARTESIAN_POINT('Ctrl Pts',(-88.4815120123473,1.40135395616427,-4.62764332949355));
#44836=CARTESIAN_POINT('Ctrl Pts',(-88.3629799130972,3.43655134272674,-3.40132207917299));
#44837=CARTESIAN_POINT('Ctrl Pts',(-88.2444478138472,4.64183718447002,-1.35359675214318));
#44838=CARTESIAN_POINT('Ctrl Pts',(-88.1259157145971,4.72614040198114,1.02101593581497));
#44839=CARTESIAN_POINT('Ctrl Pts',(-88.0073836153469,3.66910215939564,3.14905796407129));
#44840=CARTESIAN_POINT('Ctrl Pts',(-87.8888515160969,1.72599239185885,4.51661675449933));
#44841=CARTESIAN_POINT('Ctrl Pts',(-87.7703194168468,-0.63393670618787,
4.79343310597768));
#44842=CARTESIAN_POINT('Ctrl Pts',(-87.6517873175967,-2.84077296642872,
3.91265710493609));
#44843=CARTESIAN_POINT('Ctrl Pts',(-87.5332552183467,-4.36157544465854,
2.08699216952231));
#44844=CARTESIAN_POINT('Ctrl Pts',(-87.4147231190965,-4.82907724304558,
-0.242671907128827));
#44845=CARTESIAN_POINT('Ctrl Pts',(-87.2961910198465,-4.13037879836486,
-2.5137318184529));
#44846=CARTESIAN_POINT('Ctrl Pts',(-87.1776589205964,-2.43421261483795,
-4.17773690169677));
#44847=CARTESIAN_POINT('Ctrl Pts',(-87.0591268213463,-0.15019512967007,
-4.83283747879104));
#44848=CARTESIAN_POINT('Ctrl Pts',(-86.9405947220962,2.17009379782133,-4.32082973309242));
#44849=CARTESIAN_POINT('Ctrl Pts',(-86.8220626228462,3.96631491959732,-2.76536121187931));
#44850=CARTESIAN_POINT('Ctrl Pts',(-86.703530523596,4.80468898481305,-0.542070505409861));
#44851=CARTESIAN_POINT('Ctrl Pts',(-86.5849984243459,4.48275246070997,1.81212776856987));
#44852=CARTESIAN_POINT('Ctrl Pts',(-86.4664663250959,3.07825155712221,3.72870540867557));
#44853=CARTESIAN_POINT('Ctrl Pts',(-86.3479342258458,0.930366869566953,
4.74481761099761));
#44854=CARTESIAN_POINT('Ctrl Pts',(-86.2294021265957,-1.44219719559694,
4.61507788911824));
#44855=CARTESIAN_POINT('Ctrl Pts',(-86.1108700273456,-3.46647718176477,
3.37081779720027));
#44856=CARTESIAN_POINT('Ctrl Pts',(-85.9923379280955,-4.6536186571259,1.31252050180827));
#44857=CARTESIAN_POINT('Ctrl Pts',(-85.8738058288454,-4.71693234184641,
-1.062744539417));
#44858=CARTESIAN_POINT('Ctrl Pts',(-85.7552737295953,-3.6411282683421,-3.18136159640766));
#44859=CARTESIAN_POINT('Ctrl Pts',(-85.6367416303453,-1.68600823907419,
-4.53169426278861));
#44860=CARTESIAN_POINT('Ctrl Pts',(-85.5182095310951,0.676275129935608,
-4.78764332654887));
#44861=CARTESIAN_POINT('Ctrl Pts',(-85.3996774318452,2.87524112355692,-3.88739825011851));
#44862=CARTESIAN_POINT('Ctrl Pts',(-85.2811453325949,4.37984943178903,-2.04836413473647));
#44863=CARTESIAN_POINT('Ctrl Pts',(-85.162613233345,4.82674397511501,0.285340625057606));
#44864=CARTESIAN_POINT('Ctrl Pts',(-85.0440811340948,4.10800174903465,2.55013691858802));
#44865=CARTESIAN_POINT('Ctrl Pts',(-84.9255490348447,2.39719573996768,4.19908671712054));
#44866=CARTESIAN_POINT('Ctrl Pts',(-84.8070169355947,0.107477836593331,
4.83397612615729));
#44867=CARTESIAN_POINT('Ctrl Pts',(-84.6884848363446,-2.2081954766547,4.3014822341257));
#44868=CARTESIAN_POINT('Ctrl Pts',(-84.5699527370944,-3.99059960162677,
2.730199899845));
#44869=CARTESIAN_POINT('Ctrl Pts',(-84.4514206378445,-4.80929202951765,
0.499586677599988));
#44870=CARTESIAN_POINT('Ctrl Pts',(-84.3328885385942,-4.4665622536785,-1.85167446049024));
#44871=CARTESIAN_POINT('Ctrl Pts',(-84.2143564393443,-3.04517795989258,
-3.75576461805074));
#44872=CARTESIAN_POINT('Ctrl Pts',(-84.0958243400941,-0.88839700580379,
-4.75285466153723));
#44873=CARTESIAN_POINT('Ctrl Pts',(-83.9772922408441,1.48292779422635,-4.60215186958539));
#44874=CARTESIAN_POINT('Ctrl Pts',(-83.8587601415939,3.49613226050008,-3.34005028266161));
#44875=CARTESIAN_POINT('Ctrl Pts',(-83.740228042344,4.66503664900773,-1.27134170742255));
#44876=CARTESIAN_POINT('Ctrl Pts',(-83.6216959430937,4.70735585364263,1.10439012164805));
#44877=CARTESIAN_POINT('Ctrl Pts',(-83.5031638438438,3.61286997850212,3.21341674733537));
#44878=CARTESIAN_POINT('Ctrl Pts',(-83.3846317445935,1.64589239637687,4.54641780890914));
#44879=CARTESIAN_POINT('Ctrl Pts',(-83.2660996453436,-0.718560731498145,
4.78147959827983));
#44880=CARTESIAN_POINT('Ctrl Pts',(-83.1475675460934,-2.9094847030715,3.86183575986994));
#44881=CARTESIAN_POINT('Ctrl Pts',(-83.0290354468434,-4.39778132017769,
2.00957610791767));
#44882=CARTESIAN_POINT('Ctrl Pts',(-82.9105033475932,-4.82403370269499,
-0.327987055964406));
#44883=CARTESIAN_POINT('Ctrl Pts',(-82.7919712483432,-4.08530383429795,
-2.58634283402023));
#44884=CARTESIAN_POINT('Ctrl Pts',(-82.673439149093,-2.35999162633504,-4.22010855277988));
#44885=CARTESIAN_POINT('Ctrl Pts',(-82.5549070498431,-0.0647521486992605,
-4.83473720411525));
#44886=CARTESIAN_POINT('Ctrl Pts',(-82.4363749505929,2.24612467904481,-4.28179875750872));
#44887=CARTESIAN_POINT('Ctrl Pts',(-82.3178428513428,4.01457258823341,-2.6948253389454));
#44888=CARTESIAN_POINT('Ctrl Pts',(-82.1993107520927,4.81351943284894,-0.457063828368594));
#44889=CARTESIAN_POINT('Ctrl Pts',(-82.0807786528427,4.45002317501111,1.89107652290472));
#44890=CARTESIAN_POINT('Ctrl Pts',(-81.9622465535925,3.01186651168125,3.7825304743558));
#44891=CARTESIAN_POINT('Ctrl Pts',(-81.8437144543425,0.846357751646158,
4.76052047888104));
#44892=CARTESIAN_POINT('Ctrl Pts',(-81.7251823550923,-1.52354256519767,
4.58886638786185));
#44893=CARTESIAN_POINT('Ctrl Pts',(-81.6066502558424,-3.52551426537858,
3.30902188542618));
#44894=CARTESIAN_POINT('Ctrl Pts',(-81.4881181565922,-4.67609026693143,
1.23006361182116));
#44895=CARTESIAN_POINT('Ctrl Pts',(-81.3695860573422,-4.69741168603698,
-1.14594944282047));
#44896=CARTESIAN_POINT('Ctrl Pts',(-81.251053958092,-3.58432949672381,-3.24522090658449));
#44897=CARTESIAN_POINT('Ctrl Pts',(-81.132521858842,-1.60564799727745,-4.5607862460826));
#44898=CARTESIAN_POINT('Ctrl Pts',(-81.0139897595918,0.760790208138697,
-4.77494240099476));
#44899=CARTESIAN_POINT('Ctrl Pts',(-80.8954576603418,2.94350103025408,-3.83597163160921));
#44900=CARTESIAN_POINT('Ctrl Pts',(-80.7769255610917,4.41536970923133,-1.97063111830187));
#44901=CARTESIAN_POINT('Ctrl Pts',(-80.6583934618416,4.82094663746786,0.370607868649802));
#44902=CARTESIAN_POINT('Ctrl Pts',(-80.5398613625915,4.06228682703513,2.62234673689682));
#44903=CARTESIAN_POINT('Ctrl Pts',(-80.4213292633414,2.32260317985487,4.24080076666502));
#44904=CARTESIAN_POINT('Ctrl Pts',(-80.3027971640914,0.0220214031817654,
4.83512065324315));
#44905=CARTESIAN_POINT('Ctrl Pts',(-80.1842650648412,-2.28387844243946,
4.26178084065517));
#44906=CARTESIAN_POINT('Ctrl Pts',(-80.0657329655913,-4.03823200695045,
2.65924029220176));
#44907=CARTESIAN_POINT('Ctrl Pts',(-79.947200866341,-4.81737086461236,0.41450527906331));
#44908=CARTESIAN_POINT('Ctrl Pts',(-79.8286687670911,-4.43313651653883,
-1.93033087821979));
#44909=CARTESIAN_POINT('Ctrl Pts',(-79.7101366678409,-2.97831981434657,
-3.80900088697707));
#44910=CARTESIAN_POINT('Ctrl Pts',(-79.5916045685908,-0.804252390697374,
-4.76781446427664));
#44911=CARTESIAN_POINT('Ctrl Pts',(-79.4730724693408,1.56403833624816,-4.57522248163207));
#44912=CARTESIAN_POINT('Ctrl Pts',(-79.3545403700905,3.55462090134293,-3.27773502906268));
#44913=CARTESIAN_POINT('Ctrl Pts',(-79.2360082708407,4.68677864773865,-1.18868943908753));
#44914=CARTESIAN_POINT('Ctrl Pts',(-79.1174761715904,4.68710061531734,1.18741925675842));
#44915=CARTESIAN_POINT('Ctrl Pts',(-78.9989440723404,3.55550905308716,3.27677159018463));
#44916=CARTESIAN_POINT('Ctrl Pts',(-78.8804119730904,1.56527818343671,4.57479845168433));
#44917=CARTESIAN_POINT('Ctrl Pts',(-78.7618798738402,-0.802960257947215,
4.76803224598841));
#44918=CARTESIAN_POINT('Ctrl Pts',(-78.6433477745902,-2.97728745517533,
3.80980788412455));
#44919=CARTESIAN_POINT('Ctrl Pts',(-78.5248156753401,-4.43261321107233,
1.93153221058489));
#44920=CARTESIAN_POINT('Ctrl Pts',(-78.4062835760899,-4.81748304894133,
-0.413199739758205));
#44921=CARTESIAN_POINT('Ctrl Pts',(-78.2877514768399,-4.03895246787828,
-2.65814580367513));
#44922=CARTESIAN_POINT('Ctrl Pts',(-78.1692193775897,-2.28503343597506,
-4.26116176546116));
#44923=CARTESIAN_POINT('Ctrl Pts',(-78.0506872783397,0.020711294246199,
-4.83512639746945));
#44924=CARTESIAN_POINT('Ctrl Pts',(-77.9321551790896,2.32145335099778,-4.24143014000017));
#44925=CARTESIAN_POINT('Ctrl Pts',(-77.8136230798395,4.06157695031397,-2.62344735199687));
#44926=CARTESIAN_POINT('Ctrl Pts',(-77.6950909805894,4.82084412981051,-0.371914730583939));
#44927=CARTESIAN_POINT('Ctrl Pts',(-77.5765588813394,4.41590741205818,1.96943521916934));
#44928=CARTESIAN_POINT('Ctrl Pts',(-77.4580267820892,2.94453280515897,3.8351722601915));
#44929=CARTESIAN_POINT('Ctrl Pts',(-77.3394946828392,0.762099685052078,
4.77473912574775));
#44930=CARTESIAN_POINT('Ctrl Pts',(-77.220962583589,-1.60444310737234,4.5612150180854));
#44931=CARTESIAN_POINT('Ctrl Pts',(-77.102430484339,-3.58338713328238,3.24620464095956));
#44932=CARTESIAN_POINT('Ctrl Pts',(-76.9838983850889,-4.69722735727226,
1.14719727903154));
#44933=CARTESIAN_POINT('Ctrl Pts',(-76.8653662858388,-4.67616887870502,
-1.22874568924441));
#44934=CARTESIAN_POINT('Ctrl Pts',(-76.7468341865888,-3.52692359059955,
-3.30816831203879));
#44935=CARTESIAN_POINT('Ctrl Pts',(-76.6283020873386,-1.52375360109911,
-4.58824794687301));
#44936=CARTESIAN_POINT('Ctrl Pts',(-76.5097699880886,0.842988748438532,
-4.76116334647018));
#44937=CARTESIAN_POINT('Ctrl Pts',(-76.3912378888385,3.01501894936562,-3.78251298870692));
#44938=CARTESIAN_POINT('Ctrl Pts',(-76.2727057895883,4.44120823230232,-1.89396867615214));
#44939=CARTESIAN_POINT('Ctrl Pts',(-76.1146629905883,4.95712946233337,1.24361489014421));
#44940=CARTESIAN_POINT('Ctrl Pts',(-75.9171094918381,2.5512429668698,4.84553287634373));
#44941=CARTESIAN_POINT('Ctrl Pts',(-75.680045293338,-2.67456677969549,4.78172443106303));
#44942=CARTESIAN_POINT('Ctrl Pts',(-75.4429810948378,-5.46174753973659,
0.372151986012044));
#44943=CARTESIAN_POINT('Ctrl Pts',(-75.2059168963376,-3.2971137632781,-4.37240699867927));
#44944=CARTESIAN_POINT('Ctrl Pts',(-74.9688526978375,1.86305883325509,-5.14970185212314));
#44945=CARTESIAN_POINT('Ctrl Pts',(-74.7317884993372,5.33075216937959,-1.25216404197114));
#44946=CARTESIAN_POINT('Ctrl Pts',(-74.4947243008371,3.96060776250636,3.7817371972363));
#44947=CARTESIAN_POINT('Ctrl Pts',(-74.257660102337,-1.00464789158865,5.38289105344675));
#44948=CARTESIAN_POINT('Ctrl Pts',(-74.0205959038367,-5.05816936880361,
2.09889018731971));
#44949=CARTESIAN_POINT('Ctrl Pts',(-73.7835317053366,-4.52000646077214,
-3.09167328879938));
#44950=CARTESIAN_POINT('Ctrl Pts',(-73.5464675068364,0.119525221102254,
-5.47310670552218));
#44951=CARTESIAN_POINT('Ctrl Pts',(-73.3094033083362,4.65310819007873,-2.8925387058945));
#44952=CARTESIAN_POINT('Ctrl Pts',(-73.0723391098361,4.95818239084454,2.3247487844603));
#44953=CARTESIAN_POINT('Ctrl Pts',(-72.8747856110859,1.47121392816465,4.89440906329828));
#44954=CARTESIAN_POINT('Ctrl Pts',(-72.7167428120858,-1.6868479230387,4.52393545416548));
#44955=CARTESIAN_POINT('Ctrl Pts',(-72.5982107128358,-3.63924035608306,
3.18648292093757));
#44956=CARTESIAN_POINT('Ctrl Pts',(-72.4796786135856,-4.71715339776492,
1.06196528366983));
#44957=CARTESIAN_POINT('Ctrl Pts',(-72.3611465143356,-4.65372133648087,
-1.31023737590922));
#44958=CARTESIAN_POINT('Ctrl Pts',(-72.2426144150854,-3.4675161084115,-3.37038568009834));
#44959=CARTESIAN_POINT('Ctrl Pts',(-72.1240823158354,-1.44338551238339,
-4.61443491812896));
#44960=CARTESIAN_POINT('Ctrl Pts',(-72.0055502165852,0.929050015461517,
-4.7451946758479));
#44961=CARTESIAN_POINT('Ctrl Pts',(-71.8870181173353,3.07725631653146,-3.72947737361796));
#44962=CARTESIAN_POINT('Ctrl Pts',(-71.768486018085,4.48225357004057,-1.81337339228878));
#44963=CARTESIAN_POINT('Ctrl Pts',(-71.6499539188351,4.80483950103485,0.540783707408174));
#44964=CARTESIAN_POINT('Ctrl Pts',(-71.5314218195849,3.96706231821827,2.76427861645173));
#44965=CARTESIAN_POINT('Ctrl Pts',(-71.4128897203349,2.17126561708203,4.32024524471151));
#44966=CARTESIAN_POINT('Ctrl Pts',(-71.2943576210847,-0.148885866739932,
4.83287613015675));
#44967=CARTESIAN_POINT('Ctrl Pts',(-71.1758255218347,-2.43308010916401,
4.17839736195729));
#44968=CARTESIAN_POINT('Ctrl Pts',(-71.0572934225846,-4.12969752813031,
2.5148506157454));
#44969=CARTESIAN_POINT('Ctrl Pts',(-70.9387613233345,-4.82901124371636,
0.243980829731282));
#44970=CARTESIAN_POINT('Ctrl Pts',(-70.8202292240844,-4.36214089721349,
-2.08581019937327));
#44971=CARTESIAN_POINT('Ctrl Pts',(-70.7016971248343,-2.84183319619745,
-3.91188704289449));
#44972=CARTESIAN_POINT('Ctrl Pts',(-70.5831650255843,-0.63523573242734,
-4.79326115666786));
#44973=CARTESIAN_POINT('Ctrl Pts',(-70.4646329263341,1.72476830811586,-4.51708432983258));
#44974=CARTESIAN_POINT('Ctrl Pts',(-70.3461008270841,3.66824861337767,-3.15005219244613));
#44975=CARTESIAN_POINT('Ctrl Pts',(-70.227568727834,4.72586352991972,-1.02229671387652));
#44976=CARTESIAN_POINT('Ctrl Pts',(-70.1090366285839,4.64220384320865,1.35233876790359));
#44977=CARTESIAN_POINT('Ctrl Pts',(-69.9905045293338,3.4374729934287,3.40039058054721));
#44978=CARTESIAN_POINT('Ctrl Pts',(-69.8719724300837,1.40260801182774,4.62726349310103));
#44979=CARTESIAN_POINT('Ctrl Pts',(-69.7534403308337,-0.970980440073939,
4.73667326934116));
#44980=CARTESIAN_POINT('Ctrl Pts',(-69.6349082315835,-3.11008152158803,
3.7021979420454));
#44981=CARTESIAN_POINT('Ctrl Pts',(-69.5163761323335,-4.49811202702977,
1.77365861032375));
#44982=CARTESIAN_POINT('Ctrl Pts',(-69.3978440330833,-4.79986888746694,
-0.583211228316955));
#44983=CARTESIAN_POINT('Ctrl Pts',(-69.2793119338334,-3.94247919019627,
-2.79923820143815));
#44984=CARTESIAN_POINT('Ctrl Pts',(-69.1607798345832,-2.13299865687961,
-4.33926185006489));
#44985=CARTESIAN_POINT('Ctrl Pts',(-69.0422477353331,0.191591373937665,
-4.83137345058526));
#44986=CARTESIAN_POINT('Ctrl Pts',(-68.923715636083,2.4699129572611,-4.15673028439206));
#44987=CARTESIAN_POINT('Ctrl Pts',(-68.805183536833,4.15176176824522,-2.47825561501481));
#44988=CARTESIAN_POINT('Ctrl Pts',(-68.6866514375828,4.83097895015671,-0.201293459305886));
#44989=CARTESIAN_POINT('Ctrl Pts',(-68.5681193383328,4.34353663540522,2.12428015348995));
#44990=CARTESIAN_POINT('Ctrl Pts',(-68.4495872390826,2.80714993131055,3.93684974780085));
#44991=CARTESIAN_POINT('Ctrl Pts',(-68.3310551398326,0.592849255801311,
4.79868799084851));
#44992=CARTESIAN_POINT('Ctrl Pts',(-68.2125230405825,-1.76462182502469,
4.5016648573904));
#44993=CARTESIAN_POINT('Ctrl Pts',(-68.0939909413324,-3.69594474179837,
3.11751008646168));
#44994=CARTESIAN_POINT('Ctrl Pts',(-67.9754588420824,-4.73471377318983,
0.980490774859142));
#44995=CARTESIAN_POINT('Ctrl Pts',(-67.8569267428322,-4.63007091136744,
-1.39331261005075));
#44996=CARTESIAN_POINT('Ctrl Pts',(-67.7383946435822,-3.40728693266096,
-3.43063732156799));
#44997=CARTESIAN_POINT('Ctrl Pts',(-67.6198625443321,-1.36165861973998,
-4.63947868589835));
#44998=CARTESIAN_POINT('Ctrl Pts',(-67.501330445082,1.01280407153856,-4.72790699848171));
#44999=CARTESIAN_POINT('Ctrl Pts',(-67.3827983458318,3.1426791749781,-3.67456722305856));
#45000=CARTESIAN_POINT('Ctrl Pts',(-67.2642662465818,4.51361151706789,-1.73383613603175));
#45001=CARTESIAN_POINT('Ctrl Pts',(-67.1457341473317,4.79452715758092,0.625608510840759));
#45002=CARTESIAN_POINT('Ctrl Pts',(-67.0272020480816,3.91758624394338,2.83397154094444));
#45003=CARTESIAN_POINT('Ctrl Pts',(-66.9086699488316,2.09456602781867,4.35794330260563));
#45004=CARTESIAN_POINT('Ctrl Pts',(-66.7901378495815,-0.234282380263663,
4.82949153016292));
#45005=CARTESIAN_POINT('Ctrl Pts',(-66.6716057503314,-2.50655265653141,
4.13473946623638));
#45006=CARTESIAN_POINT('Ctrl Pts',(-66.5530736510812,-4.17350183933125,
2.44146658193717));
#45007=CARTESIAN_POINT('Ctrl Pts',(-66.4345415518312,-4.83256926453413,
0.158590595866855));
#45008=CARTESIAN_POINT('Ctrl Pts',(-66.3160094525811,-4.32459313936726,
-2.16258429952568));
#45009=CARTESIAN_POINT('Ctrl Pts',(-66.197477353331,-2.77224739319749,-3.96150489896542));
#45010=CARTESIAN_POINT('Ctrl Pts',(-66.0789452540809,-0.550416480202624,
-4.80374004000411));
#45011=CARTESIAN_POINT('Ctrl Pts',(-65.9604131548309,1.80433751533385,-4.48589375758903));
#45012=CARTESIAN_POINT('Ctrl Pts',(-65.8418810555807,3.723352187812,-3.08472448674641));
#45013=CARTESIAN_POINT('Ctrl Pts',(-65.7233489563307,4.74319420105255,-0.938608248801809));
#45014=CARTESIAN_POINT('Ctrl Pts',(-65.6048168570806,4.61757633622901,1.43417762244263));
#45015=CARTESIAN_POINT('Ctrl Pts',(-65.4862847578305,3.37683473772516,3.46061610522028));
#45016=CARTESIAN_POINT('Ctrl Pts',(-65.3677526585804,1.32060287191181,4.65133150058299));
#45017=CARTESIAN_POINT('Ctrl Pts',(-65.2492205593303,-1.05454859544256,
4.71877144323261));
#45018=CARTESIAN_POINT('Ctrl Pts',(-65.1306884600802,-3.17503136184424,
3.64664949301723));
#45019=CARTESIAN_POINT('Ctrl Pts',(-65.0121563608302,-4.52875846056089,
1.69387823633091));
#45020=CARTESIAN_POINT('Ctrl Pts',(-64.8936242615801,-4.78881093957408,
-0.667956928725949));
#45021=CARTESIAN_POINT('Ctrl Pts',(-64.77509216233,-3.89238730514893,-2.86848352624393));
#45022=CARTESIAN_POINT('Ctrl Pts',(-64.6565600630799,-2.05596979761929,
-4.37628436746227));
#45023=CARTESIAN_POINT('Ctrl Pts',(-64.5380279638298,0.276955087399081,
-4.82723239063349));
#45024=CARTESIAN_POINT('Ctrl Pts',(-64.4194958645797,2.5429965754503,-4.11242569426676));
#45025=CARTESIAN_POINT('Ctrl Pts',(-64.3009637653297,4.19491592897319,-2.40448685221282));
#45026=CARTESIAN_POINT('Ctrl Pts',(-64.1824316660795,4.83378211941362,-0.115875345326565));
#45027=CARTESIAN_POINT('Ctrl Pts',(-64.0638995668295,4.30531186053404,2.2007195316901));
#45028=CARTESIAN_POINT('Ctrl Pts',(-63.9453674675794,2.73712832200404,3.98585062721882));
#45029=CARTESIAN_POINT('Ctrl Pts',(-63.8268353683293,0.507940712994964,
4.80841688143817));
#45030=CARTESIAN_POINT('Ctrl Pts',(-63.7083032690792,-1.84391227350212,
4.46977227621784));
#45031=CARTESIAN_POINT('Ctrl Pts',(-63.5897711698291,-3.75046881240742,
3.05169794717246));
#45032=CARTESIAN_POINT('Ctrl Pts',(-63.4712390705791,-4.75130415027271,
0.896652410479528));
#45033=CARTESIAN_POINT('Ctrl Pts',(-63.3527069713289,-4.60472109413483,
-1.47493061492638));
#45034=CARTESIAN_POINT('Ctrl Pts',(-63.2341748720789,-3.34611878695376,
-3.4903245890909));
#45035=CARTESIAN_POINT('Ctrl Pts',(-63.1156427728288,-1.2794439752057,-4.66282101178322));
#45036=CARTESIAN_POINT('Ctrl Pts',(-62.9971106735787,1.09621075128068,-4.70926731693943));
#45037=CARTESIAN_POINT('Ctrl Pts',(-62.8785785743286,3.20713555521509,-3.61844693260701));
#45038=CARTESIAN_POINT('Ctrl Pts',(-62.7600464750785,4.54355167443271,-1.65378803217808));
#45039=CARTESIAN_POINT('Ctrl Pts',(-62.6415143758284,4.78272067991945,0.710253174221426));
#45040=CARTESIAN_POINT('Ctrl Pts',(-62.5229822765784,3.86688434203933,2.90277146170738));
#45041=CARTESIAN_POINT('Ctrl Pts',(-62.4044501773282,2.01721298093314,4.39428361205534));
#45042=CARTESIAN_POINT('Ctrl Pts',(-62.2859180780782,-0.319606162291232,
4.82459620845565));
#45043=CARTESIAN_POINT('Ctrl Pts',(-62.1673859788281,-2.57924186747184,
4.08979071135275));
#45044=CARTESIAN_POINT('Ctrl Pts',(-62.048853879578,-4.2160023645836,2.36731931423363));
#45045=CARTESIAN_POINT('Ctrl Pts',(-61.9303217803279,-4.83461742003818,
0.0731510440626118));
#45046=CARTESIAN_POINT('Ctrl Pts',(-61.8117896810779,-4.28569430496499,
-2.2386828713388));
#45047=CARTESIAN_POINT('Ctrl Pts',(-61.6932575818277,-2.70179546069225,
-4.00988503097871));
#45048=CARTESIAN_POINT('Ctrl Pts',(-61.5747254825777,-0.465425272047941,
-4.81271814985559));
#45049=CARTESIAN_POINT('Ctrl Pts',(-61.4561933833275,1.88334300884449,-4.45330167248215));
#45050=CARTESIAN_POINT('Ctrl Pts',(-61.3376612840775,3.77729249677535,-3.01843304736144));
#45051=CARTESIAN_POINT('Ctrl Pts',(-61.2191291848274,4.75904298901387,-0.854626536946514));
#45052=CARTESIAN_POINT('Ctrl Pts',(-61.1005970855773,4.59150618593059,1.51556840437503));
#45053=CARTESIAN_POINT('Ctrl Pts',(-60.9820649863272,3.31514148602376,3.51976045275908));
#45054=CARTESIAN_POINT('Ctrl Pts',(-60.8635328870771,1.23818513127863,4.67394632201816));
#45055=CARTESIAN_POINT('Ctrl Pts',(-60.745000787827,-1.13778725842931,4.69939536207552));
#45056=CARTESIAN_POINT('Ctrl Pts',(-60.626468688577,-3.23898930088597,3.58996174439405));
#45057=CARTESIAN_POINT('Ctrl Pts',(-60.5079365893268,-4.55798989573565,
1.6135686554452));
#45058=CARTESIAN_POINT('Ctrl Pts',(-60.3894044900768,-4.7762570707901,-0.752493944743505));
#45059=CARTESIAN_POINT('Ctrl Pts',(-60.2708723908267,-3.84107891060167,
-2.93683266704434));
#45060=CARTESIAN_POINT('Ctrl Pts',(-60.1523402915766,-1.97829948301663,
-4.41193963483726));
#45061=CARTESIAN_POINT('Ctrl Pts',(-60.0338081923265,0.362234041972942,
-4.82158318082052));
#45062=CARTESIAN_POINT('Ctrl Pts',(-59.9152760930764,2.6152821400511,-4.06683630300412));
#45063=CARTESIAN_POINT('Ctrl Pts',(-59.7967439938263,4.2367666720035,-2.32996683572293));
#45064=CARTESIAN_POINT('Ctrl Pts',(-59.6782118945763,4.83506065487822,-0.030421100219405));
#45065=CARTESIAN_POINT('Ctrl Pts',(-59.5596797953262,4.26577110404982,2.27647149478029));
#45066=CARTESIAN_POINT('Ctrl Pts',(-59.4411476960761,2.66619290172915,4.03360596859099));
#45067=CARTESIAN_POINT('Ctrl Pts',(-59.322615596826,0.422992612477064,4.81664368466023));
#45068=CARTESIAN_POINT('Ctrl Pts',(-59.204083497576,-1.9228769776405,4.43648563329933));
#45069=CARTESIAN_POINT('Ctrl Pts',(-59.1250620980759,-3.17632302407693,
3.46869957107404));
#45070=CARTESIAN_POINT('Ctrl Pts',(-59.0855513983258,-3.65041170719121,
2.86454901554256));
#45071=CARTESIAN_POINT('Ctrl Pts',(-89.7394486016742,2.52761008811564,-3.54684587865056));
#45072=CARTESIAN_POINT('Ctrl Pts',(-89.6999379019242,3.11462028856781,-3.1285212727181));
#45073=CARTESIAN_POINT('Ctrl Pts',(-89.620916502424,4.07636262409054,-1.99522233842116));
#45074=CARTESIAN_POINT('Ctrl Pts',(-89.5023844031741,4.53448910523299,0.187820039239741));
#45075=CARTESIAN_POINT('Ctrl Pts',(-89.3838523039238,3.89753628036537,2.32501849344766));
#45076=CARTESIAN_POINT('Ctrl Pts',(-89.2653202046739,2.31935775862443,3.90097121455338));
#45077=CARTESIAN_POINT('Ctrl Pts',(-89.1467881054237,0.181058926714198,
4.53474058120341));
#45078=CARTESIAN_POINT('Ctrl Pts',(-89.0282560061737,-2.00096185804225,
4.07344848849573));
#45079=CARTESIAN_POINT('Ctrl Pts',(-88.9097239069235,-3.69976090180139,
2.62840836387239));
#45080=CARTESIAN_POINT('Ctrl Pts',(-88.7911918076736,-4.50508374556393,
0.548633797852129));
#45081=CARTESIAN_POINT('Ctrl Pts',(-88.6726597084233,-4.22244966799141,
-1.66364041778071));
#45082=CARTESIAN_POINT('Ctrl Pts',(-88.5541276091733,-2.92011297449154,
-3.47414950719992));
#45083=CARTESIAN_POINT('Ctrl Pts',(-88.4355955099232,-0.912582336477606,
-4.44566899874856));
#45084=CARTESIAN_POINT('Ctrl Pts',(-88.3170634106731,1.31533283942694,-4.34357873231296));
#45085=CARTESIAN_POINT('Ctrl Pts',(-88.198531311423,3.22560108071319,-3.19253434046722));
#45086=CARTESIAN_POINT('Ctrl Pts',(-88.079999212173,4.35690130758848,-1.27050717743633));
#45087=CARTESIAN_POINT('Ctrl Pts',(-87.9614671129229,4.43602963200212,0.958341598172394));
#45088=CARTESIAN_POINT('Ctrl Pts',(-87.8429350136728,3.44387693076133,2.95575527880146));
#45089=CARTESIAN_POINT('Ctrl Pts',(-87.7244029144227,1.62004357544825,4.23936744472458));
#45090=CARTESIAN_POINT('Ctrl Pts',(-87.6058708151726,-0.595022951980973,
4.4991916211849));
#45091=CARTESIAN_POINT('Ctrl Pts',(-87.4873387159225,-2.66639413665873,
3.67248142905029));
#45092=CARTESIAN_POINT('Ctrl Pts',(-87.3688066166724,-4.0938432355094,1.95888363830165));
#45093=CARTESIAN_POINT('Ctrl Pts',(-87.2502745174224,-4.53264776822913,
-0.227775664562744));
#45094=CARTESIAN_POINT('Ctrl Pts',(-87.1317424181724,-3.87683843105025,
-2.35942817714205));
#45095=CARTESIAN_POINT('Ctrl Pts',(-87.013210318922,-2.28479020333122,-3.92128949086385));
#45096=CARTESIAN_POINT('Ctrl Pts',(-86.8946782196722,-0.140975508370298,
-4.53617718457553));
#45097=CARTESIAN_POINT('Ctrl Pts',(-86.776146120422,2.03688413220314,-4.05559867049211));
#45098=CARTESIAN_POINT('Ctrl Pts',(-86.657614021172,3.72284549689011,-2.5956114790715));
#45099=CARTESIAN_POINT('Ctrl Pts',(-86.5390819219218,4.50975656589686,-0.508795892653628));
#45100=CARTESIAN_POINT('Ctrl Pts',(-86.4205498226717,4.20758188654404,1.70089159327138));
#45101=CARTESIAN_POINT('Ctrl Pts',(-86.3020177234218,2.88929527282486,3.49982147694086));
#45102=CARTESIAN_POINT('Ctrl Pts',(-86.1834856241715,0.873256960436869,
4.45356035381594));
#45103=CARTESIAN_POINT('Ctrl Pts',(-86.0649535249215,-1.35366894563198,
4.33178461256555));
#45104=CARTESIAN_POINT('Ctrl Pts',(-85.9464214256714,-3.25368994338844,
3.16390254216576));
#45105=CARTESIAN_POINT('Ctrl Pts',(-85.8278893264213,-4.36795958291779,
1.23195236353769));
#45106=CARTESIAN_POINT('Ctrl Pts',(-85.7093572271712,-4.42738680209512,
-0.997508721096433));
#45107=CARTESIAN_POINT('Ctrl Pts',(-85.5908251279211,-3.41762019713068,
-2.9860759756232));
#45108=CARTESIAN_POINT('Ctrl Pts',(-85.472293028671,-1.58251382146784,-4.25351943088223));
#45109=CARTESIAN_POINT('Ctrl Pts',(-85.3537609294211,0.63476246167444,-4.49375724325186));
#45110=CARTESIAN_POINT('Ctrl Pts',(-85.2352288301708,2.69874649045617,-3.64877307108568));
#45111=CARTESIAN_POINT('Ctrl Pts',(-85.1166967309209,4.11099548692616,-1.92262675798041));
#45112=CARTESIAN_POINT('Ctrl Pts',(-84.9981646316706,4.53045772629236,0.267825193563669));
#45113=CARTESIAN_POINT('Ctrl Pts',(-84.8796325324207,3.8558349809911,2.39359857607639));
#45114=CARTESIAN_POINT('Ctrl Pts',(-84.7611004331704,2.2500455830191,3.94132876303992));
#45115=CARTESIAN_POINT('Ctrl Pts',(-84.6425683339206,0.100880385972347,
4.53724593688237));
#45116=CARTESIAN_POINT('Ctrl Pts',(-84.5240362346703,-2.072646966558,4.0374388040003));
#45117=CARTESIAN_POINT('Ctrl Pts',(-84.4055041354203,-3.74563948097091,
2.56260851918929));
#45118=CARTESIAN_POINT('Ctrl Pts',(-84.2869720361702,-4.51407705597339,
0.46891990442305));
#45119=CARTESIAN_POINT('Ctrl Pts',(-84.1684399369201,-4.19238550386574,
-1.73801073961178));
#45120=CARTESIAN_POINT('Ctrl Pts',(-84.0499078376701,-2.85825187485767,
-3.52521967597796));
#45121=CARTESIAN_POINT('Ctrl Pts',(-83.9313757384199,-0.833863386935234,
-4.46110405571966));
#45122=CARTESIAN_POINT('Ctrl Pts',(-83.8128436391699,1.39189932540943,-4.31965204755595));
#45123=CARTESIAN_POINT('Ctrl Pts',(-83.6943115399198,3.28152466618975,-3.13502366964235));
#45124=CARTESIAN_POINT('Ctrl Pts',(-83.5757794406697,4.37867668948207,-1.19330130018193));
#45125=CARTESIAN_POINT('Ctrl Pts',(-83.4572473414196,4.41839815981427,1.03659791885736));
#45126=CARTESIAN_POINT('Ctrl Pts',(-83.3387152421695,3.39109652233098,3.01616344389097));
#45127=CARTESIAN_POINT('Ctrl Pts',(-83.2201831429194,1.54486046126646,4.26733918258733));
#45128=CARTESIAN_POINT('Ctrl Pts',(-83.1016510436694,-0.674452391635007,
4.4879718710624));
#45129=CARTESIAN_POINT('Ctrl Pts',(-82.9831189444192,-2.73088805217719,
3.62477971613523));
#45130=CARTESIAN_POINT('Ctrl Pts',(-82.8645868451691,-4.12782663908925,
1.88621970662346));
#45131=CARTESIAN_POINT('Ctrl Pts',(-82.7460547459191,-4.5279138220188,-0.307853803615623));
#45132=CARTESIAN_POINT('Ctrl Pts',(-82.627522646669,-3.8345303616204,-2.42758201711926));
#45133=CARTESIAN_POINT('Ctrl Pts',(-82.5089905474189,-2.21512521746297,
-3.96106018825632));
#45134=CARTESIAN_POINT('Ctrl Pts',(-82.3904584481687,-0.0607773840669588,
-4.53796029661075));
#45135=CARTESIAN_POINT('Ctrl Pts',(-82.2719263489188,2.10824791181349,-4.01896358360754));
#45136=CARTESIAN_POINT('Ctrl Pts',(-82.1533942496687,3.76814090283094,-2.52940540057184));
#45137=CARTESIAN_POINT('Ctrl Pts',(-82.0348621504185,4.51804496315537,-0.429007290073176));
#45138=CARTESIAN_POINT('Ctrl Pts',(-81.9163300511686,4.17686166478898,1.77499413442573));
#45139=CARTESIAN_POINT('Ctrl Pts',(-81.7977979519183,2.82698522622225,3.5503425292147));
#45140=CARTESIAN_POINT('Ctrl Pts',(-81.6792658526684,0.794404682519185,
4.46829931231348));
#45141=CARTESIAN_POINT('Ctrl Pts',(-81.5607337534181,-1.43002098752725,
4.30718208568678));
#45142=CARTESIAN_POINT('Ctrl Pts',(-81.4422016541682,-3.30910307757889,
3.10589992852112));
#45143=CARTESIAN_POINT('Ctrl Pts',(-81.323669554918,-4.38905178892469,1.15455703114506));
#45144=CARTESIAN_POINT('Ctrl Pts',(-81.205137455668,-4.40906440787034,-1.07560615063343));
#45145=CARTESIAN_POINT('Ctrl Pts',(-81.0866053564178,-3.36430797774455,
-3.04601532742597));
#45146=CARTESIAN_POINT('Ctrl Pts',(-80.9680732571678,-1.50708643600638,
-4.28082562345572));
#45147=CARTESIAN_POINT('Ctrl Pts',(-80.8495411579177,0.714089641862045,
-4.48183595498707));
#45148=CARTESIAN_POINT('Ctrl Pts',(-80.7310090586676,2.76281631128911,-3.60050323900763));
#45149=CARTESIAN_POINT('Ctrl Pts',(-80.6124769594176,4.14433537737989,-1.84966532751926));
#45150=CARTESIAN_POINT('Ctrl Pts',(-80.4939448601674,4.52501625409684,0.34785836800249));
#45151=CARTESIAN_POINT('Ctrl Pts',(-80.3754127609173,3.81292623699154,2.46137584600368));
#45152=CARTESIAN_POINT('Ctrl Pts',(-80.2568806616673,2.18003183420017,3.98048222529689));
#45153=CARTESIAN_POINT('Ctrl Pts',(-80.1383485624171,0.0206696349967715,
4.53832020798643));
#45154=CARTESIAN_POINT('Ctrl Pts',(-80.0198164631671,-2.1436841872716,4.00017445235445));
#45155=CARTESIAN_POINT('Ctrl Pts',(-79.901284363917,-3.79034800494341,2.49600471663431));
#45156=CARTESIAN_POINT('Ctrl Pts',(-79.7827522646669,-4.52165997751698,
0.38906116707308));
#45157=CARTESIAN_POINT('Ctrl Pts',(-79.6642201654169,-4.16101158184665,
-1.8118388890356));
#45158=CARTESIAN_POINT('Ctrl Pts',(-79.5456880661666,-2.79549776906375,
-3.5751880743682));
#45159=CARTESIAN_POINT('Ctrl Pts',(-79.4271559669167,-0.754883929230383,
-4.47514556159899));
#45160=CARTESIAN_POINT('Ctrl Pts',(-79.3086238676665,1.46803095444983,-4.29437570094498));
#45161=CARTESIAN_POINT('Ctrl Pts',(-79.1900917684164,3.33642302337897,-3.07653359360171));
#45162=CARTESIAN_POINT('Ctrl Pts',(-79.0715596691664,4.39908407107168,-1.11572258260244));
#45163=CARTESIAN_POINT('Ctrl Pts',(-78.9530275699163,4.39938627489934,1.11453036951301));
#45164=CARTESIAN_POINT('Ctrl Pts',(-78.8344954706662,3.3372566565595,3.07562929473458));
#45165=CARTESIAN_POINT('Ctrl Pts',(-78.7159633714162,1.46919469449974,4.29397769977425));
#45166=CARTESIAN_POINT('Ctrl Pts',(-78.5974312721659,-0.753671113130901,
4.47534997493514));
#45167=CARTESIAN_POINT('Ctrl Pts',(-78.478899172916,-2.79452878052665,3.57594553456924));
#45168=CARTESIAN_POINT('Ctrl Pts',(-78.3603670736658,-4.16052039911434,
1.81296647846714));
#45169=CARTESIAN_POINT('Ctrl Pts',(-78.2418349744158,-4.52176527549064,
-0.387835767370506));
#45170=CARTESIAN_POINT('Ctrl Pts',(-78.1233028751657,-3.79102424088914,
-2.49497741250814));
#45171=CARTESIAN_POINT('Ctrl Pts',(-78.0047707759156,-2.14476828234976,
-3.99959337865132));
#45172=CARTESIAN_POINT('Ctrl Pts',(-77.8862386766655,0.0194399461672552,
-4.53832559960748));
#45173=CARTESIAN_POINT('Ctrl Pts',(-77.7677065774155,2.17895258677039,-3.98107296499709));
#45174=CARTESIAN_POINT('Ctrl Pts',(-77.6491744781653,3.81225993554848,-2.46240890062791));
#45175=CARTESIAN_POINT('Ctrl Pts',(-77.5306423789153,4.52492003879919,-0.349085009145456));
#45176=CARTESIAN_POINT('Ctrl Pts',(-77.4121102796651,4.14484007370081,1.84854283780517));
#45177=CARTESIAN_POINT('Ctrl Pts',(-77.2935781804151,2.76378475142464,3.59975293643636));
#45178=CARTESIAN_POINT('Ctrl Pts',(-77.175046081165,0.715318737465615,4.48164515764665));
#45179=CARTESIAN_POINT('Ctrl Pts',(-77.056513981915,-1.5059555074119,4.28122807559381));
#45180=CARTESIAN_POINT('Ctrl Pts',(-76.9379818826647,-3.36342346061332,
3.04693867596547));
#45181=CARTESIAN_POINT('Ctrl Pts',(-76.8194497834148,-4.40889139399587,
1.07677738930539));
#45182=CARTESIAN_POINT('Ctrl Pts',(-76.7009176841647,-4.3891255751704,-1.15332000830917));
#45183=CARTESIAN_POINT('Ctrl Pts',(-76.5823855849146,-3.31042589237266,
-3.10509875112957));
#45184=CARTESIAN_POINT('Ctrl Pts',(-76.4638534856645,-1.43021906913979,
-4.30660160725856));
#45185=CARTESIAN_POINT('Ctrl Pts',(-76.3453213864143,0.791242483179356,
-4.46890271793249));
#45186=CARTESIAN_POINT('Ctrl Pts',(-76.2267892871643,2.82994415375967,-3.55032611690991));
#45187=CARTESIAN_POINT('Ctrl Pts',(-76.1082571879142,4.16858782107412,-1.77770875490129));
#45188=CARTESIAN_POINT('Ctrl Pts',(-75.9502143889141,4.65283959303529,1.16727647387843));
#45189=CARTESIAN_POINT('Ctrl Pts',(-75.752660890164,2.39463673037035,4.54809328417136));
#45190=CARTESIAN_POINT('Ctrl Pts',(-75.5155966916638,-2.51039039858494,
4.48820167495918));
#45191=CARTESIAN_POINT('Ctrl Pts',(-75.2785324931636,-5.12648204836021,
0.349307700817715));
#45192=CARTESIAN_POINT('Ctrl Pts',(-75.0414682946634,-3.09472277798867,
-4.10400990228395));
#45193=CARTESIAN_POINT('Ctrl Pts',(-74.8044040961632,1.74869629074469,-4.83359106352794));
#45194=CARTESIAN_POINT('Ctrl Pts',(-74.5673398976631,5.0035277357217,-1.1753008420958));
#45195=CARTESIAN_POINT('Ctrl Pts',(-74.3302756991629,3.71748866958139,3.54959794684745));
#45196=CARTESIAN_POINT('Ctrl Pts',(-74.0932115006628,-0.942978294709073,
5.05246611144249));
#45197=CARTESIAN_POINT('Ctrl Pts',(-73.8561473021625,-4.74767723665014,
1.97005130473179));
#45198=CARTESIAN_POINT('Ctrl Pts',(-73.6190831036625,-4.24254907628667,
-2.90189312104113));
#45199=CARTESIAN_POINT('Ctrl Pts',(-73.3820189051621,0.112188250344633,
-5.13714393982636));
#45200=CARTESIAN_POINT('Ctrl Pts',(-73.1449547066621,4.36748045052756,-2.7149822729943));
#45201=CARTESIAN_POINT('Ctrl Pts',(-72.9078905081619,4.65382788827805,2.1820457323917));
#45202=CARTESIAN_POINT('Ctrl Pts',(-72.7103370094117,1.3809045066915,4.5939692411232));
#45203=CARTESIAN_POINT('Ctrl Pts',(-72.5522942104116,-1.58330196202896,
4.24623689121268));
#45204=CARTESIAN_POINT('Ctrl Pts',(-72.4337621111616,-3.41584817302406,
2.99088293128623));
#45205=CARTESIAN_POINT('Ctrl Pts',(-72.3152300119113,-4.42759428865317,
0.996777299409477));
#45206=CARTESIAN_POINT('Ctrl Pts',(-72.1966979126615,-4.36805595937351,
-1.22980938569953));
#45207=CARTESIAN_POINT('Ctrl Pts',(-72.0781658134112,-3.25466509626123,
-3.16349695026509));
#45208=CARTESIAN_POINT('Ctrl Pts',(-71.9596337141612,-1.35478431843691,
-4.33118110989355));
#45209=CARTESIAN_POINT('Ctrl Pts',(-71.8411016149111,0.872020940484935,
-4.45391427280835));
#45210=CARTESIAN_POINT('Ctrl Pts',(-71.722569515661,2.88836112437056,-3.50054605536382));
#45211=CARTESIAN_POINT('Ctrl Pts',(-71.6040374164109,4.20711361992387,-1.70206075526345));
#45212=CARTESIAN_POINT('Ctrl Pts',(-71.4855053171608,4.50989784278735,0.507588083832879));
#45213=CARTESIAN_POINT('Ctrl Pts',(-71.3669732179108,3.72354701697782,2.59459533799494));
#45214=CARTESIAN_POINT('Ctrl Pts',(-71.2484411186606,2.03798402017123,4.05505006051512));
#45215=CARTESIAN_POINT('Ctrl Pts',(-71.1299090194107,-0.139746613614768,
4.53621346335462));
#45216=CARTESIAN_POINT('Ctrl Pts',(-71.0113769201604,-2.28372721571331,
3.92190940924059));
#45217=CARTESIAN_POINT('Ctrl Pts',(-70.8928448209104,-3.87619898010495,
2.36047829785777));
#45218=CARTESIAN_POINT('Ctrl Pts',(-70.7743127216604,-4.53258582022182,
0.229004239881362));
#45219=CARTESIAN_POINT('Ctrl Pts',(-70.6557806224101,-4.09437397816109,
-1.9577742225503));
#45220=CARTESIAN_POINT('Ctrl Pts',(-70.5372485231602,-2.66738928497651,
-3.67175863671992));
#45221=CARTESIAN_POINT('Ctrl Pts',(-70.41871642391,-0.596242238417822,-4.49903022686127));
#45222=CARTESIAN_POINT('Ctrl Pts',(-70.30018432466,1.61889463121599,-4.23980631827825));
#45223=CARTESIAN_POINT('Ctrl Pts',(-70.1816522254098,3.44307577905915,-2.95668847717401));
#45224=CARTESIAN_POINT('Ctrl Pts',(-70.0631201261598,4.43576975553545,-0.95954375658275));
#45225=CARTESIAN_POINT('Ctrl Pts',(-69.9445880269097,4.35724545924099,1.26932641366537));
#45226=CARTESIAN_POINT('Ctrl Pts',(-69.8260559276596,3.22646615654172,3.19166002122267));
#45227=CARTESIAN_POINT('Ctrl Pts',(-69.7075238284095,1.31650991577464,4.34322221190749));
#45228=CARTESIAN_POINT('Ctrl Pts',(-69.5889917291594,-0.911377495780072,
4.44591594678435));
#45229=CARTESIAN_POINT('Ctrl Pts',(-69.4704596299094,-2.91917137754172,
3.47494115231241));
#45230=CARTESIAN_POINT('Ctrl Pts',(-69.3519275306593,-4.22199861680048,
1.66478383696633));
#45231=CARTESIAN_POINT('Ctrl Pts',(-69.2333954314092,-4.50523234680097,
-0.547411221521476));
#45232=CARTESIAN_POINT('Ctrl Pts',(-69.1148633321591,-3.70047290679963,
-2.62740895370075));
#45233=CARTESIAN_POINT('Ctrl Pts',(-68.996331232909,-2.00206605012669,-4.0728993450629));
#45234=CARTESIAN_POINT('Ctrl Pts',(-68.8777991336589,0.179830673601517,
-4.53480302470077));
#45235=CARTESIAN_POINT('Ctrl Pts',(-68.7592670344089,2.31829910560496,-3.90157234983416));
#45236=CARTESIAN_POINT('Ctrl Pts',(-68.6407349351587,3.89690882252018,-2.32612965524106));
#45237=CARTESIAN_POINT('Ctrl Pts',(-68.5222028359087,4.53443274040068,-0.188937203354069));
#45238=CARTESIAN_POINT('Ctrl Pts',(-68.4036707366585,4.07691172574293,1.99388272587192));
#45239=CARTESIAN_POINT('Ctrl Pts',(-68.2851386374085,2.63483502765729,3.69518902372516));
#45240=CARTESIAN_POINT('Ctrl Pts',(-68.1666065381584,0.556457625537843,
4.50412393868227));
#45241=CARTESIAN_POINT('Ctrl Pts',(-68.0480744389084,-1.65630176831098,
4.2253333591942));
#45242=CARTESIAN_POINT('Ctrl Pts',(-67.9295423396582,-3.46907180031879,
2.92614394523961));
#45243=CARTESIAN_POINT('Ctrl Pts',(-67.8110102404082,-4.44407673291178,
0.920304045422876));
#45244=CARTESIAN_POINT('Ctrl Pts',(-67.692478141158,-4.34585729879867,-1.30778510563007));
#45245=CARTESIAN_POINT('Ctrl Pts',(-67.573946041908,-3.19813304566272,-3.22005008754051));
#45246=CARTESIAN_POINT('Ctrl Pts',(-67.4554139426579,-1.2780741730198,-4.35468758377558));
#45247=CARTESIAN_POINT('Ctrl Pts',(-67.3368818434078,0.950633813348891,
-4.43768778723192));
#45248=CARTESIAN_POINT('Ctrl Pts',(-67.2183497441577,2.94976804714372,-3.44900652537501));
#45249=CARTESIAN_POINT('Ctrl Pts',(-67.0998176449076,4.2365466816572,-1.6274058369592));
#45250=CARTESIAN_POINT('Ctrl Pts',(-66.9812855456576,4.50021851520795,0.587205976986872));
#45251=CARTESIAN_POINT('Ctrl Pts',(-66.8627534464074,3.67710799636248,2.66001021184443));
#45252=CARTESIAN_POINT('Ctrl Pts',(-66.7442213471574,1.9659925806888,4.09043404991525));
#45253=CARTESIAN_POINT('Ctrl Pts',(-66.6256892479072,-0.219901122842242,
4.53303662462618));
#45254=CARTESIAN_POINT('Ctrl Pts',(-66.5071571486572,-2.35268970297329,
3.88093142242336));
#45255=CARTESIAN_POINT('Ctrl Pts',(-66.3886250494071,-3.91731439479203,
2.29159889081503));
#45256=CARTESIAN_POINT('Ctrl Pts',(-66.270092950157,-4.53592543446018,0.14885562484077));
#45257=CARTESIAN_POINT('Ctrl Pts',(-66.1515608509069,-4.05913106274721,
-2.0298355991238));
#45258=CARTESIAN_POINT('Ctrl Pts',(-66.0330287516569,-2.60207495704307,
-3.7183307359565));
#45259=CARTESIAN_POINT('Ctrl Pts',(-65.9144966524067,-0.516629555714746,
-4.50886587139066));
#45260=CARTESIAN_POINT('Ctrl Pts',(-65.7959645531567,1.69357953919417,-4.21053035714652));
#45261=CARTESIAN_POINT('Ctrl Pts',(-65.6774324539066,3.49479685973577,-2.89537086626402));
#45262=CARTESIAN_POINT('Ctrl Pts',(-65.5589003546564,4.4520365957367,-0.880992448464069));
#45263=CARTESIAN_POINT('Ctrl Pts',(-65.4403682554065,4.33412969427594,1.3461416482767));
#45264=CARTESIAN_POINT('Ctrl Pts',(-65.3218361561563,3.16955013707242,3.2481886448625));
#45265=CARTESIAN_POINT('Ctrl Pts',(-65.2033040569063,1.2395386030961,4.36581282185392));
#45266=CARTESIAN_POINT('Ctrl Pts',(-65.0847719576561,-0.989815879318478,
4.42911301154967));
#45267=CARTESIAN_POINT('Ctrl Pts',(-64.966239858406,-2.98013431800993,3.42280250535274));
#45268=CARTESIAN_POINT('Ctrl Pts',(-64.847707759156,-4.25076384078795,1.58990072453571));
#45269=CARTESIAN_POINT('Ctrl Pts',(-64.7291756599058,-4.49485318318126,
-0.626954867334768));
#45270=CARTESIAN_POINT('Ctrl Pts',(-64.6106435606558,-3.6534558765185,-2.692403703452));
#45271=CARTESIAN_POINT('Ctrl Pts',(-64.4921114614057,-1.92976555265208,
-4.10764926153961));
#45272=CARTESIAN_POINT('Ctrl Pts',(-64.3735793621557,0.259954396175193,
-4.53091616077132));
#45273=CARTESIAN_POINT('Ctrl Pts',(-64.2550472629055,2.38689653782794,-3.85998736548898));
#45274=CARTESIAN_POINT('Ctrl Pts',(-64.1365151636555,3.93741399575905,-2.25688913552044));
#45275=CARTESIAN_POINT('Ctrl Pts',(-64.0179830644053,4.5370638391048,-0.108762419599618));
#45276=CARTESIAN_POINT('Ctrl Pts',(-63.8994509651554,4.04103335151306,2.06562992716232));
#45277=CARTESIAN_POINT('Ctrl Pts',(-63.7809188659052,2.56911164507772,3.74118201898217));
#45278=CARTESIAN_POINT('Ctrl Pts',(-63.6623867666552,0.476761133292039,
4.51325562823685));
#45279=CARTESIAN_POINT('Ctrl Pts',(-63.543854667405,-1.73072502895579,4.19539848145269));
#45280=CARTESIAN_POINT('Ctrl Pts',(-63.425322568155,-3.52024894960062,2.86437163735175));
#45281=CARTESIAN_POINT('Ctrl Pts',(-63.3067904689048,-4.45964872148725,
0.841612039461598));
#45282=CARTESIAN_POINT('Ctrl Pts',(-63.1882583696549,-4.32206356208222,
-1.38439304727765));
#45283=CARTESIAN_POINT('Ctrl Pts',(-63.0697262704046,-3.14071966311106,
-3.27607349456283));
#45284=CARTESIAN_POINT('Ctrl Pts',(-62.9511941711547,-1.20090621601503,
-4.37659705757406));
#45285=CARTESIAN_POINT('Ctrl Pts',(-62.8326620719044,1.02892063332738,-4.42019228929496));
#45286=CARTESIAN_POINT('Ctrl Pts',(-62.7141299726545,3.01026781828531,-3.39633113907137));
#45287=CARTESIAN_POINT('Ctrl Pts',(-62.5955978734043,4.26464898373894,-1.55227142907499));
#45288=CARTESIAN_POINT('Ctrl Pts',(-62.4770657741543,4.48913676978754,0.666654787858014));
#45289=CARTESIAN_POINT('Ctrl Pts',(-62.3585336749041,3.62951839467588,2.72458689836349));
#45290=CARTESIAN_POINT('Ctrl Pts',(-62.2400015756541,1.89338779561597,4.12454363529436));
#45291=CARTESIAN_POINT('Ctrl Pts',(-62.1214694764039,-0.29998736514476,
4.52844179876308));
#45292=CARTESIAN_POINT('Ctrl Pts',(-62.002937377154,-2.42091693835619,3.83874181491576));
#45293=CARTESIAN_POINT('Ctrl Pts',(-61.8844052779038,-3.95720605550443,
2.22200310044728));
#45294=CARTESIAN_POINT('Ctrl Pts',(-61.7658731786537,-4.53784786539412,
0.0686607192070461));
#45295=CARTESIAN_POINT('Ctrl Pts',(-61.6473410794036,-4.02262000565155,
-2.10126291418506));
#45296=CARTESIAN_POINT('Ctrl Pts',(-61.5288089801535,-2.53594766634852,
-3.76374108794713));
#45297=CARTESIAN_POINT('Ctrl Pts',(-61.4102768809035,-0.436855472474266,
-4.51729286634914));
#45298=CARTESIAN_POINT('Ctrl Pts',(-61.2917447816534,1.76773533663033,-4.1799389140226));
#45299=CARTESIAN_POINT('Ctrl Pts',(-61.1732126824033,3.54542608116568,-2.83314867977618));
#45300=CARTESIAN_POINT('Ctrl Pts',(-61.0546805831532,4.46691251711184,-0.802165894310029));
#45301=CARTESIAN_POINT('Ctrl Pts',(-60.9361484839031,4.30965984162703,1.42253631489993));
#45302=CARTESIAN_POINT('Ctrl Pts',(-60.817616384653,3.11164388178486,3.30370245865813));
#45303=CARTESIAN_POINT('Ctrl Pts',(-60.6990842854029,1.16218001690214,4.38703944854634));
#45304=CARTESIAN_POINT('Ctrl Pts',(-60.5805521861529,-1.06794499613072,
4.41092631736494));
#45305=CARTESIAN_POINT('Ctrl Pts',(-60.4620200869028,-3.04016624441482,
3.36959449389407));
#45306=CARTESIAN_POINT('Ctrl Pts',(-60.3434879876527,-4.27820092508761,
1.51452089020126));
#45307=CARTESIAN_POINT('Ctrl Pts',(-60.2249558884026,-4.48306992471128,
-0.706302638699686));
#45308=CARTESIAN_POINT('Ctrl Pts',(-60.1064237891525,-3.60529701130859,
-2.75655728081619));
#45309=CARTESIAN_POINT('Ctrl Pts',(-59.9878916899025,-1.85686297511547,
-4.14111585566494));
#45310=CARTESIAN_POINT('Ctrl Pts',(-59.8693595906524,0.339998562725392,
-4.52561372368815));
#45311=CARTESIAN_POINT('Ctrl Pts',(-59.7508274914022,2.45474490441493,-3.81719644661123));
#45312=CARTESIAN_POINT('Ctrl Pts',(-59.6322953921522,3.97669576066936,-2.18694347728569));
#45313=CARTESIAN_POINT('Ctrl Pts',(-59.513763292902,4.53826389257849,-0.0285537226009381));
#45314=CARTESIAN_POINT('Ctrl Pts',(-59.395231193652,4.00391977626628,2.1367319098308));
#45315=CARTESIAN_POINT('Ctrl Pts',(-59.2766990944019,2.50253054516668,3.78600593266119));
#45316=CARTESIAN_POINT('Ctrl Pts',(-59.1581669951518,0.397027511556691,
4.52097743498945));
#45317=CARTESIAN_POINT('Ctrl Pts',(-59.0396348959017,-1.80484254084631,
4.16415511545482));
#45318=CARTESIAN_POINT('Ctrl Pts',(-58.9606134964017,-2.98134669247437,
3.25577591290924));
#45319=CARTESIAN_POINT('Ctrl Pts',(-58.9211027966516,-3.42633377868327,
2.68871070989395));
#45320=CARTESIAN_POINT('Ctrl Pts',(-89.575,2.36230756092335,-3.31488661006744));
#45321=CARTESIAN_POINT('Ctrl Pts',(-89.53548930025,2.91092803106123,-2.9239199082961));
#45322=CARTESIAN_POINT('Ctrl Pts',(-89.4564679007499,3.80977362498712,-1.86473730182378));
#45323=CARTESIAN_POINT('Ctrl Pts',(-89.3379358014998,4.23793920928767,0.175536844418832));
#45324=CARTESIAN_POINT('Ctrl Pts',(-89.2194037022498,3.6426422996848,2.17296520226056));
#45325=CARTESIAN_POINT('Ctrl Pts',(-89.1008716029996,2.16767467238955,3.64585259348834));
#45326=CARTESIAN_POINT('Ctrl Pts',(-88.9823395037495,0.169217900166083,
4.23817423904527));
#45327=CARTESIAN_POINT('Ctrl Pts',(-88.8638074044995,-1.87010146406577,
3.80705007020246));
#45328=CARTESIAN_POINT('Ctrl Pts',(-88.7452753052494,-3.45780118263798,
2.45651375596413));
#45329=CARTESIAN_POINT('Ctrl Pts',(-88.6267432059994,-4.21045692323235,
0.512753836099102));
#45330=CARTESIAN_POINT('Ctrl Pts',(-88.5082111067491,-3.94630675958036,
-1.5548404226029));
#45331=CARTESIAN_POINT('Ctrl Pts',(-88.3896790074992,-2.72914125118652,
-3.24694449006369));
#45332=CARTESIAN_POINT('Ctrl Pts',(-88.271146908249,-0.852900597114338,
-4.15492782628333));
#45333=CARTESIAN_POINT('Ctrl Pts',(-88.152614808999,1.22931172268961,-4.05951413513238));
#45334=CARTESIAN_POINT('Ctrl Pts',(-88.0340827097489,3.01465081869963,-2.98374660176146));
#45335=CARTESIAN_POINT('Ctrl Pts',(-87.9155506104989,4.07196543070694,-1.18741760272948));
#45336=CARTESIAN_POINT('Ctrl Pts',(-87.7970185112487,4.1459188620231,0.895667260529816));
#45337=CARTESIAN_POINT('Ctrl Pts',(-87.6784864119986,3.21865170212703,2.76245259353163));
#45338=CARTESIAN_POINT('Ctrl Pts',(-87.5599543127485,1.51409475903765,3.96211813494982));
#45339=CARTESIAN_POINT('Ctrl Pts',(-87.4414222134985,-0.556109197774073,
4.20495013639211));
#45340=CARTESIAN_POINT('Ctrl Pts',(-87.3228901142483,-2.49201530688875,
3.43230575316451));
#45341=CARTESIAN_POINT('Ctrl Pts',(-87.2043580149983,-3.82611102636026,
1.830775107081));
#45342=CARTESIAN_POINT('Ctrl Pts',(-87.0858259157481,-4.23621829341267,
-0.212879421996658));
#45343=CARTESIAN_POINT('Ctrl Pts',(-86.9672938164981,-3.62329806373565,
-2.2051245358312));
#45344=CARTESIAN_POINT('Ctrl Pts',(-86.848761717248,-2.1353677918245,-3.66484208003093));
#45345=CARTESIAN_POINT('Ctrl Pts',(-86.730229617998,-0.131755887070526,
-4.23951689036003));
#45346=CARTESIAN_POINT('Ctrl Pts',(-86.6116975187478,1.90367446658495,-3.7903676078918));
#45347=CARTESIAN_POINT('Ctrl Pts',(-86.4931654194978,3.47937607418291,-2.42586174626368));
#45348=CARTESIAN_POINT('Ctrl Pts',(-86.3746333202476,4.21482414698068,-0.475521279897397));
#45349=CARTESIAN_POINT('Ctrl Pts',(-86.2561012209977,3.93241131237811,1.58965541797289));
#45350=CARTESIAN_POINT('Ctrl Pts',(-86.1375691217474,2.70033898852751,3.27093754520615));
#45351=CARTESIAN_POINT('Ctrl Pts',(-86.0190370224974,0.816147051306786,
4.16230309663427));
#45352=CARTESIAN_POINT('Ctrl Pts',(-85.9005049232474,-1.26514069566702,
4.04849133601287));
#45353=CARTESIAN_POINT('Ctrl Pts',(-85.7819728239972,-3.04090270501211,
2.95698728713125));
#45354=CARTESIAN_POINT('Ctrl Pts',(-85.6634407247472,-4.08230050870968,
1.15138422526712));
#45355=CARTESIAN_POINT('Ctrl Pts',(-85.544908625497,-4.13784126234383,-0.932272902775868));
#45356=CARTESIAN_POINT('Ctrl Pts',(-85.426376526247,-3.19411212591926,-2.79079035483874));
#45357=CARTESIAN_POINT('Ctrl Pts',(-85.3078444269969,-1.47901940386148,
-3.97534459897585));
#45358=CARTESIAN_POINT('Ctrl Pts',(-85.1893123277468,0.593249793413271,
-4.19987115995485));
#45359=CARTESIAN_POINT('Ctrl Pts',(-85.0707802284967,2.52225185735541,-3.41014789205285));
#45360=CARTESIAN_POINT('Ctrl Pts',(-84.9522481292466,3.84214154206329,-1.79688938122436));
#45361=CARTESIAN_POINT('Ctrl Pts',(-84.8337160299966,4.23417147746969,0.250309762069736));
#45362=CARTESIAN_POINT('Ctrl Pts',(-84.7151839307464,3.60366821294754,2.23706023356476));
#45363=CARTESIAN_POINT('Ctrl Pts',(-84.5966518314964,2.10289542607052,3.6835708089593));
#45364=CARTESIAN_POINT('Ctrl Pts',(-84.4781197322463,0.094282935351365,
4.24051574760746));
#45365=CARTESIAN_POINT('Ctrl Pts',(-84.3595876329963,-1.9370984564613,3.77339537387491));
#45366=CARTESIAN_POINT('Ctrl Pts',(-84.241055533746,-3.50067936031506,2.39501713853357));
#45367=CARTESIAN_POINT('Ctrl Pts',(-84.1225234344961,-4.21886208242914,
0.43825313124611));
#45368=CARTESIAN_POINT('Ctrl Pts',(-84.0039913352459,-3.91820875405299,
-1.62434701873333));
#45369=CARTESIAN_POINT('Ctrl Pts',(-83.8854592359959,-2.67132578982276,
-3.29467473390518));
#45370=CARTESIAN_POINT('Ctrl Pts',(-83.7669271367457,-0.779329768066677,
-4.16935344990209));
#45371=CARTESIAN_POINT('Ctrl Pts',(-83.6483950374957,1.3008708565925,-4.03715222552651));
#45372=CARTESIAN_POINT('Ctrl Pts',(-83.5298629382456,3.06691707187941,-2.92999705662308));
#45373=CARTESIAN_POINT('Ctrl Pts',(-83.4113308389955,4.0923167299564,-1.11526089294132));
#45374=CARTESIAN_POINT('Ctrl Pts',(-83.2927987397454,4.12944046598591,0.968805716066663));
#45375=CARTESIAN_POINT('Ctrl Pts',(-83.1742666404953,3.16932306615985,2.81891014044657));
#45376=CARTESIAN_POINT('Ctrl Pts',(-83.0557345412452,1.44382852615606,3.98826055626553));
#45377=CARTESIAN_POINT('Ctrl Pts',(-82.9372024419952,-0.630344051771873,
4.19446414384497));
#45378=CARTESIAN_POINT('Ctrl Pts',(-82.818670342745,-2.55229140128288,3.38772367240052));
#45379=CARTESIAN_POINT('Ctrl Pts',(-82.700138243495,-3.8578719580008,1.76286330532926));
#45380=CARTESIAN_POINT('Ctrl Pts',(-82.581606144245,-4.23179394134261,-0.287720551266843));
#45381=CARTESIAN_POINT('Ctrl Pts',(-82.4630740449948,-3.58375688894285,
-2.26882120021829));
#45382=CARTESIAN_POINT('Ctrl Pts',(-82.3445419457447,-2.0702588085909,-3.70201182373276));
#45383=CARTESIAN_POINT('Ctrl Pts',(-82.2260098464947,-0.0568026194346637,
-4.24118338910624));
#45384=CARTESIAN_POINT('Ctrl Pts',(-82.1074777472446,1.97037114458219,-3.75612840970636));
#45385=CARTESIAN_POINT('Ctrl Pts',(-81.9889456479944,3.52170921742845,-2.36398546219828));
#45386=CARTESIAN_POINT('Ctrl Pts',(-81.8704135487444,4.2225704934618,-0.40095075177776));
#45387=CARTESIAN_POINT('Ctrl Pts',(-81.7518814494942,3.90370015456685,1.65891174594675));
#45388=CARTESIAN_POINT('Ctrl Pts',(-81.6333493502442,2.64210394076326,3.31815458407359));
#45389=CARTESIAN_POINT('Ctrl Pts',(-81.514817250994,0.742451613392211,4.17607814574591));
#45390=CARTESIAN_POINT('Ctrl Pts',(-81.3962851517442,-1.33649940985683,
4.02549778351171));
#45391=CARTESIAN_POINT('Ctrl Pts',(-81.2777530524938,-3.09269188977919,
2.90277797161605));
#45392=CARTESIAN_POINT('Ctrl Pts',(-81.159220953244,-4.10201331091795,1.07905045046897));
#45393=CARTESIAN_POINT('Ctrl Pts',(-81.0406888539936,-4.12071712970371,
-1.00526285844639));
#45394=CARTESIAN_POINT('Ctrl Pts',(-80.9221567547438,-3.14428645876529,
-2.84680974826745));
#45395=CARTESIAN_POINT('Ctrl Pts',(-80.8036246554935,-1.40852487473531,
-4.00086500082885));
#45396=CARTESIAN_POINT('Ctrl Pts',(-80.6850925562435,0.667389075585396,
-4.18872950897938));
#45397=CARTESIAN_POINT('Ctrl Pts',(-80.5665604569934,2.58213159232414,-3.36503484640604));
#45398=CARTESIAN_POINT('Ctrl Pts',(-80.4480283577433,3.87330104552845,-1.72869953673665));
#45399=CARTESIAN_POINT('Ctrl Pts',(-80.3294962584933,4.22908587072581,0.325108867355182));
#45400=CARTESIAN_POINT('Ctrl Pts',(-80.2109641592431,3.56356564694796,2.30040495511053));
#45401=CARTESIAN_POINT('Ctrl Pts',(-80.0924320599931,2.03746048854546,3.72016368392876));
#45402=CARTESIAN_POINT('Ctrl Pts',(-79.9738999607429,0.0193178668117769,
4.2415197627297));
#45403=CARTESIAN_POINT('Ctrl Pts',(-79.855367861493,-2.00348993210374,3.73856806405375));
#45404=CARTESIAN_POINT('Ctrl Pts',(-79.7368357622428,-3.54246400293638,
2.33276914106685));
#45405=CARTESIAN_POINT('Ctrl Pts',(-79.6183036629927,-4.2259490904216,0.36361705508285));
#45406=CARTESIAN_POINT('Ctrl Pts',(-79.4997715637427,-3.88888664715446,
-1.69334689985141));
#45407=CARTESIAN_POINT('Ctrl Pts',(-79.3812394644925,-2.61267572378093,
-3.34137526175934));
#45408=CARTESIAN_POINT('Ctrl Pts',(-79.2627073652425,-0.705515467763387,
-4.18247665892133));
#45409=CARTESIAN_POINT('Ctrl Pts',(-79.1441752659924,1.3720235726515,-4.01352892025788));
#45410=CARTESIAN_POINT('Ctrl Pts',(-79.0256431667423,3.11822514541502,-2.87533215814075));
#45411=CARTESIAN_POINT('Ctrl Pts',(-78.9071110674922,4.11138949440471,-1.04275572611736));
#45412=CARTESIAN_POINT('Ctrl Pts',(-78.7885789682421,4.11167193448134,1.04164148226761));
#45413=CARTESIAN_POINT('Ctrl Pts',(-78.670046868992,3.11900426003185,2.87448699928452));
#45414=CARTESIAN_POINT('Ctrl Pts',(-78.551514769742,1.37311120556277,4.01315694786418));
#45415=CARTESIAN_POINT('Ctrl Pts',(-78.4329826704918,-0.704381968314586,
4.18266770388186));
#45416=CARTESIAN_POINT('Ctrl Pts',(-78.3144505712418,-2.61177010587796,
3.34208318501393));
#45417=CARTESIAN_POINT('Ctrl Pts',(-78.1959184719917,-3.88842758715636,
1.69440074634939));
#45418=CARTESIAN_POINT('Ctrl Pts',(-78.0773863727416,-4.22604750203994,
-0.362471794982803));
#45419=CARTESIAN_POINT('Ctrl Pts',(-77.9588542734915,-3.54309601390001,
-2.33180902134115));
#45420=CARTESIAN_POINT('Ctrl Pts',(-77.8403221742414,-2.00450312872445,
-3.73802499184148));
#45421=CARTESIAN_POINT('Ctrl Pts',(-77.7217900749913,0.0181685980883059,
-4.2415248017455));
#45422=CARTESIAN_POINT('Ctrl Pts',(-77.6032579757413,2.03645182254301,-3.72071578999402));
#45423=CARTESIAN_POINT('Ctrl Pts',(-77.4847258764911,3.56294292078298,-2.30137044925895));
#45424=CARTESIAN_POINT('Ctrl Pts',(-77.3661937772411,4.22899594778787,-0.326255287706977));
#45425=CARTESIAN_POINT('Ctrl Pts',(-77.247661677991,3.87377273534343,1.72765045644101));
#45426=CARTESIAN_POINT('Ctrl Pts',(-77.1291295787409,2.58303669769032,3.36433361268123));
#45427=CARTESIAN_POINT('Ctrl Pts',(-77.0105974794908,0.668537789879148,
4.18855118954554));
#45428=CARTESIAN_POINT('Ctrl Pts',(-76.8920653802408,-1.40746790745146,
4.00124113310223));
#45429=CARTESIAN_POINT('Ctrl Pts',(-76.7735332809906,-3.14345978794428,
2.84767271097138));
#45430=CARTESIAN_POINT('Ctrl Pts',(-76.6550011817406,-4.12055543071948,
1.00635749957924));
#45431=CARTESIAN_POINT('Ctrl Pts',(-76.5364690824904,-4.1020822716358,-1.07789432737393));
#45432=CARTESIAN_POINT('Ctrl Pts',(-76.4179369832404,-3.09392819414575,
-2.90202919022035));
#45433=CARTESIAN_POINT('Ctrl Pts',(-76.2994048839903,-1.33668453718049,
-4.02495526764412));
#45434=CARTESIAN_POINT('Ctrl Pts',(-76.1808727847402,0.739496217920181,
-4.17664208939481));
#45435=CARTESIAN_POINT('Ctrl Pts',(-76.0623406854901,2.64486935815373,-3.3181392451129));
#45436=CARTESIAN_POINT('Ctrl Pts',(-75.9438085862401,3.89596740984592,-1.66144883365045));
#45437=CARTESIAN_POINT('Ctrl Pts',(-75.7857657872398,4.3485497237372,1.09093805761265));
#45438=CARTESIAN_POINT('Ctrl Pts',(-75.5882122884899,2.2380304938709,4.25065369199898));
#45439=CARTESIAN_POINT('Ctrl Pts',(-75.3511480899896,-2.34621401747439,
4.19467891885534));
#45440=CARTESIAN_POINT('Ctrl Pts',(-75.1140838914895,-4.79121655698383,
0.326463415623377));
#45441=CARTESIAN_POINT('Ctrl Pts',(-74.8770196929892,-2.89233179269924,
-3.83561280588861));
#45442=CARTESIAN_POINT('Ctrl Pts',(-74.639955494489,1.63433374823429,-4.51748027493275));
#45443=CARTESIAN_POINT('Ctrl Pts',(-74.402891295989,4.6763033020638,-1.09843764222045));
#45444=CARTESIAN_POINT('Ctrl Pts',(-74.1658270974887,3.47436957665643,3.31745869645859));
#45445=CARTESIAN_POINT('Ctrl Pts',(-73.9287628989886,-0.881308697829502,
4.72204116943823));
#45446=CARTESIAN_POINT('Ctrl Pts',(-73.6916987004883,-4.43718510449666,
1.84121242214388));
#45447=CARTESIAN_POINT('Ctrl Pts',(-73.4546345019883,-3.96509169180119,
-2.71211295328289));
#45448=CARTESIAN_POINT('Ctrl Pts',(-73.217570303488,0.104851279587011,-4.80118117413053));
#45449=CARTESIAN_POINT('Ctrl Pts',(-72.9805061049878,4.0818527109764,-2.5374258400941));
#45450=CARTESIAN_POINT('Ctrl Pts',(-72.7434419064878,4.34947338571156,2.0393426803231));
#45451=CARTESIAN_POINT('Ctrl Pts',(-72.5458884077375,1.29059508521834,4.29352941894811));
#45452=CARTESIAN_POINT('Ctrl Pts',(-72.3878456087375,-1.47975600101921,
3.96853832825987));
#45453=CARTESIAN_POINT('Ctrl Pts',(-72.2693135094873,-3.19245598996507,
2.7952829416349));
#45454=CARTESIAN_POINT('Ctrl Pts',(-72.1507814102373,-4.13803517954143,
0.931589315149122));
#45455=CARTESIAN_POINT('Ctrl Pts',(-72.0322493109872,-4.08239058226615,
-1.14938139548983));
#45456=CARTESIAN_POINT('Ctrl Pts',(-71.9137172117371,-3.04181408411095,
-2.95660822043184));
#45457=CARTESIAN_POINT('Ctrl Pts',(-71.7951851124869,-1.26618312449043,
-4.04792730165813));
#45458=CARTESIAN_POINT('Ctrl Pts',(-71.676653013237,0.814991865508356,-4.1626338697688));
#45459=CARTESIAN_POINT('Ctrl Pts',(-71.5581209139868,2.69946593220966,-3.27161473710967));
#45460=CARTESIAN_POINT('Ctrl Pts',(-71.4395888147368,3.93197366980717,-1.59074811823812));
#45461=CARTESIAN_POINT('Ctrl Pts',(-71.3210567154866,4.21495618453984,0.474392460257583));
#45462=CARTESIAN_POINT('Ctrl Pts',(-71.2025246162366,3.48003171573737,2.42491205953816));
#45463=CARTESIAN_POINT('Ctrl Pts',(-71.0839925169865,1.90470242326041,3.78985487631873));
#45464=CARTESIAN_POINT('Ctrl Pts',(-70.9654604177364,-0.130607360489598,
4.2395507965525));
#45465=CARTESIAN_POINT('Ctrl Pts',(-70.8469283184863,-2.13437432226263,
3.6654214565239));
#45466=CARTESIAN_POINT('Ctrl Pts',(-70.7283962192362,-3.62270043207957,
2.20610597997014));
#45467=CARTESIAN_POINT('Ctrl Pts',(-70.6098641199862,-4.2361603967273,0.214027650031447));
#45468=CARTESIAN_POINT('Ctrl Pts',(-70.491332020736,-3.82660705910867,-1.82973824572734));
#45469=CARTESIAN_POINT('Ctrl Pts',(-70.372799921486,-2.49294537375558,-3.43163023054535));
#45470=CARTESIAN_POINT('Ctrl Pts',(-70.2542678222358,-0.557248744408297,
-4.20479929705468));
#45471=CARTESIAN_POINT('Ctrl Pts',(-70.1357357229858,1.51302095431612,-3.96252830672392));
#45472=CARTESIAN_POINT('Ctrl Pts',(-70.0172036237356,3.21790294474063,-2.7633247619019));
#45473=CARTESIAN_POINT('Ctrl Pts',(-69.8986715244856,4.14567598115117,-0.896790799288985));
#45474=CARTESIAN_POINT('Ctrl Pts',(-69.7801394252355,4.07228707527332,1.18631405942714));
#45475=CARTESIAN_POINT('Ctrl Pts',(-69.6616073259855,3.01545931965475,2.98292946189813));
#45476=CARTESIAN_POINT('Ctrl Pts',(-69.5430752267353,1.23041181972154,4.05918093071395));
#45477=CARTESIAN_POINT('Ctrl Pts',(-69.4245431274853,-0.851774551486206,
4.15515862422754));
#45478=CARTESIAN_POINT('Ctrl Pts',(-69.3060110282352,-2.72826123349541,
3.24768436257942));
#45479=CARTESIAN_POINT('Ctrl Pts',(-69.1874789289851,-3.9458852065712,1.5559090636089));
#45480=CARTESIAN_POINT('Ctrl Pts',(-69.068946829735,-4.210595806135,-0.511611214725999));
#45481=CARTESIAN_POINT('Ctrl Pts',(-68.9504147304849,-3.45846662340299,
-2.45557970596334));
#45482=CARTESIAN_POINT('Ctrl Pts',(-68.8318826312348,-1.87113344337377,
-3.8065368400609));
#45483=CARTESIAN_POINT('Ctrl Pts',(-68.7133505319848,0.168069973265368,
-4.23823259881627));
#45484=CARTESIAN_POINT('Ctrl Pts',(-68.5948184327347,2.16668525394882,-3.64641441527627));
#45485=CARTESIAN_POINT('Ctrl Pts',(-68.4762863334845,3.64205587679515,-2.17400369546731));
#45486=CARTESIAN_POINT('Ctrl Pts',(-68.3577542342345,4.23788653064464,-0.176580947402252));
#45487=CARTESIAN_POINT('Ctrl Pts',(-68.2392221349844,3.81028681608063,1.86348529825389));
#45488=CARTESIAN_POINT('Ctrl Pts',(-68.1206900357343,2.46252012400403,3.45352829964948));
#45489=CARTESIAN_POINT('Ctrl Pts',(-68.0021579364842,0.520065995274375,
4.20955988651605));
#45490=CARTESIAN_POINT('Ctrl Pts',(-67.8836258372342,-1.54798171159727,
3.94900186099799));
#45491=CARTESIAN_POINT('Ctrl Pts',(-67.7650937379841,-3.24219885883922,
2.73477780401754));
#45492=CARTESIAN_POINT('Ctrl Pts',(-67.646561638734,-4.15343969263372,0.860117315986614));
#45493=CARTESIAN_POINT('Ctrl Pts',(-67.5280295394839,-4.0616436862299,-1.2222576012094));
#45494=CARTESIAN_POINT('Ctrl Pts',(-67.4094974402338,-2.98897915866447,
-3.00946285351303));
#45495=CARTESIAN_POINT('Ctrl Pts',(-67.2909653409837,-1.19448972629963,
-4.06989648165282));
#45496=CARTESIAN_POINT('Ctrl Pts',(-67.1724332417337,0.888463555159219,
-4.14746857598213));
#45497=CARTESIAN_POINT('Ctrl Pts',(-67.0539011424835,2.75685691930934,-3.22344582769147));
#45498=CARTESIAN_POINT('Ctrl Pts',(-66.9353690432335,3.95948184624652,-1.52097553788664));
#45499=CARTESIAN_POINT('Ctrl Pts',(-66.8168369439834,4.20590987283498,0.548803443132984));
#45500=CARTESIAN_POINT('Ctrl Pts',(-66.6983048447332,3.43662974878158,2.48604888274442));
#45501=CARTESIAN_POINT('Ctrl Pts',(-66.5797727454832,1.83741913355893,3.82292479722488));
#45502=CARTESIAN_POINT('Ctrl Pts',(-66.4612406462331,-0.205519865420819,
4.23658171908943));
#45503=CARTESIAN_POINT('Ctrl Pts',(-66.3427085469829,-2.19882674941518,
3.62712337861033));
#45504=CARTESIAN_POINT('Ctrl Pts',(-66.224176447733,-3.66112695025279,2.1417311996929));
#45505=CARTESIAN_POINT('Ctrl Pts',(-66.1056443484827,-4.23928160438623,
0.139120653814684));
#45506=CARTESIAN_POINT('Ctrl Pts',(-65.9871122492328,-3.79366898612715,
-1.89708689872192));
#45507=CARTESIAN_POINT('Ctrl Pts',(-65.8685801499826,-2.43190252088865,
-3.47515657294758));
#45508=CARTESIAN_POINT('Ctrl Pts',(-65.7500480507326,-0.482842631226866,
-4.21399170277722));
#45509=CARTESIAN_POINT('Ctrl Pts',(-65.6315159514825,1.58282156305449,-3.93516695670401));
#45510=CARTESIAN_POINT('Ctrl Pts',(-65.5129838522324,3.26624153165954,-2.70601724578163));
#45511=CARTESIAN_POINT('Ctrl Pts',(-65.3944517529823,4.16087899042085,-0.823376648126326));
#45512=CARTESIAN_POINT('Ctrl Pts',(-65.2759196537323,4.05068305232286,1.25810567411077));
#45513=CARTESIAN_POINT('Ctrl Pts',(-65.1573875544821,2.96226553641969,3.03576118450472));
#45514=CARTESIAN_POINT('Ctrl Pts',(-65.0388554552321,1.1584743342804,4.08029414312485));
#45515=CARTESIAN_POINT('Ctrl Pts',(-64.9203233559819,-0.925083163194395,
4.13945457986673));
#45516=CARTESIAN_POINT('Ctrl Pts',(-64.8017912567319,-2.78523727417561,
3.19895551768826));
#45517=CARTESIAN_POINT('Ctrl Pts',(-64.6832591574818,-3.97276922101502,
1.4859232127405));
#45518=CARTESIAN_POINT('Ctrl Pts',(-64.5647270582317,-4.20089542678846,
-0.585952805943586));
#45519=CARTESIAN_POINT('Ctrl Pts',(-64.4461949589816,-3.41452444788805,
-2.51632388066006));
#45520=CARTESIAN_POINT('Ctrl Pts',(-64.3276628597316,-1.80356130768488,
-3.83901415561695));
#45521=CARTESIAN_POINT('Ctrl Pts',(-64.2091307604814,0.242953704951307,
-4.23459993090915));
#45522=CARTESIAN_POINT('Ctrl Pts',(-64.0905986612314,2.23079650020559,-3.60754903671119));
#45523=CARTESIAN_POINT('Ctrl Pts',(-63.9720665619813,3.67991206254491,-2.10929141882807));
#45524=CARTESIAN_POINT('Ctrl Pts',(-63.8535344627312,4.24034555879598,-0.101649493872672));
#45525=CARTESIAN_POINT('Ctrl Pts',(-63.7350023634811,3.77675484249208,1.93054032263455));
#45526=CARTESIAN_POINT('Ctrl Pts',(-63.6164702642311,2.40109496815141,3.49651341074552));
#45527=CARTESIAN_POINT('Ctrl Pts',(-63.4979381649809,0.445581553589111,
4.21809437503554));
#45528=CARTESIAN_POINT('Ctrl Pts',(-63.3794060657309,-1.61753778440945,
3.92102468668754));
#45529=CARTESIAN_POINT('Ctrl Pts',(-63.2608739664807,-3.29002908679384,
2.67704532753104));
#45530=CARTESIAN_POINT('Ctrl Pts',(-63.1423418672307,-4.16799329270179,
0.786571668443664));
#45531=CARTESIAN_POINT('Ctrl Pts',(-63.0238097679806,-4.03940603002961,
-1.29385547962891));
#45532=CARTESIAN_POINT('Ctrl Pts',(-62.9052776687305,-2.93532053926837,
-3.06182240003477));
#45533=CARTESIAN_POINT('Ctrl Pts',(-62.7867455694804,-1.12236845682437,
-4.09037310336489));
#45534=CARTESIAN_POINT('Ctrl Pts',(-62.6682134702303,0.961630515374074,
-4.13111726165049));
#45535=CARTESIAN_POINT('Ctrl Pts',(-62.5496813709802,2.81340008135553,-3.17421534553572));
#45536=CARTESIAN_POINT('Ctrl Pts',(-62.4311492717302,3.98574629304517,-1.4507548259719));
#45537=CARTESIAN_POINT('Ctrl Pts',(-62.31261717248,4.19555285965564,0.623056401494609));
#45538=CARTESIAN_POINT('Ctrl Pts',(-62.19408507323,3.39215244731244,2.5464023350196));
#45539=CARTESIAN_POINT('Ctrl Pts',(-62.0755529739799,1.7695626102988,3.85480365853339));
#45540=CARTESIAN_POINT('Ctrl Pts',(-61.9570208747298,-0.280368567998288,
4.23228738907051));
#45541=CARTESIAN_POINT('Ctrl Pts',(-61.8384887754797,-2.26259200924054,
3.58769291847877));
#45542=CARTESIAN_POINT('Ctrl Pts',(-61.7199566762296,-3.69840974642527,
2.07668688666092));
#45543=CARTESIAN_POINT('Ctrl Pts',(-61.6014245769796,-4.24107831075006,
0.0641703943514818));
#45544=CARTESIAN_POINT('Ctrl Pts',(-61.4828924777294,-3.75954570633811,
-1.96384295703131));
#45545=CARTESIAN_POINT('Ctrl Pts',(-61.3643603784794,-2.3700998720048,-3.51759714491556));
#45546=CARTESIAN_POINT('Ctrl Pts',(-61.2458282792293,-0.408285672900589,
-4.22186758284269));
#45547=CARTESIAN_POINT('Ctrl Pts',(-61.1272961799792,1.65212766441617,-3.90657615556305));
#45548=CARTESIAN_POINT('Ctrl Pts',(-61.0087640807291,3.31355966555602,-2.64786431219091));
#45549=CARTESIAN_POINT('Ctrl Pts',(-60.8902319814791,4.1747820452098,-0.749705251673546));
#45550=CARTESIAN_POINT('Ctrl Pts',(-60.7716998822289,4.02781349732346,1.32950422542484));
#45551=CARTESIAN_POINT('Ctrl Pts',(-60.6531677829789,2.90814627754596,3.08764446455717));
#45552=CARTESIAN_POINT('Ctrl Pts',(-60.5346356837287,1.08617490252564,4.10013257507453));
#45553=CARTESIAN_POINT('Ctrl Pts',(-60.4161035844787,-0.998102733832139,
4.12245727265436));
#45554=CARTESIAN_POINT('Ctrl Pts',(-60.2975714852285,-2.84134318794365,
3.14922724339409));
#45555=CARTESIAN_POINT('Ctrl Pts',(-60.1790393859785,-3.99841195443958,
1.41547312495732));
#45556=CARTESIAN_POINT('Ctrl Pts',(-60.0605072867284,-4.18988277863246,
-0.660111332655873));
#45557=CARTESIAN_POINT('Ctrl Pts',(-59.9419751874784,-3.36951511201551,
-2.57628189458803));
#45558=CARTESIAN_POINT('Ctrl Pts',(-59.8234430882282,-1.73542646721431,
-3.87029207649262));
#45559=CARTESIAN_POINT('Ctrl Pts',(-59.7049109889782,0.317763083477844,
-4.22964426655577));
#45560=CARTESIAN_POINT('Ctrl Pts',(-59.586378889728,2.29420766877876,-3.56755659021834));
#45561=CARTESIAN_POINT('Ctrl Pts',(-59.4678467904781,3.71662484933523,-2.04392011884845));
#45562=CARTESIAN_POINT('Ctrl Pts',(-59.3493146912278,4.24146713027876,-0.0266863449824727));
#45563=CARTESIAN_POINT('Ctrl Pts',(-59.2307825919778,3.74206844848274,1.99699232488131));
#45564=CARTESIAN_POINT('Ctrl Pts',(-59.1122504927277,2.33886818860421,3.53840589673139));
#45565=CARTESIAN_POINT('Ctrl Pts',(-58.9937183934776,0.371062410636318,
4.22531118531867));
#45566=CARTESIAN_POINT('Ctrl Pts',(-58.8751862942276,-1.68680810405213,
3.89182459761031));
#45567=CARTESIAN_POINT('Ctrl Pts',(-58.7961648947275,-2.78637036087181,
3.04285225474445));
#45568=CARTESIAN_POINT('Ctrl Pts',(-58.7566541949775,-3.20225585017534,
2.51287240424535));
#45569=CARTESIAN_POINT('Origin',(0.5,7.95374963839832,-1.25014666726696));
#45570=CARTESIAN_POINT('',(9.,7.8971245663519,-1.27883680879202));
#45571=CARTESIAN_POINT('',(0.499999999999999,7.8971245663519,-1.27883680879202));
#45572=CARTESIAN_POINT('',(4.75,7.8971245663519,-1.27883680879202));
#45573=CARTESIAN_POINT('',(9.,7.73074086114583,-1.3631381946854));
#45574=CARTESIAN_POINT('',(9.,7.95374963839832,-1.25014666726696));
#45575=CARTESIAN_POINT('',(0.5,7.73074086114583,-1.3631381946854));
#45576=CARTESIAN_POINT('',(0.5,7.73074086114583,-1.3631381946854));
#45577=CARTESIAN_POINT('',(0.5,7.95374963839832,-1.25014666726696));
#45578=CARTESIAN_POINT('Origin',(0.5,7.82922163644705,-1.3805030124521));
#45579=CARTESIAN_POINT('',(0.499999999999999,7.85825762906118,-1.49926216363308));
#45580=CARTESIAN_POINT('Origin',(0.5,0.,0.));
#45581=CARTESIAN_POINT('',(0.5,7.73074086114583,-1.3631381946854));
#45582=CARTESIAN_POINT('Origin',(0.5,7.73074086114583,-1.3631381946854));
#45583=CARTESIAN_POINT('',(9.,7.85825762906118,-1.49926216363308));
#45584=CARTESIAN_POINT('',(4.75,7.85825762906118,-1.49926216363308));
#45585=CARTESIAN_POINT('',(9.,7.73074086114583,-1.3631381946854));
#45586=CARTESIAN_POINT('Origin',(9.,7.82922163644705,-1.3805030124521));
#45587=CARTESIAN_POINT('Origin',(9.,0.,0.));
#45588=CARTESIAN_POINT('Origin',(0.5,7.61582861882541,-2.61230826065375));
#45589=CARTESIAN_POINT('',(9.,7.55508181806639,-2.63072969389153));
#45590=CARTESIAN_POINT('',(0.499999999999999,7.55508181806639,-2.63072969389153));
#45591=CARTESIAN_POINT('',(4.75,7.55508181806639,-2.63072969389153));
#45592=CARTESIAN_POINT('',(9.,7.37658707316938,-2.6848581251065));
#45593=CARTESIAN_POINT('',(9.,7.61582861882541,-2.61230826065375));
#45594=CARTESIAN_POINT('',(0.5,7.37658707316938,-2.6848581251065));
#45595=CARTESIAN_POINT('',(0.5,7.37658707316938,-2.6848581251065));
#45596=CARTESIAN_POINT('',(0.5,7.61582861882541,-2.61230826065375));
#45597=CARTESIAN_POINT('Origin',(0.5,7.47055633524797,-2.71906013943907));
#45598=CARTESIAN_POINT('',(0.499999999999999,7.47852889570692,-2.84105711946744));
#45599=CARTESIAN_POINT('Origin',(0.5,0.,0.));
#45600=CARTESIAN_POINT('',(0.5,7.37658707316938,-2.6848581251065));
#45601=CARTESIAN_POINT('Origin',(0.5,7.37658707316938,-2.6848581251065));
#45602=CARTESIAN_POINT('',(9.,7.47852889570692,-2.84105711946744));
#45603=CARTESIAN_POINT('',(4.75,7.47852889570692,-2.84105711946744));
#45604=CARTESIAN_POINT('',(9.,7.37658707316938,-2.6848581251065));
#45605=CARTESIAN_POINT('Origin',(9.,7.47055633524797,-2.71906013943907));
#45606=CARTESIAN_POINT('Origin',(9.,0.,0.));
#45607=CARTESIAN_POINT('Origin',(0.5,7.04650450046473,-3.89509618943234));
#45608=CARTESIAN_POINT('',(9.,6.98348173179481,-3.9026891884556));
#45609=CARTESIAN_POINT('',(0.499999999999999,6.98348173179481,-3.9026891884556));
#45610=CARTESIAN_POINT('',(4.75,6.98348173179481,-3.9026891884556));
#45611=CARTESIAN_POINT('',(9.,6.79829941970784,-3.925));
#45612=CARTESIAN_POINT('',(9.,7.04650450046473,-3.89509618943234));
#45613=CARTESIAN_POINT('',(0.5,6.79829941970784,-3.925));
#45614=CARTESIAN_POINT('',(0.5,6.79829941970784,-3.925));
#45615=CARTESIAN_POINT('',(0.5,7.04650450046473,-3.89509618943234));
#45616=CARTESIAN_POINT('Origin',(0.5,6.88490196008629,-3.975));
#45617=CARTESIAN_POINT('',(0.499999999999999,6.87156884617482,-4.09652799237106));
#45618=CARTESIAN_POINT('Origin',(0.5,0.,0.));
#45619=CARTESIAN_POINT('',(0.5,6.79829941970784,-3.925));
#45620=CARTESIAN_POINT('Origin',(0.5,6.79829941970784,-3.925));
#45621=CARTESIAN_POINT('',(9.,6.87156884617482,-4.09652799237106));
#45622=CARTESIAN_POINT('',(4.75,6.87156884617482,-4.09652799237106));
#45623=CARTESIAN_POINT('',(9.,6.79829941970784,-3.925));
#45624=CARTESIAN_POINT('Origin',(9.,6.88490196008629,-3.975));
#45625=CARTESIAN_POINT('Origin',(9.,0.,0.));
#45626=CARTESIAN_POINT('Origin',(0.5,6.26307590856075,-5.0595335915088));
#45627=CARTESIAN_POINT('',(9.,6.1996920869149,-5.05606744688446));
#45628=CARTESIAN_POINT('',(0.499999999999999,6.1996920869149,-5.05606744688446));
#45629=CARTESIAN_POINT('',(4.75,6.1996920869149,-5.05606744688446));
#45630=CARTESIAN_POINT('',(9.,6.01344887848397,-5.04588273603934));
#45631=CARTESIAN_POINT('',(9.,6.26307590856075,-5.0595335915088));
#45632=CARTESIAN_POINT('',(0.5,6.01344887848397,-5.04588273603934));
#45633=CARTESIAN_POINT('',(0.5,6.01344887848397,-5.04588273603934));
#45634=CARTESIAN_POINT('',(0.5,6.26307590856075,-5.0595335915088));
#45635=CARTESIAN_POINT('Origin',(0.5,6.09005332279587,-5.11016149700799));
#45636=CARTESIAN_POINT('',(0.499999999999999,6.05581965443331,-5.22752793516966));
#45637=CARTESIAN_POINT('Origin',(0.5,0.,0.));
#45638=CARTESIAN_POINT('',(0.5,6.01344887848397,-5.04588273603934));
#45639=CARTESIAN_POINT('Origin',(0.5,6.01344887848397,-5.04588273603934));
#45640=CARTESIAN_POINT('',(9.,6.05581965443331,-5.22752793516966));
#45641=CARTESIAN_POINT('',(4.75,6.05581965443331,-5.22752793516966));
#45642=CARTESIAN_POINT('',(9.,6.01344887848397,-5.04588273603934));
#45643=CARTESIAN_POINT('Origin',(9.,6.09005332279587,-5.11016149700799));
#45644=CARTESIAN_POINT('Origin',(9.,0.,0.));
#45645=CARTESIAN_POINT('Origin',(0.5,5.28934692444449,-6.07023962565479));
#45646=CARTESIAN_POINT('',(9.,5.22752793516966,-6.05581965443332));
#45647=CARTESIAN_POINT('',(0.499999999999999,5.22752793516966,-6.05581965443332));
#45648=CARTESIAN_POINT('',(4.75,5.22752793516966,-6.05581965443332));
#45649=CARTESIAN_POINT('',(9.,5.04588273603933,-6.01344887848398));
#45650=CARTESIAN_POINT('',(9.,5.28934692444449,-6.07023962565479));
#45651=CARTESIAN_POINT('',(0.5,5.04588273603933,-6.01344887848398));
#45652=CARTESIAN_POINT('',(0.5,5.04588273603933,-6.01344887848398));
#45653=CARTESIAN_POINT('',(0.5,5.28934692444449,-6.07023962565479));
#45654=CARTESIAN_POINT('Origin',(0.5,5.11016149700799,-6.09005332279588));
#45655=CARTESIAN_POINT('',(0.499999999999999,5.05606744688446,-6.19969208691491));
#45656=CARTESIAN_POINT('Origin',(0.5,0.,0.));
#45657=CARTESIAN_POINT('',(0.5,5.04588273603933,-6.01344887848398));
#45658=CARTESIAN_POINT('Origin',(0.5,5.04588273603933,-6.01344887848398));
#45659=CARTESIAN_POINT('',(9.,5.05606744688446,-6.19969208691491));
#45660=CARTESIAN_POINT('',(4.75,5.05606744688446,-6.19969208691491));
#45661=CARTESIAN_POINT('',(9.,5.04588273603933,-6.01344887848398));
#45662=CARTESIAN_POINT('Origin',(9.,5.11016149700799,-6.09005332279588));
#45663=CARTESIAN_POINT('Origin',(9.,0.,0.));
#45664=CARTESIAN_POINT('Origin',(0.5,4.15490381056767,-6.89650450046473));
#45665=CARTESIAN_POINT('',(9.,4.09652799237105,-6.87156884617482));
#45666=CARTESIAN_POINT('',(0.499999999999999,4.09652799237105,-6.87156884617482));
#45667=CARTESIAN_POINT('',(4.75,4.09652799237105,-6.87156884617482));
#45668=CARTESIAN_POINT('',(9.,3.925,-6.79829941970784));
#45669=CARTESIAN_POINT('',(9.,4.15490381056767,-6.89650450046473));
#45670=CARTESIAN_POINT('',(0.5,3.925,-6.79829941970784));
#45671=CARTESIAN_POINT('',(0.5,3.925,-6.79829941970784));
#45672=CARTESIAN_POINT('',(0.5,4.15490381056767,-6.89650450046473));
#45673=CARTESIAN_POINT('Origin',(0.5,3.975,-6.88490196008629));
#45674=CARTESIAN_POINT('',(0.499999999999999,3.9026891884556,-6.98348173179481));
#45675=CARTESIAN_POINT('Origin',(0.5,0.,0.));
#45676=CARTESIAN_POINT('',(0.5,3.925,-6.79829941970784));
#45677=CARTESIAN_POINT('Origin',(0.5,3.925,-6.79829941970784));
#45678=CARTESIAN_POINT('',(9.,3.9026891884556,-6.98348173179481));
#45679=CARTESIAN_POINT('',(4.75,3.9026891884556,-6.98348173179481));
#45680=CARTESIAN_POINT('',(9.,3.925,-6.79829941970784));
#45681=CARTESIAN_POINT('Origin',(9.,3.975,-6.88490196008629));
#45682=CARTESIAN_POINT('Origin',(9.,0.,0.));
#45683=CARTESIAN_POINT('Origin',(0.5,2.89421604688952,-7.51322257582772));
#45684=CARTESIAN_POINT('',(9.,2.84105711946744,-7.47852889570692));
#45685=CARTESIAN_POINT('',(0.499999999999999,2.84105711946744,-7.47852889570692));
#45686=CARTESIAN_POINT('',(4.75,2.84105711946744,-7.47852889570692));
#45687=CARTESIAN_POINT('',(9.,2.6848581251065,-7.37658707316938));
#45688=CARTESIAN_POINT('',(9.,2.89421604688952,-7.51322257582772));
#45689=CARTESIAN_POINT('',(0.5,2.6848581251065,-7.37658707316938));
#45690=CARTESIAN_POINT('',(0.5,2.6848581251065,-7.37658707316938));
#45691=CARTESIAN_POINT('',(0.5,2.89421604688952,-7.51322257582772));
#45692=CARTESIAN_POINT('Origin',(0.5,2.71906013943906,-7.47055633524797));
#45693=CARTESIAN_POINT('',(0.499999999999999,2.63072969389152,-7.5550818180664));
#45694=CARTESIAN_POINT('Origin',(0.5,0.,0.));
#45695=CARTESIAN_POINT('',(0.5,2.6848581251065,-7.37658707316938));
#45696=CARTESIAN_POINT('Origin',(0.5,2.6848581251065,-7.37658707316938));
#45697=CARTESIAN_POINT('',(9.,2.63072969389152,-7.5550818180664));
#45698=CARTESIAN_POINT('',(4.75,2.63072969389152,-7.5550818180664));
#45699=CARTESIAN_POINT('',(9.,2.6848581251065,-7.37658707316938));
#45700=CARTESIAN_POINT('Origin',(9.,2.71906013943906,-7.47055633524797));
#45701=CARTESIAN_POINT('Origin',(9.,0.,0.));
#45702=CARTESIAN_POINT('Origin',(0.5,1.54558899317062,-7.90165518509824));
#45703=CARTESIAN_POINT('',(9.,1.49926216363307,-7.85825762906118));
#45704=CARTESIAN_POINT('',(0.499999999999999,1.49926216363307,-7.85825762906118));
#45705=CARTESIAN_POINT('',(4.75,1.49926216363307,-7.85825762906118));
#45706=CARTESIAN_POINT('',(9.,1.3631381946854,-7.73074086114583));
#45707=CARTESIAN_POINT('',(9.,1.54558899317062,-7.90165518509824));
#45708=CARTESIAN_POINT('',(0.5,1.3631381946854,-7.73074086114583));
#45709=CARTESIAN_POINT('',(0.5,1.3631381946854,-7.73074086114583));
#45710=CARTESIAN_POINT('',(0.5,1.54558899317062,-7.90165518509824));
#45711=CARTESIAN_POINT('Origin',(0.5,1.38050301245209,-7.82922163644705));
#45712=CARTESIAN_POINT('',(0.499999999999999,1.27883680879201,-7.8971245663519));
#45713=CARTESIAN_POINT('Origin',(0.5,0.,0.));
#45714=CARTESIAN_POINT('',(0.5,1.3631381946854,-7.73074086114583));
#45715=CARTESIAN_POINT('Origin',(0.5,1.3631381946854,-7.73074086114583));
#45716=CARTESIAN_POINT('',(9.,1.27883680879201,-7.8971245663519));
#45717=CARTESIAN_POINT('',(4.75,1.27883680879201,-7.8971245663519));
#45718=CARTESIAN_POINT('',(9.,1.3631381946854,-7.73074086114583));
#45719=CARTESIAN_POINT('Origin',(9.,1.38050301245209,-7.82922163644705));
#45720=CARTESIAN_POINT('Origin',(9.,0.,0.));
#45721=CARTESIAN_POINT('Origin',(0.5,0.149999999999999,-8.05));
#45722=CARTESIAN_POINT('',(9.,0.111912885619984,-7.99921718082665));
#45723=CARTESIAN_POINT('',(0.499999999999999,0.111912885619984,-7.99921718082665));
#45724=CARTESIAN_POINT('',(4.75,0.111912885619984,-7.99921718082665));
#45725=CARTESIAN_POINT('',(9.,-1.44202160599601E-15,-7.85));
#45726=CARTESIAN_POINT('',(9.,0.149999999999999,-8.05));
#45727=CARTESIAN_POINT('',(0.5,-1.44202160599601E-15,-7.85));
#45728=CARTESIAN_POINT('',(0.5,-1.44202160599601E-15,-7.85));
#45729=CARTESIAN_POINT('',(0.5,0.149999999999999,-8.05));
#45730=CARTESIAN_POINT('Origin',(0.5,-1.46039130798322E-15,-7.95));
#45731=CARTESIAN_POINT('',(0.499999999999999,-0.111912885619986,-7.99921718082665));
#45732=CARTESIAN_POINT('Origin',(0.5,0.,0.));
#45733=CARTESIAN_POINT('',(0.5,-1.44202160599601E-15,-7.85));
#45734=CARTESIAN_POINT('Origin',(0.5,-1.44202160599601E-15,-7.85));
#45735=CARTESIAN_POINT('',(9.,-0.111912885619986,-7.99921718082665));
#45736=CARTESIAN_POINT('',(4.75,-0.111912885619986,-7.99921718082665));
#45737=CARTESIAN_POINT('',(9.,-1.44202160599601E-15,-7.85));
#45738=CARTESIAN_POINT('Origin',(9.,-1.46039130798322E-15,-7.95));
#45739=CARTESIAN_POINT('Origin',(9.,0.,0.));
#45740=CARTESIAN_POINT('Origin',(0.5,-1.25014666726696,-7.95374963839832));
#45741=CARTESIAN_POINT('',(9.,-1.27883680879202,-7.8971245663519));
#45742=CARTESIAN_POINT('',(0.499999999999999,-1.27883680879202,-7.8971245663519));
#45743=CARTESIAN_POINT('',(4.75,-1.27883680879202,-7.8971245663519));
#45744=CARTESIAN_POINT('',(9.,-1.3631381946854,-7.73074086114583));
#45745=CARTESIAN_POINT('',(9.,-1.25014666726696,-7.95374963839832));
#45746=CARTESIAN_POINT('',(0.5,-1.3631381946854,-7.73074086114583));
#45747=CARTESIAN_POINT('',(0.5,-1.3631381946854,-7.73074086114583));
#45748=CARTESIAN_POINT('',(0.5,-1.25014666726696,-7.95374963839832));
#45749=CARTESIAN_POINT('Origin',(0.5,-1.3805030124521,-7.82922163644705));
#45750=CARTESIAN_POINT('',(0.499999999999999,-1.49926216363308,-7.85825762906118));
#45751=CARTESIAN_POINT('Origin',(0.5,0.,0.));
#45752=CARTESIAN_POINT('',(0.5,-1.3631381946854,-7.73074086114583));
#45753=CARTESIAN_POINT('Origin',(0.5,-1.3631381946854,-7.73074086114583));
#45754=CARTESIAN_POINT('',(9.,-1.49926216363308,-7.85825762906118));
#45755=CARTESIAN_POINT('',(4.75,-1.49926216363308,-7.85825762906118));
#45756=CARTESIAN_POINT('',(9.,-1.3631381946854,-7.73074086114583));
#45757=CARTESIAN_POINT('Origin',(9.,-1.3805030124521,-7.82922163644705));
#45758=CARTESIAN_POINT('Origin',(9.,0.,0.));
#45759=CARTESIAN_POINT('Origin',(0.5,-2.61230826065375,-7.61582861882541));
#45760=CARTESIAN_POINT('',(9.,-2.63072969389153,-7.55508181806639));
#45761=CARTESIAN_POINT('',(0.499999999999999,-2.63072969389153,-7.55508181806639));
#45762=CARTESIAN_POINT('',(4.75,-2.63072969389153,-7.55508181806639));
#45763=CARTESIAN_POINT('',(9.,-2.6848581251065,-7.37658707316938));
#45764=CARTESIAN_POINT('',(9.,-2.61230826065375,-7.61582861882541));
#45765=CARTESIAN_POINT('',(0.5,-2.6848581251065,-7.37658707316938));
#45766=CARTESIAN_POINT('',(0.5,-2.6848581251065,-7.37658707316938));
#45767=CARTESIAN_POINT('',(0.5,-2.61230826065375,-7.61582861882541));
#45768=CARTESIAN_POINT('Origin',(0.5,-2.71906013943907,-7.47055633524797));
#45769=CARTESIAN_POINT('',(0.499999999999999,-2.84105711946745,-7.47852889570692));
#45770=CARTESIAN_POINT('Origin',(0.5,0.,0.));
#45771=CARTESIAN_POINT('',(0.5,-2.6848581251065,-7.37658707316938));
#45772=CARTESIAN_POINT('Origin',(0.5,-2.6848581251065,-7.37658707316938));
#45773=CARTESIAN_POINT('',(9.,-2.84105711946745,-7.47852889570692));
#45774=CARTESIAN_POINT('',(4.75,-2.84105711946744,-7.47852889570692));
#45775=CARTESIAN_POINT('',(9.,-2.6848581251065,-7.37658707316938));
#45776=CARTESIAN_POINT('Origin',(9.,-2.71906013943907,-7.47055633524797));
#45777=CARTESIAN_POINT('Origin',(9.,0.,0.));
#45778=CARTESIAN_POINT('Origin',(0.5,-3.89509618943234,-7.04650450046473));
#45779=CARTESIAN_POINT('',(9.,-3.9026891884556,-6.98348173179481));
#45780=CARTESIAN_POINT('',(0.499999999999999,-3.9026891884556,-6.98348173179481));
#45781=CARTESIAN_POINT('',(4.75,-3.9026891884556,-6.98348173179481));
#45782=CARTESIAN_POINT('',(9.,-3.925,-6.79829941970784));
#45783=CARTESIAN_POINT('',(9.,-3.89509618943234,-7.04650450046473));
#45784=CARTESIAN_POINT('',(0.5,-3.925,-6.79829941970784));
#45785=CARTESIAN_POINT('',(0.5,-3.925,-6.79829941970784));
#45786=CARTESIAN_POINT('',(0.5,-3.89509618943234,-7.04650450046473));
#45787=CARTESIAN_POINT('Origin',(0.5,-3.975,-6.88490196008629));
#45788=CARTESIAN_POINT('',(0.499999999999999,-4.09652799237106,-6.87156884617482));
#45789=CARTESIAN_POINT('Origin',(0.5,0.,0.));
#45790=CARTESIAN_POINT('',(0.5,-3.925,-6.79829941970784));
#45791=CARTESIAN_POINT('Origin',(0.5,-3.925,-6.79829941970784));
#45792=CARTESIAN_POINT('',(9.,-4.09652799237106,-6.87156884617482));
#45793=CARTESIAN_POINT('',(4.75,-4.09652799237106,-6.87156884617482));
#45794=CARTESIAN_POINT('',(9.,-3.925,-6.79829941970784));
#45795=CARTESIAN_POINT('Origin',(9.,-3.975,-6.88490196008629));
#45796=CARTESIAN_POINT('Origin',(9.,0.,0.));
#45797=CARTESIAN_POINT('Origin',(0.5,-5.0595335915088,-6.26307590856075));
#45798=CARTESIAN_POINT('',(9.,-5.05606744688446,-6.1996920869149));
#45799=CARTESIAN_POINT('',(0.499999999999999,-5.05606744688446,-6.1996920869149));
#45800=CARTESIAN_POINT('',(4.75,-5.05606744688446,-6.1996920869149));
#45801=CARTESIAN_POINT('',(9.,-5.04588273603933,-6.01344887848398));
#45802=CARTESIAN_POINT('',(9.,-5.0595335915088,-6.26307590856075));
#45803=CARTESIAN_POINT('',(0.5,-5.04588273603933,-6.01344887848398));
#45804=CARTESIAN_POINT('',(0.5,-5.04588273603933,-6.01344887848398));
#45805=CARTESIAN_POINT('',(0.5,-5.0595335915088,-6.26307590856075));
#45806=CARTESIAN_POINT('Origin',(0.5,-5.11016149700799,-6.09005332279587));
#45807=CARTESIAN_POINT('',(0.499999999999999,-5.22752793516966,-6.05581965443332));
#45808=CARTESIAN_POINT('Origin',(0.5,0.,0.));
#45809=CARTESIAN_POINT('',(0.5,-5.04588273603933,-6.01344887848398));
#45810=CARTESIAN_POINT('Origin',(0.5,-5.04588273603933,-6.01344887848398));
#45811=CARTESIAN_POINT('',(9.,-5.22752793516966,-6.05581965443332));
#45812=CARTESIAN_POINT('',(4.75,-5.22752793516966,-6.05581965443332));
#45813=CARTESIAN_POINT('',(9.,-5.04588273603933,-6.01344887848398));
#45814=CARTESIAN_POINT('Origin',(9.,-5.11016149700799,-6.09005332279587));
#45815=CARTESIAN_POINT('Origin',(9.,0.,0.));
#45816=CARTESIAN_POINT('Origin',(0.5,-6.07023962565479,-5.28934692444449));
#45817=CARTESIAN_POINT('',(9.,-6.05581965443332,-5.22752793516966));
#45818=CARTESIAN_POINT('',(0.499999999999999,-6.05581965443332,-5.22752793516966));
#45819=CARTESIAN_POINT('',(4.75,-6.05581965443332,-5.22752793516966));
#45820=CARTESIAN_POINT('',(9.,-6.01344887848398,-5.04588273603933));
#45821=CARTESIAN_POINT('',(9.,-6.07023962565479,-5.28934692444449));
#45822=CARTESIAN_POINT('',(0.5,-6.01344887848398,-5.04588273603933));
#45823=CARTESIAN_POINT('',(0.5,-6.01344887848398,-5.04588273603933));
#45824=CARTESIAN_POINT('',(0.5,-6.07023962565479,-5.28934692444449));
#45825=CARTESIAN_POINT('Origin',(0.5,-6.09005332279588,-5.11016149700799));
#45826=CARTESIAN_POINT('',(0.499999999999999,-6.1996920869149,-5.05606744688446));
#45827=CARTESIAN_POINT('Origin',(0.5,0.,0.));
#45828=CARTESIAN_POINT('',(0.5,-6.01344887848398,-5.04588273603933));
#45829=CARTESIAN_POINT('Origin',(0.5,-6.01344887848398,-5.04588273603933));
#45830=CARTESIAN_POINT('',(9.,-6.1996920869149,-5.05606744688446));
#45831=CARTESIAN_POINT('',(4.75,-6.1996920869149,-5.05606744688446));
#45832=CARTESIAN_POINT('',(9.,-6.01344887848398,-5.04588273603933));
#45833=CARTESIAN_POINT('Origin',(9.,-6.09005332279588,-5.11016149700799));
#45834=CARTESIAN_POINT('Origin',(9.,0.,0.));
#45835=CARTESIAN_POINT('Origin',(0.5,-6.89650450046473,-4.15490381056766));
#45836=CARTESIAN_POINT('',(9.,-6.87156884617482,-4.09652799237105));
#45837=CARTESIAN_POINT('',(0.499999999999999,-6.87156884617482,-4.09652799237105));
#45838=CARTESIAN_POINT('',(4.75,-6.87156884617482,-4.09652799237105));
#45839=CARTESIAN_POINT('',(9.,-6.79829941970784,-3.925));
#45840=CARTESIAN_POINT('',(9.,-6.89650450046473,-4.15490381056766));
#45841=CARTESIAN_POINT('',(0.5,-6.79829941970784,-3.925));
#45842=CARTESIAN_POINT('',(0.5,-6.79829941970784,-3.925));
#45843=CARTESIAN_POINT('',(0.5,-6.89650450046473,-4.15490381056766));
#45844=CARTESIAN_POINT('Origin',(0.5,-6.88490196008629,-3.975));
#45845=CARTESIAN_POINT('',(0.499999999999999,-6.98348173179481,-3.90268918845559));
#45846=CARTESIAN_POINT('Origin',(0.5,0.,0.));
#45847=CARTESIAN_POINT('',(0.5,-6.79829941970784,-3.925));
#45848=CARTESIAN_POINT('Origin',(0.5,-6.79829941970784,-3.925));
#45849=CARTESIAN_POINT('',(9.,-6.98348173179481,-3.90268918845559));
#45850=CARTESIAN_POINT('',(4.75,-6.98348173179481,-3.90268918845559));
#45851=CARTESIAN_POINT('',(9.,-6.79829941970784,-3.925));
#45852=CARTESIAN_POINT('Origin',(9.,-6.88490196008629,-3.975));
#45853=CARTESIAN_POINT('Origin',(9.,0.,0.));
#45854=CARTESIAN_POINT('Origin',(0.5,-7.51322257582771,-2.89421604688952));
#45855=CARTESIAN_POINT('',(9.,-7.47852889570692,-2.84105711946744));
#45856=CARTESIAN_POINT('',(0.499999999999999,-7.47852889570692,-2.84105711946744));
#45857=CARTESIAN_POINT('',(4.75,-7.47852889570692,-2.84105711946744));
#45858=CARTESIAN_POINT('',(9.,-7.37658707316938,-2.6848581251065));
#45859=CARTESIAN_POINT('',(9.,-7.51322257582771,-2.89421604688952));
#45860=CARTESIAN_POINT('',(0.5,-7.37658707316938,-2.6848581251065));
#45861=CARTESIAN_POINT('',(0.5,-7.37658707316938,-2.6848581251065));
#45862=CARTESIAN_POINT('',(0.5,-7.51322257582771,-2.89421604688952));
#45863=CARTESIAN_POINT('Origin',(0.5,-7.47055633524797,-2.71906013943907));
#45864=CARTESIAN_POINT('',(0.499999999999999,-7.55508181806639,-2.63072969389152));
#45865=CARTESIAN_POINT('Origin',(0.5,0.,0.));
#45866=CARTESIAN_POINT('',(0.5,-7.37658707316938,-2.6848581251065));
#45867=CARTESIAN_POINT('Origin',(0.5,-7.37658707316938,-2.6848581251065));
#45868=CARTESIAN_POINT('',(9.,-7.55508181806639,-2.63072969389152));
#45869=CARTESIAN_POINT('',(4.75,-7.55508181806639,-2.63072969389152));
#45870=CARTESIAN_POINT('',(9.,-7.37658707316938,-2.6848581251065));
#45871=CARTESIAN_POINT('Origin',(9.,-7.47055633524797,-2.71906013943907));
#45872=CARTESIAN_POINT('Origin',(9.,0.,0.));
#45873=CARTESIAN_POINT('Origin',(0.5,-7.90165518509824,-1.54558899317062));
#45874=CARTESIAN_POINT('',(9.,-7.85825762906118,-1.49926216363307));
#45875=CARTESIAN_POINT('',(0.499999999999999,-7.85825762906118,-1.49926216363307));
#45876=CARTESIAN_POINT('',(4.75,-7.85825762906118,-1.49926216363307));
#45877=CARTESIAN_POINT('',(9.,-7.73074086114583,-1.3631381946854));
#45878=CARTESIAN_POINT('',(9.,-7.90165518509824,-1.54558899317062));
#45879=CARTESIAN_POINT('',(0.5,-7.73074086114583,-1.3631381946854));
#45880=CARTESIAN_POINT('',(0.5,-7.73074086114583,-1.3631381946854));
#45881=CARTESIAN_POINT('',(0.5,-7.90165518509824,-1.54558899317062));
#45882=CARTESIAN_POINT('Origin',(0.5,-7.82922163644705,-1.38050301245209));
#45883=CARTESIAN_POINT('',(0.499999999999999,-7.8971245663519,-1.27883680879201));
#45884=CARTESIAN_POINT('Origin',(0.5,0.,0.));
#45885=CARTESIAN_POINT('',(0.5,-7.73074086114583,-1.3631381946854));
#45886=CARTESIAN_POINT('Origin',(0.5,-7.73074086114583,-1.3631381946854));
#45887=CARTESIAN_POINT('',(9.,-7.8971245663519,-1.27883680879201));
#45888=CARTESIAN_POINT('',(4.75,-7.8971245663519,-1.27883680879201));
#45889=CARTESIAN_POINT('',(9.,-7.73074086114583,-1.3631381946854));
#45890=CARTESIAN_POINT('Origin',(9.,-7.82922163644705,-1.38050301245209));
#45891=CARTESIAN_POINT('Origin',(9.,0.,0.));
#45892=CARTESIAN_POINT('Origin',(0.5,-8.05,-0.149999999999999));
#45893=CARTESIAN_POINT('',(9.,-7.99921718082665,-0.111912885619986));
#45894=CARTESIAN_POINT('',(0.499999999999999,-7.99921718082665,-0.111912885619986));
#45895=CARTESIAN_POINT('',(4.75,-7.99921718082665,-0.111912885619986));
#45896=CARTESIAN_POINT('',(9.,-7.85,9.61347737330672E-16));
#45897=CARTESIAN_POINT('',(9.,-8.05,-0.149999999999999));
#45898=CARTESIAN_POINT('',(0.5,-7.85,9.61347737330672E-16));
#45899=CARTESIAN_POINT('',(0.5,-7.85,9.61347737330672E-16));
#45900=CARTESIAN_POINT('',(0.5,-8.05,-0.149999999999999));
#45901=CARTESIAN_POINT('Origin',(0.5,-7.95,9.73594205322146E-16));
#45902=CARTESIAN_POINT('',(0.5,-8.,-9.79717439317883E-16));
#45903=CARTESIAN_POINT('Origin',(0.5,0.,0.));
#45904=CARTESIAN_POINT('',(0.499999999999999,-7.99921718082665,0.111912885619986));
#45905=CARTESIAN_POINT('',(0.5,-7.85,9.61347737330672E-16));
#45906=CARTESIAN_POINT('Origin',(0.5,0.,0.));
#45907=CARTESIAN_POINT('Origin',(0.5,-7.85,9.61347737330672E-16));
#45908=CARTESIAN_POINT('',(9.,-7.99921718082665,0.111912885619986));
#45909=CARTESIAN_POINT('',(4.75,-7.99921718082665,0.111912885619986));
#45910=CARTESIAN_POINT('',(9.,-7.85,9.61347737330672E-16));
#45911=CARTESIAN_POINT('Origin',(9.,-7.95,9.73594205322146E-16));
#45912=CARTESIAN_POINT('',(9.,-8.,-9.79717439317883E-16));
#45913=CARTESIAN_POINT('Origin',(9.,0.,0.));
#45914=CARTESIAN_POINT('Origin',(9.,0.,0.));
#45915=CARTESIAN_POINT('Origin',(0.5,-7.95374963839832,1.25014666726696));
#45916=CARTESIAN_POINT('',(9.,-7.8971245663519,1.27883680879202));
#45917=CARTESIAN_POINT('',(0.499999999999999,-7.8971245663519,1.27883680879202));
#45918=CARTESIAN_POINT('',(4.75,-7.8971245663519,1.27883680879202));
#45919=CARTESIAN_POINT('',(9.,-7.73074086114583,1.36313819468541));
#45920=CARTESIAN_POINT('',(9.,-7.95374963839832,1.25014666726696));
#45921=CARTESIAN_POINT('',(0.5,-7.73074086114583,1.36313819468541));
#45922=CARTESIAN_POINT('',(0.5,-7.73074086114583,1.36313819468541));
#45923=CARTESIAN_POINT('',(0.5,-7.95374963839832,1.25014666726696));
#45924=CARTESIAN_POINT('Origin',(0.5,-7.82922163644705,1.3805030124521));
#45925=CARTESIAN_POINT('',(0.499999999999999,-7.85825762906118,1.49926216363308));
#45926=CARTESIAN_POINT('Origin',(0.5,0.,0.));
#45927=CARTESIAN_POINT('',(0.5,-7.73074086114583,1.36313819468541));
#45928=CARTESIAN_POINT('Origin',(0.5,-7.73074086114583,1.36313819468541));
#45929=CARTESIAN_POINT('',(9.,-7.85825762906118,1.49926216363308));
#45930=CARTESIAN_POINT('',(4.75,-7.85825762906118,1.49926216363308));
#45931=CARTESIAN_POINT('',(9.,-7.73074086114583,1.36313819468541));
#45932=CARTESIAN_POINT('Origin',(9.,-7.82922163644705,1.3805030124521));
#45933=CARTESIAN_POINT('Origin',(9.,0.,0.));
#45934=CARTESIAN_POINT('Origin',(0.5,-7.61582861882541,2.61230826065375));
#45935=CARTESIAN_POINT('',(9.,-7.55508181806639,2.63072969389153));
#45936=CARTESIAN_POINT('',(0.499999999999999,-7.55508181806639,2.63072969389153));
#45937=CARTESIAN_POINT('',(4.75,-7.55508181806639,2.63072969389153));
#45938=CARTESIAN_POINT('',(9.,-7.37658707316938,2.6848581251065));
#45939=CARTESIAN_POINT('',(9.,-7.61582861882541,2.61230826065375));
#45940=CARTESIAN_POINT('',(0.5,-7.37658707316938,2.6848581251065));
#45941=CARTESIAN_POINT('',(0.5,-7.37658707316938,2.6848581251065));
#45942=CARTESIAN_POINT('',(0.5,-7.61582861882541,2.61230826065375));
#45943=CARTESIAN_POINT('Origin',(0.5,-7.47055633524797,2.71906013943907));
#45944=CARTESIAN_POINT('',(0.499999999999999,-7.47852889570692,2.84105711946744));
#45945=CARTESIAN_POINT('Origin',(0.5,0.,0.));
#45946=CARTESIAN_POINT('',(0.5,-7.37658707316938,2.6848581251065));
#45947=CARTESIAN_POINT('Origin',(0.5,-7.37658707316938,2.6848581251065));
#45948=CARTESIAN_POINT('',(9.,-7.47852889570692,2.84105711946744));
#45949=CARTESIAN_POINT('',(4.75,-7.47852889570692,2.84105711946744));
#45950=CARTESIAN_POINT('',(9.,-7.37658707316938,2.6848581251065));
#45951=CARTESIAN_POINT('Origin',(9.,-7.47055633524797,2.71906013943907));
#45952=CARTESIAN_POINT('Origin',(9.,0.,0.));
#45953=CARTESIAN_POINT('Origin',(0.5,-7.04650450046473,3.89509618943233));
#45954=CARTESIAN_POINT('',(9.,-6.98348173179481,3.90268918845559));
#45955=CARTESIAN_POINT('',(0.499999999999999,-6.98348173179481,3.90268918845559));
#45956=CARTESIAN_POINT('',(4.75,-6.98348173179481,3.90268918845559));
#45957=CARTESIAN_POINT('',(9.,-6.79829941970784,3.925));
#45958=CARTESIAN_POINT('',(9.,-7.04650450046473,3.89509618943233));
#45959=CARTESIAN_POINT('',(0.5,-6.79829941970784,3.925));
#45960=CARTESIAN_POINT('',(0.5,-6.79829941970784,3.925));
#45961=CARTESIAN_POINT('',(0.5,-7.04650450046473,3.89509618943233));
#45962=CARTESIAN_POINT('Origin',(0.5,-6.88490196008629,3.975));
#45963=CARTESIAN_POINT('',(0.499999999999999,-6.87156884617482,4.09652799237105));
#45964=CARTESIAN_POINT('Origin',(0.5,0.,0.));
#45965=CARTESIAN_POINT('',(0.5,-6.79829941970784,3.925));
#45966=CARTESIAN_POINT('Origin',(0.5,-6.79829941970784,3.925));
#45967=CARTESIAN_POINT('',(9.,-6.87156884617482,4.09652799237105));
#45968=CARTESIAN_POINT('',(4.75,-6.87156884617482,4.09652799237105));
#45969=CARTESIAN_POINT('',(9.,-6.79829941970784,3.925));
#45970=CARTESIAN_POINT('Origin',(9.,-6.88490196008629,3.975));
#45971=CARTESIAN_POINT('Origin',(9.,0.,0.));
#45972=CARTESIAN_POINT('Origin',(0.5,-6.26307590856075,5.0595335915088));
#45973=CARTESIAN_POINT('',(9.,-6.1996920869149,5.05606744688446));
#45974=CARTESIAN_POINT('',(0.499999999999999,-6.1996920869149,5.05606744688446));
#45975=CARTESIAN_POINT('',(4.75,-6.1996920869149,5.05606744688446));
#45976=CARTESIAN_POINT('',(9.,-6.01344887848398,5.04588273603933));
#45977=CARTESIAN_POINT('',(9.,-6.26307590856075,5.0595335915088));
#45978=CARTESIAN_POINT('',(0.5,-6.01344887848398,5.04588273603933));
#45979=CARTESIAN_POINT('',(0.5,-6.01344887848398,5.04588273603933));
#45980=CARTESIAN_POINT('',(0.5,-6.26307590856075,5.0595335915088));
#45981=CARTESIAN_POINT('Origin',(0.5,-6.09005332279587,5.11016149700799));
#45982=CARTESIAN_POINT('',(0.499999999999999,-6.05581965443332,5.22752793516966));
#45983=CARTESIAN_POINT('Origin',(0.5,0.,0.));
#45984=CARTESIAN_POINT('',(0.5,-6.01344887848398,5.04588273603933));
#45985=CARTESIAN_POINT('Origin',(0.5,-6.01344887848398,5.04588273603933));
#45986=CARTESIAN_POINT('',(9.,-6.05581965443332,5.22752793516966));
#45987=CARTESIAN_POINT('',(4.75,-6.05581965443332,5.22752793516966));
#45988=CARTESIAN_POINT('',(9.,-6.01344887848398,5.04588273603933));
#45989=CARTESIAN_POINT('Origin',(9.,-6.09005332279587,5.11016149700799));
#45990=CARTESIAN_POINT('Origin',(9.,0.,0.));
#45991=CARTESIAN_POINT('Origin',(0.5,-5.28934692444449,6.07023962565479));
#45992=CARTESIAN_POINT('',(9.,-5.22752793516966,6.05581965443332));
#45993=CARTESIAN_POINT('',(0.499999999999999,-5.22752793516966,6.05581965443332));
#45994=CARTESIAN_POINT('',(4.75,-5.22752793516966,6.05581965443332));
#45995=CARTESIAN_POINT('',(9.,-5.04588273603933,6.01344887848398));
#45996=CARTESIAN_POINT('',(9.,-5.28934692444449,6.07023962565479));
#45997=CARTESIAN_POINT('',(0.5,-5.04588273603933,6.01344887848398));
#45998=CARTESIAN_POINT('',(0.5,-5.04588273603933,6.01344887848398));
#45999=CARTESIAN_POINT('',(0.5,-5.28934692444449,6.07023962565479));
#46000=CARTESIAN_POINT('Origin',(0.5,-5.11016149700799,6.09005332279587));
#46001=CARTESIAN_POINT('',(0.499999999999999,-5.05606744688446,6.1996920869149));
#46002=CARTESIAN_POINT('Origin',(0.5,0.,0.));
#46003=CARTESIAN_POINT('',(0.5,-5.04588273603933,6.01344887848398));
#46004=CARTESIAN_POINT('Origin',(0.5,-5.04588273603933,6.01344887848398));
#46005=CARTESIAN_POINT('',(9.,-5.05606744688446,6.1996920869149));
#46006=CARTESIAN_POINT('',(4.75,-5.05606744688446,6.1996920869149));
#46007=CARTESIAN_POINT('',(9.,-5.04588273603933,6.01344887848398));
#46008=CARTESIAN_POINT('Origin',(9.,-5.11016149700799,6.09005332279587));
#46009=CARTESIAN_POINT('Origin',(9.,0.,0.));
#46010=CARTESIAN_POINT('Origin',(0.5,-4.15490381056767,6.89650450046473));
#46011=CARTESIAN_POINT('',(9.,-4.09652799237105,6.87156884617482));
#46012=CARTESIAN_POINT('',(0.499999999999999,-4.09652799237105,6.87156884617482));
#46013=CARTESIAN_POINT('',(4.75,-4.09652799237105,6.87156884617482));
#46014=CARTESIAN_POINT('',(9.,-3.925,6.79829941970784));
#46015=CARTESIAN_POINT('',(9.,-4.15490381056767,6.89650450046473));
#46016=CARTESIAN_POINT('',(0.5,-3.925,6.79829941970784));
#46017=CARTESIAN_POINT('',(0.5,-3.925,6.79829941970784));
#46018=CARTESIAN_POINT('',(0.5,-4.15490381056767,6.89650450046473));
#46019=CARTESIAN_POINT('Origin',(0.5,-3.975,6.88490196008629));
#46020=CARTESIAN_POINT('',(0.499999999999999,-3.90268918845559,6.98348173179481));
#46021=CARTESIAN_POINT('Origin',(0.5,0.,0.));
#46022=CARTESIAN_POINT('',(0.5,-3.925,6.79829941970784));
#46023=CARTESIAN_POINT('Origin',(0.5,-3.925,6.79829941970784));
#46024=CARTESIAN_POINT('',(9.,-3.90268918845559,6.98348173179481));
#46025=CARTESIAN_POINT('',(4.75,-3.90268918845559,6.98348173179481));
#46026=CARTESIAN_POINT('',(9.,-3.925,6.79829941970784));
#46027=CARTESIAN_POINT('Origin',(9.,-3.975,6.88490196008629));
#46028=CARTESIAN_POINT('Origin',(9.,0.,0.));
#46029=CARTESIAN_POINT('Origin',(0.5,-2.89421604688952,7.51322257582771));
#46030=CARTESIAN_POINT('',(9.,-2.84105711946744,7.47852889570692));
#46031=CARTESIAN_POINT('',(0.499999999999999,-2.84105711946744,7.47852889570692));
#46032=CARTESIAN_POINT('',(4.75,-2.84105711946744,7.47852889570692));
#46033=CARTESIAN_POINT('',(9.,-2.6848581251065,7.37658707316938));
#46034=CARTESIAN_POINT('',(9.,-2.89421604688952,7.51322257582771));
#46035=CARTESIAN_POINT('',(0.5,-2.6848581251065,7.37658707316938));
#46036=CARTESIAN_POINT('',(0.5,-2.6848581251065,7.37658707316938));
#46037=CARTESIAN_POINT('',(0.5,-2.89421604688952,7.51322257582771));
#46038=CARTESIAN_POINT('Origin',(0.5,-2.71906013943907,7.47055633524797));
#46039=CARTESIAN_POINT('',(0.499999999999999,-2.63072969389152,7.55508181806639));
#46040=CARTESIAN_POINT('Origin',(0.5,0.,0.));
#46041=CARTESIAN_POINT('',(0.5,-2.6848581251065,7.37658707316938));
#46042=CARTESIAN_POINT('Origin',(0.5,-2.6848581251065,7.37658707316938));
#46043=CARTESIAN_POINT('',(9.,-2.63072969389152,7.55508181806639));
#46044=CARTESIAN_POINT('',(4.75,-2.63072969389152,7.55508181806639));
#46045=CARTESIAN_POINT('',(9.,-2.6848581251065,7.37658707316938));
#46046=CARTESIAN_POINT('Origin',(9.,-2.71906013943907,7.47055633524797));
#46047=CARTESIAN_POINT('Origin',(9.,0.,0.));
#46048=CARTESIAN_POINT('Origin',(0.5,-1.54558899317062,7.90165518509824));
#46049=CARTESIAN_POINT('',(9.,-1.49926216363308,7.85825762906118));
#46050=CARTESIAN_POINT('',(0.499999999999999,-1.49926216363308,7.85825762906118));
#46051=CARTESIAN_POINT('',(4.75,-1.49926216363308,7.85825762906118));
#46052=CARTESIAN_POINT('',(9.,-1.3631381946854,7.73074086114583));
#46053=CARTESIAN_POINT('',(9.,-1.54558899317062,7.90165518509824));
#46054=CARTESIAN_POINT('',(0.5,-1.3631381946854,7.73074086114583));
#46055=CARTESIAN_POINT('',(0.5,-1.3631381946854,7.73074086114583));
#46056=CARTESIAN_POINT('',(0.5,-1.54558899317062,7.90165518509824));
#46057=CARTESIAN_POINT('Origin',(0.5,-1.3805030124521,7.82922163644705));
#46058=CARTESIAN_POINT('',(0.499999999999999,-1.27883680879202,7.8971245663519));
#46059=CARTESIAN_POINT('Origin',(0.5,0.,0.));
#46060=CARTESIAN_POINT('',(0.5,-1.3631381946854,7.73074086114583));
#46061=CARTESIAN_POINT('Origin',(0.5,-1.3631381946854,7.73074086114583));
#46062=CARTESIAN_POINT('',(9.,-1.27883680879202,7.8971245663519));
#46063=CARTESIAN_POINT('',(4.75,-1.27883680879202,7.8971245663519));
#46064=CARTESIAN_POINT('',(9.,-1.3631381946854,7.73074086114583));
#46065=CARTESIAN_POINT('Origin',(9.,-1.3805030124521,7.82922163644705));
#46066=CARTESIAN_POINT('Origin',(9.,0.,0.));
#46067=CARTESIAN_POINT('Origin',(0.5,-0.15,8.05));
#46068=CARTESIAN_POINT('',(9.,-0.111912885619985,7.99921718082665));
#46069=CARTESIAN_POINT('',(0.499999999999999,-0.111912885619985,7.99921718082665));
#46070=CARTESIAN_POINT('',(4.75,-0.111912885619985,7.99921718082665));
#46071=CARTESIAN_POINT('',(9.,4.80673868665336E-16,7.85));
#46072=CARTESIAN_POINT('',(9.,-0.15,8.05));
#46073=CARTESIAN_POINT('',(0.5,4.80673868665336E-16,7.85));
#46074=CARTESIAN_POINT('',(0.5,4.80673868665336E-16,7.85));
#46075=CARTESIAN_POINT('',(0.5,-0.15,8.05));
#46076=CARTESIAN_POINT('Origin',(0.5,4.86797102661073E-16,7.95));
#46077=CARTESIAN_POINT('',(0.499999999999999,0.111912885619987,7.99921718082665));
#46078=CARTESIAN_POINT('Origin',(0.5,0.,0.));
#46079=CARTESIAN_POINT('',(0.5,4.80673868665336E-16,7.85));
#46080=CARTESIAN_POINT('Origin',(0.5,4.80673868665336E-16,7.85));
#46081=CARTESIAN_POINT('',(9.,0.111912885619987,7.99921718082665));
#46082=CARTESIAN_POINT('',(4.75,0.111912885619987,7.99921718082665));
#46083=CARTESIAN_POINT('',(9.,4.80673868665336E-16,7.85));
#46084=CARTESIAN_POINT('Origin',(9.,4.86797102661073E-16,7.95));
#46085=CARTESIAN_POINT('Origin',(9.,0.,0.));
#46086=CARTESIAN_POINT('Origin',(0.5,1.25014666726696,7.95374963839832));
#46087=CARTESIAN_POINT('',(9.,1.27883680879202,7.8971245663519));
#46088=CARTESIAN_POINT('',(0.499999999999999,1.27883680879202,7.8971245663519));
#46089=CARTESIAN_POINT('',(4.75,1.27883680879202,7.8971245663519));
#46090=CARTESIAN_POINT('',(9.,1.3631381946854,7.73074086114583));
#46091=CARTESIAN_POINT('',(9.,1.25014666726696,7.95374963839832));
#46092=CARTESIAN_POINT('',(0.5,1.3631381946854,7.73074086114583));
#46093=CARTESIAN_POINT('',(0.5,1.3631381946854,7.73074086114583));
#46094=CARTESIAN_POINT('',(0.5,1.25014666726696,7.95374963839832));
#46095=CARTESIAN_POINT('Origin',(0.5,1.3805030124521,7.82922163644705));
#46096=CARTESIAN_POINT('',(0.499999999999999,1.49926216363308,7.85825762906118));
#46097=CARTESIAN_POINT('Origin',(0.5,0.,0.));
#46098=CARTESIAN_POINT('',(0.5,1.3631381946854,7.73074086114583));
#46099=CARTESIAN_POINT('Origin',(0.5,1.3631381946854,7.73074086114583));
#46100=CARTESIAN_POINT('',(9.,1.49926216363308,7.85825762906118));
#46101=CARTESIAN_POINT('',(4.75,1.49926216363308,7.85825762906118));
#46102=CARTESIAN_POINT('',(9.,1.3631381946854,7.73074086114583));
#46103=CARTESIAN_POINT('Origin',(9.,1.3805030124521,7.82922163644705));
#46104=CARTESIAN_POINT('Origin',(9.,0.,0.));
#46105=CARTESIAN_POINT('Origin',(0.5,2.61230826065375,7.61582861882541));
#46106=CARTESIAN_POINT('',(9.,2.63072969389153,7.55508181806639));
#46107=CARTESIAN_POINT('',(0.499999999999999,2.63072969389153,7.55508181806639));
#46108=CARTESIAN_POINT('',(4.75,2.63072969389153,7.55508181806639));
#46109=CARTESIAN_POINT('',(9.,2.6848581251065,7.37658707316938));
#46110=CARTESIAN_POINT('',(9.,2.61230826065375,7.61582861882541));
#46111=CARTESIAN_POINT('',(0.5,2.6848581251065,7.37658707316938));
#46112=CARTESIAN_POINT('',(0.5,2.6848581251065,7.37658707316938));
#46113=CARTESIAN_POINT('',(0.5,2.61230826065375,7.61582861882541));
#46114=CARTESIAN_POINT('Origin',(0.5,2.71906013943907,7.47055633524797));
#46115=CARTESIAN_POINT('',(0.499999999999999,2.84105711946744,7.47852889570692));
#46116=CARTESIAN_POINT('Origin',(0.5,0.,0.));
#46117=CARTESIAN_POINT('',(0.5,2.6848581251065,7.37658707316938));
#46118=CARTESIAN_POINT('Origin',(0.5,2.6848581251065,7.37658707316938));
#46119=CARTESIAN_POINT('',(9.,2.84105711946744,7.47852889570692));
#46120=CARTESIAN_POINT('',(4.75,2.84105711946744,7.47852889570692));
#46121=CARTESIAN_POINT('',(9.,2.6848581251065,7.37658707316938));
#46122=CARTESIAN_POINT('Origin',(9.,2.71906013943907,7.47055633524797));
#46123=CARTESIAN_POINT('Origin',(9.,0.,0.));
#46124=CARTESIAN_POINT('Origin',(0.5,3.89509618943234,7.04650450046473));
#46125=CARTESIAN_POINT('',(9.,3.9026891884556,6.98348173179481));
#46126=CARTESIAN_POINT('',(0.499999999999999,3.9026891884556,6.98348173179481));
#46127=CARTESIAN_POINT('',(4.75,3.9026891884556,6.98348173179481));
#46128=CARTESIAN_POINT('',(9.,3.925,6.79829941970784));
#46129=CARTESIAN_POINT('',(9.,3.89509618943234,7.04650450046473));
#46130=CARTESIAN_POINT('',(0.5,3.925,6.79829941970784));
#46131=CARTESIAN_POINT('',(0.5,3.925,6.79829941970784));
#46132=CARTESIAN_POINT('',(0.5,3.89509618943234,7.04650450046473));
#46133=CARTESIAN_POINT('Origin',(0.5,3.975,6.88490196008629));
#46134=CARTESIAN_POINT('',(0.499999999999999,4.09652799237105,6.87156884617482));
#46135=CARTESIAN_POINT('Origin',(0.5,0.,0.));
#46136=CARTESIAN_POINT('',(0.5,3.925,6.79829941970784));
#46137=CARTESIAN_POINT('Origin',(0.5,3.925,6.79829941970784));
#46138=CARTESIAN_POINT('',(9.,4.09652799237105,6.87156884617482));
#46139=CARTESIAN_POINT('',(4.75,4.09652799237105,6.87156884617482));
#46140=CARTESIAN_POINT('',(9.,3.925,6.79829941970784));
#46141=CARTESIAN_POINT('Origin',(9.,3.975,6.88490196008629));
#46142=CARTESIAN_POINT('Origin',(9.,0.,0.));
#46143=CARTESIAN_POINT('Origin',(0.5,5.0595335915088,6.26307590856075));
#46144=CARTESIAN_POINT('',(9.,5.05606744688446,6.1996920869149));
#46145=CARTESIAN_POINT('',(0.499999999999999,5.05606744688446,6.1996920869149));
#46146=CARTESIAN_POINT('',(4.75,5.05606744688446,6.1996920869149));
#46147=CARTESIAN_POINT('',(9.,5.04588273603933,6.01344887848398));
#46148=CARTESIAN_POINT('',(9.,5.0595335915088,6.26307590856075));
#46149=CARTESIAN_POINT('',(0.5,5.04588273603933,6.01344887848398));
#46150=CARTESIAN_POINT('',(0.5,5.04588273603933,6.01344887848398));
#46151=CARTESIAN_POINT('',(0.5,5.0595335915088,6.26307590856075));
#46152=CARTESIAN_POINT('Origin',(0.5,5.11016149700799,6.09005332279587));
#46153=CARTESIAN_POINT('',(0.499999999999999,5.22752793516966,6.05581965443332));
#46154=CARTESIAN_POINT('Origin',(0.5,0.,0.));
#46155=CARTESIAN_POINT('',(0.5,5.04588273603933,6.01344887848398));
#46156=CARTESIAN_POINT('Origin',(0.5,5.04588273603933,6.01344887848398));
#46157=CARTESIAN_POINT('',(9.,5.22752793516966,6.05581965443332));
#46158=CARTESIAN_POINT('',(4.75,5.22752793516966,6.05581965443332));
#46159=CARTESIAN_POINT('',(9.,5.04588273603933,6.01344887848398));
#46160=CARTESIAN_POINT('Origin',(9.,5.11016149700799,6.09005332279587));
#46161=CARTESIAN_POINT('Origin',(9.,0.,0.));
#46162=CARTESIAN_POINT('Origin',(0.5,6.07023962565479,5.28934692444449));
#46163=CARTESIAN_POINT('',(9.,6.05581965443332,5.22752793516966));
#46164=CARTESIAN_POINT('',(0.499999999999999,6.05581965443332,5.22752793516966));
#46165=CARTESIAN_POINT('',(4.75,6.05581965443332,5.22752793516966));
#46166=CARTESIAN_POINT('',(9.,6.01344887848398,5.04588273603933));
#46167=CARTESIAN_POINT('',(9.,6.07023962565479,5.28934692444449));
#46168=CARTESIAN_POINT('',(0.5,6.01344887848398,5.04588273603933));
#46169=CARTESIAN_POINT('',(0.5,6.01344887848398,5.04588273603933));
#46170=CARTESIAN_POINT('',(0.5,6.07023962565479,5.28934692444449));
#46171=CARTESIAN_POINT('Origin',(0.5,6.09005332279588,5.11016149700799));
#46172=CARTESIAN_POINT('',(0.499999999999999,6.1996920869149,5.05606744688446));
#46173=CARTESIAN_POINT('Origin',(0.5,0.,0.));
#46174=CARTESIAN_POINT('',(0.5,6.01344887848398,5.04588273603933));
#46175=CARTESIAN_POINT('Origin',(0.5,6.01344887848398,5.04588273603933));
#46176=CARTESIAN_POINT('',(9.,6.1996920869149,5.05606744688446));
#46177=CARTESIAN_POINT('',(4.75,6.1996920869149,5.05606744688446));
#46178=CARTESIAN_POINT('',(9.,6.01344887848398,5.04588273603933));
#46179=CARTESIAN_POINT('Origin',(9.,6.09005332279588,5.11016149700799));
#46180=CARTESIAN_POINT('Origin',(9.,0.,0.));
#46181=CARTESIAN_POINT('Origin',(0.5,6.89650450046473,4.15490381056767));
#46182=CARTESIAN_POINT('',(9.,6.87156884617482,4.09652799237105));
#46183=CARTESIAN_POINT('',(0.499999999999999,6.87156884617482,4.09652799237105));
#46184=CARTESIAN_POINT('',(4.75,6.87156884617482,4.09652799237105));
#46185=CARTESIAN_POINT('',(9.,6.79829941970784,3.925));
#46186=CARTESIAN_POINT('',(9.,6.89650450046473,4.15490381056767));
#46187=CARTESIAN_POINT('',(0.5,6.79829941970784,3.925));
#46188=CARTESIAN_POINT('',(0.5,6.79829941970784,3.925));
#46189=CARTESIAN_POINT('',(0.5,6.89650450046473,4.15490381056767));
#46190=CARTESIAN_POINT('Origin',(0.5,6.88490196008629,3.975));
#46191=CARTESIAN_POINT('',(0.499999999999999,6.98348173179481,3.90268918845559));
#46192=CARTESIAN_POINT('Origin',(0.5,0.,0.));
#46193=CARTESIAN_POINT('',(0.5,6.79829941970784,3.925));
#46194=CARTESIAN_POINT('Origin',(0.5,6.79829941970784,3.925));
#46195=CARTESIAN_POINT('',(9.,6.98348173179481,3.90268918845559));
#46196=CARTESIAN_POINT('',(4.75,6.98348173179481,3.90268918845559));
#46197=CARTESIAN_POINT('',(9.,6.79829941970784,3.925));
#46198=CARTESIAN_POINT('Origin',(9.,6.88490196008629,3.975));
#46199=CARTESIAN_POINT('Origin',(9.,0.,0.));
#46200=CARTESIAN_POINT('Origin',(0.5,7.51322257582771,2.89421604688952));
#46201=CARTESIAN_POINT('',(9.,7.47852889570692,2.84105711946744));
#46202=CARTESIAN_POINT('',(0.499999999999999,7.47852889570692,2.84105711946744));
#46203=CARTESIAN_POINT('',(4.75,7.47852889570692,2.84105711946744));
#46204=CARTESIAN_POINT('',(9.,7.37658707316938,2.6848581251065));
#46205=CARTESIAN_POINT('',(9.,7.51322257582771,2.89421604688952));
#46206=CARTESIAN_POINT('',(0.5,7.37658707316938,2.6848581251065));
#46207=CARTESIAN_POINT('',(0.5,7.37658707316938,2.6848581251065));
#46208=CARTESIAN_POINT('',(0.5,7.51322257582771,2.89421604688952));
#46209=CARTESIAN_POINT('Origin',(0.5,7.47055633524797,2.71906013943907));
#46210=CARTESIAN_POINT('',(0.499999999999999,7.55508181806639,2.63072969389152));
#46211=CARTESIAN_POINT('Origin',(0.5,0.,0.));
#46212=CARTESIAN_POINT('',(0.5,7.37658707316938,2.6848581251065));
#46213=CARTESIAN_POINT('Origin',(0.5,7.37658707316938,2.6848581251065));
#46214=CARTESIAN_POINT('',(9.,7.55508181806639,2.63072969389152));
#46215=CARTESIAN_POINT('',(4.75,7.55508181806639,2.63072969389152));
#46216=CARTESIAN_POINT('',(9.,7.37658707316938,2.6848581251065));
#46217=CARTESIAN_POINT('Origin',(9.,7.47055633524797,2.71906013943907));
#46218=CARTESIAN_POINT('Origin',(9.,0.,0.));
#46219=CARTESIAN_POINT('Origin',(0.5,7.90165518509824,1.54558899317062));
#46220=CARTESIAN_POINT('',(9.,7.85825762906118,1.49926216363308));
#46221=CARTESIAN_POINT('',(0.499999999999999,7.85825762906118,1.49926216363308));
#46222=CARTESIAN_POINT('',(4.75,7.85825762906118,1.49926216363308));
#46223=CARTESIAN_POINT('',(9.,7.73074086114583,1.3631381946854));
#46224=CARTESIAN_POINT('',(9.,7.90165518509824,1.54558899317062));
#46225=CARTESIAN_POINT('',(0.5,7.73074086114583,1.3631381946854));
#46226=CARTESIAN_POINT('',(0.5,7.73074086114583,1.3631381946854));
#46227=CARTESIAN_POINT('',(0.5,7.90165518509824,1.54558899317062));
#46228=CARTESIAN_POINT('Origin',(0.5,7.82922163644705,1.3805030124521));
#46229=CARTESIAN_POINT('',(0.499999999999999,7.8971245663519,1.27883680879202));
#46230=CARTESIAN_POINT('Origin',(0.5,0.,0.));
#46231=CARTESIAN_POINT('',(0.5,7.73074086114583,1.3631381946854));
#46232=CARTESIAN_POINT('Origin',(0.5,7.73074086114583,1.3631381946854));
#46233=CARTESIAN_POINT('',(9.,7.8971245663519,1.27883680879202));
#46234=CARTESIAN_POINT('',(4.75,7.8971245663519,1.27883680879202));
#46235=CARTESIAN_POINT('',(9.,7.73074086114583,1.3631381946854));
#46236=CARTESIAN_POINT('Origin',(9.,7.82922163644705,1.3805030124521));
#46237=CARTESIAN_POINT('Origin',(9.,0.,0.));
#46238=CARTESIAN_POINT('Origin',(0.5,8.05,0.15));
#46239=CARTESIAN_POINT('',(9.,7.99921718082665,0.111912885619985));
#46240=CARTESIAN_POINT('',(0.499999999999999,7.99921718082665,0.111912885619985));
#46241=CARTESIAN_POINT('',(4.75,7.99921718082665,0.111912885619985));
#46242=CARTESIAN_POINT('',(9.,7.85,0.));
#46243=CARTESIAN_POINT('',(9.,8.05,0.15));
#46244=CARTESIAN_POINT('',(0.5,7.85,0.));
#46245=CARTESIAN_POINT('',(0.5,7.85,0.));
#46246=CARTESIAN_POINT('',(0.5,8.05,0.15));
#46247=CARTESIAN_POINT('Origin',(0.5,7.95,0.));
#46248=CARTESIAN_POINT('',(0.499999999999999,7.99921718082665,-0.111912885619987));
#46249=CARTESIAN_POINT('Origin',(0.5,0.,0.));
#46250=CARTESIAN_POINT('',(0.5,7.85,0.));
#46251=CARTESIAN_POINT('Origin',(0.5,7.85,0.));
#46252=CARTESIAN_POINT('',(9.,7.99921718082665,-0.111912885619987));
#46253=CARTESIAN_POINT('',(4.75,7.99921718082665,-0.111912885619987));
#46254=CARTESIAN_POINT('',(9.,7.85,0.));
#46255=CARTESIAN_POINT('Origin',(9.,7.95,0.));
#46256=CARTESIAN_POINT('Origin',(9.,0.,0.));
#46257=CARTESIAN_POINT('Origin',(10.,5.55111512312578E-16,4.61880215351701));
#46258=CARTESIAN_POINT('',(10.,2.82820063659975E-16,4.61880215351701));
#46259=CARTESIAN_POINT('',(10.,4.,2.3094010767585));
#46260=CARTESIAN_POINT('',(10.,1.,4.04145188432738));
#46261=CARTESIAN_POINT('',(5.,5.55111512312578E-16,4.61880215351701));
#46262=CARTESIAN_POINT('',(10.,2.82820063659975E-16,4.61880215351701));
#46263=CARTESIAN_POINT('',(5.,4.,2.3094010767585));
#46264=CARTESIAN_POINT('',(5.,4.,2.3094010767585));
#46265=CARTESIAN_POINT('',(10.,4.,2.3094010767585));
#46266=CARTESIAN_POINT('Origin',(10.,-4.,2.3094010767585));
#46267=CARTESIAN_POINT('',(10.,-4.,2.3094010767585));
#46268=CARTESIAN_POINT('',(10.,-3.,2.88675134594813));
#46269=CARTESIAN_POINT('',(5.,-4.,2.3094010767585));
#46270=CARTESIAN_POINT('',(10.,-4.,2.3094010767585));
#46271=CARTESIAN_POINT('',(5.,2.82820063659975E-16,4.61880215351701));
#46272=CARTESIAN_POINT('Origin',(10.,-4.,-2.3094010767585));
#46273=CARTESIAN_POINT('',(10.,-4.,-2.3094010767585));
#46274=CARTESIAN_POINT('',(10.,-4.,-1.15470053837925));
#46275=CARTESIAN_POINT('',(5.,-4.,-2.3094010767585));
#46276=CARTESIAN_POINT('',(10.,-4.,-2.3094010767585));
#46277=CARTESIAN_POINT('',(5.,-4.,2.3094010767585));
#46278=CARTESIAN_POINT('Origin',(10.,-1.11022302462516E-15,-4.61880215351701));
#46279=CARTESIAN_POINT('',(10.,-8.48460190979926E-16,-4.61880215351701));
#46280=CARTESIAN_POINT('',(10.,-1.,-4.04145188432738));
#46281=CARTESIAN_POINT('',(5.,-1.11022302462516E-15,-4.61880215351701));
#46282=CARTESIAN_POINT('',(10.,-8.48460190979926E-16,-4.61880215351701));
#46283=CARTESIAN_POINT('',(5.,-4.,-2.3094010767585));
#46284=CARTESIAN_POINT('Origin',(10.,4.,-2.30940107675851));
#46285=CARTESIAN_POINT('',(10.,4.,-2.30940107675851));
#46286=CARTESIAN_POINT('',(10.,3.,-2.88675134594813));
#46287=CARTESIAN_POINT('',(5.,4.,-2.30940107675851));
#46288=CARTESIAN_POINT('',(10.,4.,-2.30940107675851));
#46289=CARTESIAN_POINT('',(5.,-8.48460190979926E-16,-4.61880215351701));
#46290=CARTESIAN_POINT('Origin',(10.,4.,2.3094010767585));
#46291=CARTESIAN_POINT('',(10.,4.,1.15470053837925));
#46292=CARTESIAN_POINT('',(5.,4.,-2.30940107675851));
#46293=CARTESIAN_POINT('Origin',(5.,0.,0.));
#46294=CARTESIAN_POINT('Origin',(-90.,4.5,0.));
#46295=CARTESIAN_POINT('',(-90.,-4.5,-5.51091059616309E-16));
#46296=CARTESIAN_POINT('Origin',(-90.,0.,0.));
#46297=CARTESIAN_POINT('Origin',(-89.75,0.,0.));
#46298=CARTESIAN_POINT('',(-89.75,-4.75,-5.81707229594993E-16));
#46299=CARTESIAN_POINT('Origin',(-74.75,0.,0.));
#46300=CARTESIAN_POINT('Origin',(-59.25,0.,0.));
#46301=CARTESIAN_POINT('Origin',(-59.75,0.,0.));
#46302=CARTESIAN_POINT('',(-59.5,-4.95,-6.0620016557794E-16));
#46303=CARTESIAN_POINT('Origin',(-59.5,0.,0.));
#46304=CARTESIAN_POINT('',(-59.75,-4.975,-6.09261782575808E-16));
#46305=CARTESIAN_POINT('Origin',(-29.75,0.,0.));
#46306=CARTESIAN_POINT('',(0.,-4.95,-6.0620016557794E-16));
#46307=CARTESIAN_POINT('Origin',(0.,0.,0.));
#46308=CARTESIAN_POINT('',(-29.75,-4.95,-6.0620016557794E-16));
#46309=CARTESIAN_POINT('Origin',(0.,8.,0.));
#46310=CARTESIAN_POINT('',(5.55111512312578E-16,-8.,-9.79717439317883E-16));
#46311=CARTESIAN_POINT('Origin',(0.,0.,0.));
#46312=CARTESIAN_POINT('Origin',(4.75,0.,0.));
#46313=CARTESIAN_POINT('',(9.5,-8.,-9.79717439317883E-16));
#46314=CARTESIAN_POINT('Origin',(9.5,0.,0.));
#46315=CARTESIAN_POINT('',(4.75,-8.,-9.79717439317883E-16));
#46316=CARTESIAN_POINT('',(4.75,-8.,-9.79717439317883E-16));
#46317=CARTESIAN_POINT('Origin',(9.75,0.,0.));
#46318=CARTESIAN_POINT('',(10.,-7.5,-9.18485099360515E-16));
#46319=CARTESIAN_POINT('Origin',(10.,0.,0.));
#46320=CARTESIAN_POINT('',(9.75,-7.75,-9.49101269339199E-16));
#46321=CARTESIAN_POINT('Origin',(10.,0.,0.));
#46377=UNCERTAINTY_MEASURE_WITH_UNIT(LENGTH_MEASURE(0.01),#46396,
'DISTANCE_ACCURACY_VALUE',
'Maximum model space distance between geometric entities at asserted c
onnectivities');
#46379=UNCERTAINTY_MEASURE_WITH_UNIT(LENGTH_MEASURE(0.01),#46396,
'DISTANCE_ACCURACY_VALUE',
'Maximum model space distance between geometric entities at asserted c
onnectivities');
#46393=(
GEOMETRIC_REPRESENTATION_CONTEXT(3)
GLOBAL_UNCERTAINTY_ASSIGNED_CONTEXT((#46377))
GLOBAL_UNIT_ASSIGNED_CONTEXT((#46396,#46398,#46399))
REPRESENTATION_CONTEXT('','3D')
);
#46395=(
GEOMETRIC_REPRESENTATION_CONTEXT(3)
GLOBAL_UNCERTAINTY_ASSIGNED_CONTEXT((#46379))
GLOBAL_UNIT_ASSIGNED_CONTEXT((#46396,#46398,#46399))
REPRESENTATION_CONTEXT('','3D')
);
#46396=(
LENGTH_UNIT()
NAMED_UNIT(*)
SI_UNIT(.MILLI.,.METRE.)
);
#46398=(
NAMED_UNIT(*)
PLANE_ANGLE_UNIT()
SI_UNIT($,.RADIAN.)
);
#46399=(
NAMED_UNIT(*)
SI_UNIT($,.STERADIAN.)
SOLID_ANGLE_UNIT()
);
#46413=SHAPE_DEFINITION_REPRESENTATION(#46428,#46468);
#46428=PRODUCT_DEFINITION_SHAPE('',$,#46484);
#46468=SHAPE_REPRESENTATION('',(#26605),#46393);
#46470=PRODUCT_DEFINITION_CONTEXT('part definition',#46517,'design');
#46484=PRODUCT_DEFINITION('2026-10-26-00-51-16-707',
'12_Through_Bolt_ISO_4762_M10x90',#46499,#46470);
#46499=PRODUCT_DEFINITION_FORMATION('',$,#46532);
#46517=APPLICATION_CONTEXT(
'Core Data for Automotive Mechanical Design Process');
#46518=PRODUCT_CONTEXT('part definition',#46517,'mechanical');
#46532=PRODUCT('2026-10-26-00-51-16-707',
'12_Through_Bolt_ISO_4762_M10x90',$,(#46518));
#46597=COLOUR_RGB('Black',0.12,0.14,0.17);
#46598=FILL_AREA_STYLE_COLOUR('',#46597);
#46599=FILL_AREA_STYLE('',(#46598));
#46600=SURFACE_STYLE_FILL_AREA(#46599);
#46601=SURFACE_SIDE_STYLE('',(#46600));
#46602=SURFACE_STYLE_USAGE(.BOTH.,#46601);
#46603=PRESENTATION_STYLE_ASSIGNMENT((#46602));
ENDSEC;
END-ISO-10303-21;
